ISO-10303-21;
HEADER;
/* Generated by software containing ST-Developer
 * from STEP Tools, Inc. (www.steptools.com) 
 */

FILE_DESCRIPTION(
/* description */ ('STEP AP214'),
/* implementation_level */ '2;1');

FILE_NAME(
/* name */ 'PUR-HW-4060.step',
/* time_stamp */ '2026-10-07T12:49:37-07:00',
/* author */ (''),
/* organization */ (''),
/* preprocessor_version */ 'ST-DEVELOPER v20.2',
/* originating_system */ 'Autodesk Translation Framework v15.15.0.0',
/* authorisation */ '');

FILE_SCHEMA (('AUTOMOTIVE_DESIGN { 1 0 10303 214 3 1 1 }'));
ENDSEC;

DATA;
#10=MECHANICAL_DESIGN_GEOMETRIC_PRESENTATION_REPRESENTATION('',(#299),#33016);
#202=(
BOUNDED_CURVE()
B_SPLINE_CURVE(2,(#27159,#27160,#27161,#27162,#27163,#27164,#27165,#27166,
#27167,#27168,#27169,#27170,#27171,#27172,#27173,#27174,#27175,#27176,#27177,
#27178,#27179,#27180,#27181,#27182,#27183,#27184,#27185,#27186,#27187,#27188,
#27189,#27190,#27191,#27192,#27193,#27194,#27195,#27196,#27197,#27198,#27199,
#27200,#27201,#27202,#27203,#27204,#27205,#27206,#27207,#27208,#27209,#27210,
#27211,#27212,#27213,#27214,#27215,#27216,#27217,#27218,#27219,#27220,#27221,
#27222,#27223,#27224,#27225,#27226,#27227,#27228,#27229,#27230,#27231,#27232,
#27233,#27234,#27235,#27236,#27237,#27238,#27239,#27240,#27241,#27242,#27243,
#27244,#27245,#27246,#27247,#27248,#27249,#27250,#27251,#27252,#27253,#27254,
#27255,#27256,#27257,#27258,#27259,#27260,#27261,#27262,#27263,#27264,#27265,
#27266,#27267,#27268,#27269,#27270,#27271,#27272,#27273,#27274,#27275,#27276,
#27277,#27278,#27279,#27280,#27281,#27282,#27283,#27284,#27285,#27286,#27287,
#27288,#27289,#27290,#27291,#27292,#27293,#27294,#27295,#27296,#27297,#27298,
#27299,#27300,#27301,#27302,#27303,#27304,#27305,#27306,#27307,#27308,#27309,
#27310,#27311,#27312,#27313,#27314,#27315,#27316,#27317,#27318,#27319,#27320,
#27321,#27322,#27323,#27324,#27325,#27326,#27327,#27328,#27329,#27330,#27331,
#27332,#27333,#27334,#27335,#27336,#27337,#27338,#27339,#27340,#27341,#27342,
#27343,#27344,#27345,#27346,#27347,#27348,#27349,#27350,#27351,#27352,#27353,
#27354,#27355,#27356,#27357,#27358,#27359,#27360,#27361,#27362,#27363,#27364,
#27365,#27366,#27367,#27368,#27369,#27370,#27371,#27372,#27373,#27374,#27375,
#27376,#27377,#27378,#27379,#27380,#27381,#27382,#27383,#27384,#27385,#27386,
#27387,#27388,#27389,#27390,#27391,#27392,#27393,#27394,#27395,#27396,#27397,
#27398,#27399,#27400,#27401,#27402,#27403,#27404,#27405,#27406,#27407,#27408,
#27409,#27410,#27411,#27412,#27413,#27414,#27415,#27416,#27417,#27418,#27419,
#27420,#27421,#27422,#27423,#27424,#27425,#27426,#27427,#27428,#27429,#27430,
#27431,#27432,#27433,#27434,#27435,#27436,#27437,#27438,#27439,#27440,#27441,
#27442,#27443,#27444,#27445,#27446,#27447,#27448,#27449,#27450,#27451,#27452,
#27453,#27454,#27455,#27456,#27457,#27458,#27459,#27460,#27461,#27462,#27463,
#27464,#27465,#27466,#27467,#27468,#27469,#27470,#27471,#27472,#27473,#27474,
#27475,#27476,#27477,#27478,#27479,#27480,#27481,#27482,#27483,#27484,#27485,
#27486,#27487,#27488,#27489,#27490,#27491,#27492,#27493,#27494,#27495,#27496,
#27497,#27498,#27499,#27500,#27501,#27502,#27503,#27504,#27505,#27506,#27507,
#27508,#27509,#27510,#27511,#27512,#27513,#27514,#27515,#27516,#27517,#27518,
#27519,#27520,#27521,#27522,#27523,#27524,#27525,#27526,#27527,#27528,#27529,
#27530,#27531,#27532,#27533,#27534,#27535,#27536,#27537,#27538,#27539,#27540,
#27541,#27542,#27543,#27544,#27545,#27546,#27547,#27548,#27549,#27550,#27551,
#27552,#27553,#27554,#27555,#27556,#27557,#27558,#27559,#27560,#27561,#27562,
#27563,#27564,#27565,#27566,#27567,#27568,#27569,#27570,#27571,#27572,#27573,
#27574,#27575,#27576,#27577,#27578,#27579,#27580,#27581,#27582,#27583,#27584,
#27585,#27586,#27587,#27588,#27589,#27590,#27591,#27592,#27593,#27594,#27595,
#27596,#27597,#27598,#27599,#27600,#27601,#27602,#27603,#27604,#27605,#27606,
#27607,#27608,#27609,#27610,#27611,#27612,#27613,#27614,#27615),
 .UNSPECIFIED.,.F.,.F.)
B_SPLINE_CURVE_WITH_KNOTS((3,2,2,2,2,2,2,2,2,2,2,2,2,2,2,2,2,2,2,2,2,2,
2,2,2,2,2,2,2,2,2,2,2,2,2,2,2,2,2,2,2,2,2,2,2,2,2,2,2,2,2,2,2,2,2,2,2,2,
2,2,2,2,2,2,2,2,2,2,2,2,2,2,2,2,2,2,2,2,2,2,2,2,2,2,2,2,2,2,2,2,2,2,2,2,
2,2,2,2,2,2,2,2,2,2,2,2,2,2,2,2,2,2,2,2,2,2,2,2,2,2,2,2,2,2,2,2,2,2,2,2,
2,2,2,2,2,2,2,2,2,2,2,2,2,2,2,2,2,2,2,2,2,2,2,2,2,2,2,2,2,2,2,2,2,2,2,2,
2,2,2,2,2,2,2,2,2,2,2,2,2,2,2,2,2,2,2,2,2,2,2,2,2,2,2,2,2,2,2,2,2,2,2,2,
2,2,2,2,2,2,2,2,2,2,2,2,2,2,2,2,2,2,2,2,2,2,2,2,2,2,3),(0.,0.0043859649122807,
0.0087719298245614,0.0131578947368421,0.0175438596491228,0.0219298245614035,
0.0263157894736842,0.0307017543859649,0.0350877192982456,0.0394736842105263,
0.043859649122807,0.0482456140350877,0.0526315789473684,0.0570175438596491,
0.0614035087719298,0.0657894736842105,0.0701754385964912,0.0745614035087719,
0.0789473684210526,0.0833333333333333,0.087719298245614,0.0921052631578947,
0.0964912280701754,0.100877192982456,0.105263157894737,0.109649122807018,
0.114035087719298,0.118421052631579,0.12280701754386,0.12719298245614,0.131578947368421,
0.135964912280702,0.140350877192982,0.144736842105263,0.149122807017544,
0.153508771929825,0.157894736842105,0.162280701754386,0.166666666666667,
0.171052631578947,0.175438596491228,0.179824561403509,0.184210526315789,
0.18859649122807,0.192982456140351,0.197368421052632,0.201754385964912,
0.206140350877193,0.210526315789474,0.214912280701754,0.219298245614035,
0.223684210526316,0.228070175438596,0.232456140350877,0.236842105263158,
0.241228070175439,0.245614035087719,0.25,0.254385964912281,0.258771929824561,
0.263157894736842,0.267543859649123,0.271929824561404,0.276315789473684,
0.280701754385965,0.285087719298246,0.289473684210526,0.293859649122807,
0.298245614035088,0.302631578947368,0.307017543859649,0.31140350877193,
0.315789473684211,0.320175438596491,0.324561403508772,0.328947368421053,
0.333333333333333,0.337719298245614,0.342105263157895,0.346491228070175,
0.350877192982456,0.355263157894737,0.359649122807018,0.364035087719298,
0.368421052631579,0.37280701754386,0.37719298245614,0.381578947368421,0.385964912280702,
0.390350877192982,0.394736842105263,0.399122807017544,0.403508771929825,
0.407894736842105,0.412280701754386,0.416666666666667,0.421052631578947,
0.425438596491228,0.429824561403509,0.434210526315789,0.43859649122807,
0.442982456140351,0.447368421052632,0.451754385964912,0.456140350877193,
0.460526315789474,0.464912280701754,0.469298245614035,0.473684210526316,
0.478070175438596,0.482456140350877,0.486842105263158,0.491228070175439,
0.495614035087719,0.5,0.504385964912281,0.508771929824561,0.513157894736842,
0.517543859649123,0.521929824561403,0.526315789473684,0.530701754385965,
0.535087719298246,0.539473684210526,0.543859649122807,0.548245614035088,
0.552631578947368,0.557017543859649,0.56140350877193,0.565789473684211,
0.570175438596491,0.574561403508772,0.578947368421053,0.583333333333333,
0.587719298245614,0.592105263157895,0.596491228070175,0.600877192982456,
0.605263157894737,0.609649122807018,0.614035087719298,0.618421052631579,
0.62280701754386,0.62719298245614,0.631578947368421,0.635964912280702,0.640350877192982,
0.644736842105263,0.649122807017544,0.653508771929825,0.657894736842105,
0.662280701754386,0.666666666666667,0.671052631578947,0.675438596491228,
0.679824561403509,0.684210526315789,0.68859649122807,0.692982456140351,
0.697368421052632,0.701754385964912,0.706140350877193,0.710526315789474,
0.714912280701754,0.719298245614035,0.723684210526316,0.728070175438597,
0.732456140350877,0.736842105263158,0.741228070175439,0.745614035087719,
0.75,0.754385964912281,0.758771929824561,0.763157894736842,0.767543859649123,
0.771929824561403,0.776315789473684,0.780701754385965,0.785087719298246,
0.789473684210526,0.793859649122807,0.798245614035088,0.802631578947368,
0.807017543859649,0.81140350877193,0.815789473684211,0.820175438596491,
0.824561403508772,0.828947368421053,0.833333333333333,0.837719298245614,
0.842105263157895,0.846491228070175,0.850877192982456,0.855263157894737,
0.859649122807018,0.864035087719298,0.868421052631579,0.87280701754386,
0.87719298245614,0.881578947368421,0.885964912280702,0.890350877192982,
0.894736842105263,0.899122807017544,0.903508771929825,0.907894736842105,
0.912280701754386,0.916666666666667,0.921052631578947,0.925438596491228,
0.929824561403509,0.934210526315789,0.93859649122807,0.942982456140351,
0.947368421052632,0.951754385964912,0.956140350877193,0.960526315789474,
0.964912280701754,0.969298245614035,0.973684210526316,0.978070175438597,
0.982456140350877,0.986842105263158,0.991228070175439,0.995614035087719,
1.),.UNSPECIFIED.)
CURVE()
GEOMETRIC_REPRESENTATION_ITEM()
RATIONAL_B_SPLINE_CURVE((1.,0.965925826289068,1.,0.965925826289068,1.,0.965925826289068,
1.,0.965925826289068,1.,0.965925826289068,1.,0.965925826289068,1.,0.965925826289068,
1.,0.965925826289068,1.,0.965925826289068,1.,0.965925826289068,1.,0.965925826289068,
1.,0.965925826289068,1.,0.965925826289068,1.,0.965925826289068,1.,0.965925826289068,
1.,0.965925826289068,1.,0.965925826289068,1.,0.965925826289068,1.,0.965925826289068,
1.,0.965925826289068,1.,0.965925826289068,1.,0.965925826289068,1.,0.965925826289068,
1.,0.965925826289068,1.,0.965925826289068,1.,0.965925826289068,1.,0.965925826289068,
1.,0.965925826289068,1.,0.965925826289068,1.,0.965925826289068,1.,0.965925826289068,
1.,0.965925826289068,1.,0.965925826289068,1.,0.965925826289068,1.,0.965925826289068,
1.,0.965925826289068,1.,0.965925826289068,1.,0.965925826289068,1.,0.965925826289068,
1.,0.965925826289068,1.,0.965925826289068,1.,0.965925826289068,1.,0.965925826289068,
1.,0.965925826289068,1.,0.965925826289068,1.,0.965925826289068,1.,0.965925826289068,
1.,0.965925826289068,1.,0.965925826289068,1.,0.965925826289068,1.,0.965925826289068,
1.,0.965925826289068,1.,0.965925826289068,1.,0.965925826289068,1.,0.965925826289068,
1.,0.965925826289068,1.,0.965925826289068,1.,0.965925826289068,1.,0.965925826289068,
1.,0.965925826289068,1.,0.965925826289068,1.,0.965925826289068,1.,0.965925826289068,
1.,0.965925826289068,1.,0.965925826289068,1.,0.965925826289068,1.,0.965925826289068,
1.,0.965925826289068,1.,0.965925826289068,1.,0.965925826289068,1.,0.965925826289068,
1.,0.965925826289068,1.,0.965925826289068,1.,0.965925826289068,1.,0.965925826289068,
1.,0.965925826289068,1.,0.965925826289068,1.,0.965925826289068,1.,0.965925826289068,
1.,0.965925826289068,1.,0.965925826289068,1.,0.965925826289068,1.,0.965925826289068,
1.,0.965925826289068,1.,0.965925826289068,1.,0.965925826289068,1.,0.965925826289068,
1.,0.965925826289068,1.,0.965925826289068,1.,0.965925826289068,1.,0.965925826289068,
1.,0.965925826289068,1.,0.965925826289068,1.,0.965925826289068,1.,0.965925826289068,
1.,0.965925826289068,1.,0.965925826289068,1.,0.965925826289068,1.,0.965925826289068,
1.,0.965925826289068,1.,0.965925826289068,1.,0.965925826289068,1.,0.965925826289068,
1.,0.965925826289068,1.,0.965925826289068,1.,0.965925826289068,1.,0.965925826289068,
1.,0.965925826289068,1.,0.965925826289068,1.,0.965925826289068,1.,0.965925826289068,
1.,0.965925826289068,1.,0.965925826289068,1.,0.965925826289068,1.,0.965925826289068,
1.,0.965925826289068,1.,0.965925826289068,1.,0.965925826289068,1.,0.965925826289068,
1.,0.965925826289068,1.,0.965925826289068,1.,0.965925826289068,1.,0.965925826289068,
1.,0.965925826289068,1.,0.965925826289068,1.,0.965925826289068,1.,0.965925826289068,
1.,0.965925826289068,1.,0.965925826289068,1.,0.965925826289068,1.,0.965925826289068,
1.,0.965925826289068,1.,0.965925826289068,1.,0.965925826289068,1.,0.965925826289068,
1.,0.965925826289068,1.,0.965925826289068,1.,0.965925826289068,1.,0.965925826289068,
1.,0.965925826289068,1.,0.965925826289068,1.,0.965925826289068,1.,0.965925826289068,
1.,0.965925826289068,1.,0.965925826289068,1.,0.965925826289068,1.,0.965925826289068,
1.,0.965925826289068,1.,0.965925826289068,1.,0.965925826289068,1.,0.965925826289068,
1.,0.965925826289068,1.,0.965925826289068,1.,0.965925826289068,1.,0.965925826289068,
1.,0.965925826289068,1.,0.965925826289068,1.,0.965925826289068,1.,0.965925826289068,
1.,0.965925826289068,1.,0.965925826289068,1.,0.965925826289068,1.,0.965925826289068,
1.,0.965925826289068,1.,0.965925826289068,1.,0.965925826289068,1.,0.965925826289068,
1.,0.965925826289068,1.,0.965925826289068,1.,0.965925826289068,1.,0.965925826289068,
1.,0.965925826289068,1.,0.965925826289068,1.,0.965925826289068,1.,0.965925826289068,
1.,0.965925826289068,1.,0.965925826289068,1.,0.965925826289068,1.,0.965925826289068,
1.,0.965925826289068,1.,0.965925826289068,1.,0.965925826289068,1.,0.965925826289068,
1.,0.965925826289068,1.,0.965925826289068,1.,0.965925826289068,1.,0.965925826289068,
1.,0.965925826289068,1.,0.965925826289068,1.,0.965925826289068,1.,0.965925826289068,
1.,0.965925826289068,1.,0.965925826289068,1.,0.965925826289068,1.,0.965925826289068,
1.,0.965925826289068,1.,0.965925826289068,1.,0.965925826289068,1.,0.965925826289068,
1.,0.965925826289068,1.,0.965925826289068,1.,0.965925826289068,1.,0.965925826289068,
1.,0.965925826289068,1.,0.965925826289068,1.,0.965925826289068,1.,0.965925826289068,
1.,0.965925826289068,1.,0.965925826289068,1.,0.965925826289068,1.,0.965925826289068,
1.,0.965925826289068,1.,0.965925826289068,1.,0.965925826289068,1.,0.965925826289068,
1.,0.965925826289068,1.,0.965925826289068,1.,0.965925826289068,1.,0.965925826289068,
1.,0.965925826289068,1.,0.965925826289068,1.,0.965925826289068,1.,0.965925826289068,
1.,0.965925826289068,1.,0.965925826289068,1.,0.965925826289068,1.,0.965925826289068,
1.,0.965925826289068,1.))
REPRESENTATION_ITEM('')
);
#245=SHAPE_REPRESENTATION_RELATIONSHIP('SRR','None',#33139,#272);
#272=ADVANCED_BREP_SHAPE_REPRESENTATION('',(#330),#33000);
#299=STYLED_ITEM('',(#33285),#330);
#330=MANIFOLD_SOLID_BREP('Body1',#9954);
#459=(
BOUNDED_SURFACE()
B_SPLINE_SURFACE(3,2,((#23960,#23961,#23962,#23963,#23964,#23965,#23966,
#23967,#23968,#23969,#23970,#23971,#23972,#23973,#23974,#23975,#23976,#23977,
#23978,#23979,#23980,#23981,#23982,#23983,#23984,#23985,#23986,#23987,#23988,
#23989,#23990,#23991,#23992,#23993,#23994,#23995,#23996,#23997,#23998,#23999,
#24000,#24001,#24002,#24003,#24004,#24005,#24006,#24007,#24008,#24009,#24010,
#24011,#24012,#24013,#24014,#24015,#24016,#24017,#24018,#24019,#24020,#24021,
#24022,#24023,#24024,#24025,#24026,#24027,#24028,#24029,#24030,#24031,#24032,
#24033,#24034,#24035,#24036,#24037,#24038,#24039,#24040,#24041,#24042,#24043,
#24044,#24045,#24046,#24047,#24048,#24049,#24050,#24051,#24052,#24053,#24054,
#24055,#24056,#24057,#24058,#24059,#24060,#24061,#24062,#24063,#24064,#24065,
#24066,#24067,#24068,#24069,#24070,#24071,#24072,#24073,#24074,#24075,#24076,
#24077,#24078,#24079,#24080,#24081,#24082,#24083,#24084,#24085,#24086,#24087,
#24088,#24089,#24090,#24091,#24092,#24093,#24094,#24095,#24096,#24097,#24098,
#24099,#24100,#24101,#24102,#24103,#24104,#24105,#24106,#24107,#24108,#24109,
#24110,#24111,#24112,#24113,#24114,#24115,#24116,#24117,#24118,#24119,#24120,
#24121,#24122,#24123,#24124,#24125,#24126,#24127,#24128,#24129,#24130,#24131,
#24132,#24133,#24134,#24135,#24136,#24137,#24138,#24139,#24140,#24141,#24142,
#24143,#24144,#24145,#24146,#24147,#24148,#24149,#24150,#24151,#24152,#24153,
#24154,#24155,#24156,#24157,#24158,#24159,#24160,#24161,#24162,#24163,#24164,
#24165,#24166,#24167,#24168,#24169,#24170,#24171,#24172,#24173,#24174,#24175,
#24176,#24177,#24178,#24179,#24180,#24181,#24182,#24183,#24184,#24185,#24186,
#24187,#24188,#24189,#24190,#24191,#24192,#24193,#24194,#24195,#24196,#24197,
#24198,#24199,#24200,#24201,#24202,#24203,#24204,#24205,#24206,#24207,#24208,
#24209,#24210,#24211,#24212,#24213,#24214,#24215,#24216,#24217,#24218,#24219,
#24220,#24221,#24222,#24223,#24224,#24225,#24226,#24227,#24228,#24229,#24230,
#24231,#24232,#24233,#24234,#24235,#24236,#24237,#24238,#24239,#24240,#24241,
#24242,#24243,#24244,#24245,#24246,#24247,#24248,#24249,#24250,#24251,#24252,
#24253,#24254,#24255,#24256,#24257,#24258,#24259,#24260,#24261,#24262,#24263,
#24264,#24265,#24266,#24267,#24268,#24269,#24270,#24271,#24272,#24273,#24274,
#24275,#24276,#24277,#24278,#24279,#24280,#24281,#24282,#24283,#24284,#24285,
#24286,#24287,#24288,#24289,#24290,#24291,#24292,#24293,#24294,#24295,#24296,
#24297,#24298,#24299,#24300,#24301,#24302,#24303,#24304,#24305,#24306,#24307,
#24308,#24309,#24310,#24311,#24312,#24313,#24314,#24315,#24316,#24317,#24318,
#24319,#24320,#24321,#24322,#24323,#24324,#24325,#24326,#24327,#24328,#24329,
#24330,#24331,#24332,#24333,#24334,#24335,#24336,#24337,#24338,#24339,#24340,
#24341,#24342,#24343,#24344,#24345,#24346,#24347,#24348,#24349,#24350,#24351,
#24352,#24353,#24354,#24355,#24356,#24357,#24358,#24359,#24360,#24361,#24362,
#24363,#24364,#24365,#24366,#24367,#24368,#24369,#24370,#24371,#24372,#24373,
#24374,#24375,#24376,#24377,#24378,#24379,#24380,#24381,#24382,#24383,#24384,
#24385,#24386,#24387,#24388,#24389,#24390,#24391,#24392,#24393,#24394,#24395,
#24396,#24397,#24398,#24399,#24400,#24401,#24402,#24403,#24404,#24405,#24406,
#24407,#24408,#24409,#24410,#24411,#24412,#24413,#24414,#24415,#24416),
(#24417,#24418,#24419,#24420,#24421,#24422,#24423,#24424,#24425,#24426,
#24427,#24428,#24429,#24430,#24431,#24432,#24433,#24434,#24435,#24436,#24437,
#24438,#24439,#24440,#24441,#24442,#24443,#24444,#24445,#24446,#24447,#24448,
#24449,#24450,#24451,#24452,#24453,#24454,#24455,#24456,#24457,#24458,#24459,
#24460,#24461,#24462,#24463,#24464,#24465,#24466,#24467,#24468,#24469,#24470,
#24471,#24472,#24473,#24474,#24475,#24476,#24477,#24478,#24479,#24480,#24481,
#24482,#24483,#24484,#24485,#24486,#24487,#24488,#24489,#24490,#24491,#24492,
#24493,#24494,#24495,#24496,#24497,#24498,#24499,#24500,#24501,#24502,#24503,
#24504,#24505,#24506,#24507,#24508,#24509,#24510,#24511,#24512,#24513,#24514,
#24515,#24516,#24517,#24518,#24519,#24520,#24521,#24522,#24523,#24524,#24525,
#24526,#24527,#24528,#24529,#24530,#24531,#24532,#24533,#24534,#24535,#24536,
#24537,#24538,#24539,#24540,#24541,#24542,#24543,#24544,#24545,#24546,#24547,
#24548,#24549,#24550,#24551,#24552,#24553,#24554,#24555,#24556,#24557,#24558,
#24559,#24560,#24561,#24562,#24563,#24564,#24565,#24566,#24567,#24568,#24569,
#24570,#24571,#24572,#24573,#24574,#24575,#24576,#24577,#24578,#24579,#24580,
#24581,#24582,#24583,#24584,#24585,#24586,#24587,#24588,#24589,#24590,#24591,
#24592,#24593,#24594,#24595,#24596,#24597,#24598,#24599,#24600,#24601,#24602,
#24603,#24604,#24605,#24606,#24607,#24608,#24609,#24610,#24611,#24612,#24613,
#24614,#24615,#24616,#24617,#24618,#24619,#24620,#24621,#24622,#24623,#24624,
#24625,#24626,#24627,#24628,#24629,#24630,#24631,#24632,#24633,#24634,#24635,
#24636,#24637,#24638,#24639,#24640,#24641,#24642,#24643,#24644,#24645,#24646,
#24647,#24648,#24649,#24650,#24651,#24652,#24653,#24654,#24655,#24656,#24657,
#24658,#24659,#24660,#24661,#24662,#24663,#24664,#24665,#24666,#24667,#24668,
#24669,#24670,#24671,#24672,#24673,#24674,#24675,#24676,#24677,#24678,#24679,
#24680,#24681,#24682,#24683,#24684,#24685,#24686,#24687,#24688,#24689,#24690,
#24691,#24692,#24693,#24694,#24695,#24696,#24697,#24698,#24699,#24700,#24701,
#24702,#24703,#24704,#24705,#24706,#24707,#24708,#24709,#24710,#24711,#24712,
#24713,#24714,#24715,#24716,#24717,#24718,#24719,#24720,#24721,#24722,#24723,
#24724,#24725,#24726,#24727,#24728,#24729,#24730,#24731,#24732,#24733,#24734,
#24735,#24736,#24737,#24738,#24739,#24740,#24741,#24742,#24743,#24744,#24745,
#24746,#24747,#24748,#24749,#24750,#24751,#24752,#24753,#24754,#24755,#24756,
#24757,#24758,#24759,#24760,#24761,#24762,#24763,#24764,#24765,#24766,#24767,
#24768,#24769,#24770,#24771,#24772,#24773,#24774,#24775,#24776,#24777,#24778,
#24779,#24780,#24781,#24782,#24783,#24784,#24785,#24786,#24787,#24788,#24789,
#24790,#24791,#24792,#24793,#24794,#24795,#24796,#24797,#24798,#24799,#24800,
#24801,#24802,#24803,#24804,#24805,#24806,#24807,#24808,#24809,#24810,#24811,
#24812,#24813,#24814,#24815,#24816,#24817,#24818,#24819,#24820,#24821,#24822,
#24823,#24824,#24825,#24826,#24827,#24828,#24829,#24830,#24831,#24832,#24833,
#24834,#24835,#24836,#24837,#24838,#24839,#24840,#24841,#24842,#24843,#24844,
#24845,#24846,#24847,#24848,#24849,#24850,#24851,#24852,#24853,#24854,#24855,
#24856,#24857,#24858,#24859,#24860,#24861,#24862,#24863,#24864,#24865,#24866,
#24867,#24868,#24869,#24870,#24871,#24872,#24873),(#24874,#24875,#24876,
#24877,#24878,#24879,#24880,#24881,#24882,#24883,#24884,#24885,#24886,#24887,
#24888,#24889,#24890,#24891,#24892,#24893,#24894,#24895,#24896,#24897,#24898,
#24899,#24900,#24901,#24902,#24903,#24904,#24905,#24906,#24907,#24908,#24909,
#24910,#24911,#24912,#24913,#24914,#24915,#24916,#24917,#24918,#24919,#24920,
#24921,#24922,#24923,#24924,#24925,#24926,#24927,#24928,#24929,#24930,#24931,
#24932,#24933,#24934,#24935,#24936,#24937,#24938,#24939,#24940,#24941,#24942,
#24943,#24944,#24945,#24946,#24947,#24948,#24949,#24950,#24951,#24952,#24953,
#24954,#24955,#24956,#24957,#24958,#24959,#24960,#24961,#24962,#24963,#24964,
#24965,#24966,#24967,#24968,#24969,#24970,#24971,#24972,#24973,#24974,#24975,
#24976,#24977,#24978,#24979,#24980,#24981,#24982,#24983,#24984,#24985,#24986,
#24987,#24988,#24989,#24990,#24991,#24992,#24993,#24994,#24995,#24996,#24997,
#24998,#24999,#25000,#25001,#25002,#25003,#25004,#25005,#25006,#25007,#25008,
#25009,#25010,#25011,#25012,#25013,#25014,#25015,#25016,#25017,#25018,#25019,
#25020,#25021,#25022,#25023,#25024,#25025,#25026,#25027,#25028,#25029,#25030,
#25031,#25032,#25033,#25034,#25035,#25036,#25037,#25038,#25039,#25040,#25041,
#25042,#25043,#25044,#25045,#25046,#25047,#25048,#25049,#25050,#25051,#25052,
#25053,#25054,#25055,#25056,#25057,#25058,#25059,#25060,#25061,#25062,#25063,
#25064,#25065,#25066,#25067,#25068,#25069,#25070,#25071,#25072,#25073,#25074,
#25075,#25076,#25077,#25078,#25079,#25080,#25081,#25082,#25083,#25084,#25085,
#25086,#25087,#25088,#25089,#25090,#25091,#25092,#25093,#25094,#25095,#25096,
#25097,#25098,#25099,#25100,#25101,#25102,#25103,#25104,#25105,#25106,#25107,
#25108,#25109,#25110,#25111,#25112,#25113,#25114,#25115,#25116,#25117,#25118,
#25119,#25120,#25121,#25122,#25123,#25124,#25125,#25126,#25127,#25128,#25129,
#25130,#25131,#25132,#25133,#25134,#25135,#25136,#25137,#25138,#25139,#25140,
#25141,#25142,#25143,#25144,#25145,#25146,#25147,#25148,#25149,#25150,#25151,
#25152,#25153,#25154,#25155,#25156,#25157,#25158,#25159,#25160,#25161,#25162,
#25163,#25164,#25165,#25166,#25167,#25168,#25169,#25170,#25171,#25172,#25173,
#25174,#25175,#25176,#25177,#25178,#25179,#25180,#25181,#25182,#25183,#25184,
#25185,#25186,#25187,#25188,#25189,#25190,#25191,#25192,#25193,#25194,#25195,
#25196,#25197,#25198,#25199,#25200,#25201,#25202,#25203,#25204,#25205,#25206,
#25207,#25208,#25209,#25210,#25211,#25212,#25213,#25214,#25215,#25216,#25217,
#25218,#25219,#25220,#25221,#25222,#25223,#25224,#25225,#25226,#25227,#25228,
#25229,#25230,#25231,#25232,#25233,#25234,#25235,#25236,#25237,#25238,#25239,
#25240,#25241,#25242,#25243,#25244,#25245,#25246,#25247,#25248,#25249,#25250,
#25251,#25252,#25253,#25254,#25255,#25256,#25257,#25258,#25259,#25260,#25261,
#25262,#25263,#25264,#25265,#25266,#25267,#25268,#25269,#25270,#25271,#25272,
#25273,#25274,#25275,#25276,#25277,#25278,#25279,#25280,#25281,#25282,#25283,
#25284,#25285,#25286,#25287,#25288,#25289,#25290,#25291,#25292,#25293,#25294,
#25295,#25296,#25297,#25298,#25299,#25300,#25301,#25302,#25303,#25304,#25305,
#25306,#25307,#25308,#25309,#25310,#25311,#25312,#25313,#25314,#25315,#25316,
#25317,#25318,#25319,#25320,#25321,#25322,#25323,#25324,#25325,#25326,#25327,
#25328,#25329,#25330),(#25331,#25332,#25333,#25334,#25335,#25336,#25337,
#25338,#25339,#25340,#25341,#25342,#25343,#25344,#25345,#25346,#25347,#25348,
#25349,#25350,#25351,#25352,#25353,#25354,#25355,#25356,#25357,#25358,#25359,
#25360,#25361,#25362,#25363,#25364,#25365,#25366,#25367,#25368,#25369,#25370,
#25371,#25372,#25373,#25374,#25375,#25376,#25377,#25378,#25379,#25380,#25381,
#25382,#25383,#25384,#25385,#25386,#25387,#25388,#25389,#25390,#25391,#25392,
#25393,#25394,#25395,#25396,#25397,#25398,#25399,#25400,#25401,#25402,#25403,
#25404,#25405,#25406,#25407,#25408,#25409,#25410,#25411,#25412,#25413,#25414,
#25415,#25416,#25417,#25418,#25419,#25420,#25421,#25422,#25423,#25424,#25425,
#25426,#25427,#25428,#25429,#25430,#25431,#25432,#25433,#25434,#25435,#25436,
#25437,#25438,#25439,#25440,#25441,#25442,#25443,#25444,#25445,#25446,#25447,
#25448,#25449,#25450,#25451,#25452,#25453,#25454,#25455,#25456,#25457,#25458,
#25459,#25460,#25461,#25462,#25463,#25464,#25465,#25466,#25467,#25468,#25469,
#25470,#25471,#25472,#25473,#25474,#25475,#25476,#25477,#25478,#25479,#25480,
#25481,#25482,#25483,#25484,#25485,#25486,#25487,#25488,#25489,#25490,#25491,
#25492,#25493,#25494,#25495,#25496,#25497,#25498,#25499,#25500,#25501,#25502,
#25503,#25504,#25505,#25506,#25507,#25508,#25509,#25510,#25511,#25512,#25513,
#25514,#25515,#25516,#25517,#25518,#25519,#25520,#25521,#25522,#25523,#25524,
#25525,#25526,#25527,#25528,#25529,#25530,#25531,#25532,#25533,#25534,#25535,
#25536,#25537,#25538,#25539,#25540,#25541,#25542,#25543,#25544,#25545,#25546,
#25547,#25548,#25549,#25550,#25551,#25552,#25553,#25554,#25555,#25556,#25557,
#25558,#25559,#25560,#25561,#25562,#25563,#25564,#25565,#25566,#25567,#25568,
#25569,#25570,#25571,#25572,#25573,#25574,#25575,#25576,#25577,#25578,#25579,
#25580,#25581,#25582,#25583,#25584,#25585,#25586,#25587,#25588,#25589,#25590,
#25591,#25592,#25593,#25594,#25595,#25596,#25597,#25598,#25599,#25600,#25601,
#25602,#25603,#25604,#25605,#25606,#25607,#25608,#25609,#25610,#25611,#25612,
#25613,#25614,#25615,#25616,#25617,#25618,#25619,#25620,#25621,#25622,#25623,
#25624,#25625,#25626,#25627,#25628,#25629,#25630,#25631,#25632,#25633,#25634,
#25635,#25636,#25637,#25638,#25639,#25640,#25641,#25642,#25643,#25644,#25645,
#25646,#25647,#25648,#25649,#25650,#25651,#25652,#25653,#25654,#25655,#25656,
#25657,#25658,#25659,#25660,#25661,#25662,#25663,#25664,#25665,#25666,#25667,
#25668,#25669,#25670,#25671,#25672,#25673,#25674,#25675,#25676,#25677,#25678,
#25679,#25680,#25681,#25682,#25683,#25684,#25685,#25686,#25687,#25688,#25689,
#25690,#25691,#25692,#25693,#25694,#25695,#25696,#25697,#25698,#25699,#25700,
#25701,#25702,#25703,#25704,#25705,#25706,#25707,#25708,#25709,#25710,#25711,
#25712,#25713,#25714,#25715,#25716,#25717,#25718,#25719,#25720,#25721,#25722,
#25723,#25724,#25725,#25726,#25727,#25728,#25729,#25730,#25731,#25732,#25733,
#25734,#25735,#25736,#25737,#25738,#25739,#25740,#25741,#25742,#25743,#25744,
#25745,#25746,#25747,#25748,#25749,#25750,#25751,#25752,#25753,#25754,#25755,
#25756,#25757,#25758,#25759,#25760,#25761,#25762,#25763,#25764,#25765,#25766,
#25767,#25768,#25769,#25770,#25771,#25772,#25773,#25774,#25775,#25776,#25777,
#25778,#25779,#25780,#25781,#25782,#25783,#25784,#25785,#25786,#25787),
(#25788,#25789,#25790,#25791,#25792,#25793,#25794,#25795,#25796,#25797,
#25798,#25799,#25800,#25801,#25802,#25803,#25804,#25805,#25806,#25807,#25808,
#25809,#25810,#25811,#25812,#25813,#25814,#25815,#25816,#25817,#25818,#25819,
#25820,#25821,#25822,#25823,#25824,#25825,#25826,#25827,#25828,#25829,#25830,
#25831,#25832,#25833,#25834,#25835,#25836,#25837,#25838,#25839,#25840,#25841,
#25842,#25843,#25844,#25845,#25846,#25847,#25848,#25849,#25850,#25851,#25852,
#25853,#25854,#25855,#25856,#25857,#25858,#25859,#25860,#25861,#25862,#25863,
#25864,#25865,#25866,#25867,#25868,#25869,#25870,#25871,#25872,#25873,#25874,
#25875,#25876,#25877,#25878,#25879,#25880,#25881,#25882,#25883,#25884,#25885,
#25886,#25887,#25888,#25889,#25890,#25891,#25892,#25893,#25894,#25895,#25896,
#25897,#25898,#25899,#25900,#25901,#25902,#25903,#25904,#25905,#25906,#25907,
#25908,#25909,#25910,#25911,#25912,#25913,#25914,#25915,#25916,#25917,#25918,
#25919,#25920,#25921,#25922,#25923,#25924,#25925,#25926,#25927,#25928,#25929,
#25930,#25931,#25932,#25933,#25934,#25935,#25936,#25937,#25938,#25939,#25940,
#25941,#25942,#25943,#25944,#25945,#25946,#25947,#25948,#25949,#25950,#25951,
#25952,#25953,#25954,#25955,#25956,#25957,#25958,#25959,#25960,#25961,#25962,
#25963,#25964,#25965,#25966,#25967,#25968,#25969,#25970,#25971,#25972,#25973,
#25974,#25975,#25976,#25977,#25978,#25979,#25980,#25981,#25982,#25983,#25984,
#25985,#25986,#25987,#25988,#25989,#25990,#25991,#25992,#25993,#25994,#25995,
#25996,#25997,#25998,#25999,#26000,#26001,#26002,#26003,#26004,#26005,#26006,
#26007,#26008,#26009,#26010,#26011,#26012,#26013,#26014,#26015,#26016,#26017,
#26018,#26019,#26020,#26021,#26022,#26023,#26024,#26025,#26026,#26027,#26028,
#26029,#26030,#26031,#26032,#26033,#26034,#26035,#26036,#26037,#26038,#26039,
#26040,#26041,#26042,#26043,#26044,#26045,#26046,#26047,#26048,#26049,#26050,
#26051,#26052,#26053,#26054,#26055,#26056,#26057,#26058,#26059,#26060,#26061,
#26062,#26063,#26064,#26065,#26066,#26067,#26068,#26069,#26070,#26071,#26072,
#26073,#26074,#26075,#26076,#26077,#26078,#26079,#26080,#26081,#26082,#26083,
#26084,#26085,#26086,#26087,#26088,#26089,#26090,#26091,#26092,#26093,#26094,
#26095,#26096,#26097,#26098,#26099,#26100,#26101,#26102,#26103,#26104,#26105,
#26106,#26107,#26108,#26109,#26110,#26111,#26112,#26113,#26114,#26115,#26116,
#26117,#26118,#26119,#26120,#26121,#26122,#26123,#26124,#26125,#26126,#26127,
#26128,#26129,#26130,#26131,#26132,#26133,#26134,#26135,#26136,#26137,#26138,
#26139,#26140,#26141,#26142,#26143,#26144,#26145,#26146,#26147,#26148,#26149,
#26150,#26151,#26152,#26153,#26154,#26155,#26156,#26157,#26158,#26159,#26160,
#26161,#26162,#26163,#26164,#26165,#26166,#26167,#26168,#26169,#26170,#26171,
#26172,#26173,#26174,#26175,#26176,#26177,#26178,#26179,#26180,#26181,#26182,
#26183,#26184,#26185,#26186,#26187,#26188,#26189,#26190,#26191,#26192,#26193,
#26194,#26195,#26196,#26197,#26198,#26199,#26200,#26201,#26202,#26203,#26204,
#26205,#26206,#26207,#26208,#26209,#26210,#26211,#26212,#26213,#26214,#26215,
#26216,#26217,#26218,#26219,#26220,#26221,#26222,#26223,#26224,#26225,#26226,
#26227,#26228,#26229,#26230,#26231,#26232,#26233,#26234,#26235,#26236,#26237,
#26238,#26239,#26240,#26241,#26242,#26243,#26244),(#26245,#26246,#26247,
#26248,#26249,#26250,#26251,#26252,#26253,#26254,#26255,#26256,#26257,#26258,
#26259,#26260,#26261,#26262,#26263,#26264,#26265,#26266,#26267,#26268,#26269,
#26270,#26271,#26272,#26273,#26274,#26275,#26276,#26277,#26278,#26279,#26280,
#26281,#26282,#26283,#26284,#26285,#26286,#26287,#26288,#26289,#26290,#26291,
#26292,#26293,#26294,#26295,#26296,#26297,#26298,#26299,#26300,#26301,#26302,
#26303,#26304,#26305,#26306,#26307,#26308,#26309,#26310,#26311,#26312,#26313,
#26314,#26315,#26316,#26317,#26318,#26319,#26320,#26321,#26322,#26323,#26324,
#26325,#26326,#26327,#26328,#26329,#26330,#26331,#26332,#26333,#26334,#26335,
#26336,#26337,#26338,#26339,#26340,#26341,#26342,#26343,#26344,#26345,#26346,
#26347,#26348,#26349,#26350,#26351,#26352,#26353,#26354,#26355,#26356,#26357,
#26358,#26359,#26360,#26361,#26362,#26363,#26364,#26365,#26366,#26367,#26368,
#26369,#26370,#26371,#26372,#26373,#26374,#26375,#26376,#26377,#26378,#26379,
#26380,#26381,#26382,#26383,#26384,#26385,#26386,#26387,#26388,#26389,#26390,
#26391,#26392,#26393,#26394,#26395,#26396,#26397,#26398,#26399,#26400,#26401,
#26402,#26403,#26404,#26405,#26406,#26407,#26408,#26409,#26410,#26411,#26412,
#26413,#26414,#26415,#26416,#26417,#26418,#26419,#26420,#26421,#26422,#26423,
#26424,#26425,#26426,#26427,#26428,#26429,#26430,#26431,#26432,#26433,#26434,
#26435,#26436,#26437,#26438,#26439,#26440,#26441,#26442,#26443,#26444,#26445,
#26446,#26447,#26448,#26449,#26450,#26451,#26452,#26453,#26454,#26455,#26456,
#26457,#26458,#26459,#26460,#26461,#26462,#26463,#26464,#26465,#26466,#26467,
#26468,#26469,#26470,#26471,#26472,#26473,#26474,#26475,#26476,#26477,#26478,
#26479,#26480,#26481,#26482,#26483,#26484,#26485,#26486,#26487,#26488,#26489,
#26490,#26491,#26492,#26493,#26494,#26495,#26496,#26497,#26498,#26499,#26500,
#26501,#26502,#26503,#26504,#26505,#26506,#26507,#26508,#26509,#26510,#26511,
#26512,#26513,#26514,#26515,#26516,#26517,#26518,#26519,#26520,#26521,#26522,
#26523,#26524,#26525,#26526,#26527,#26528,#26529,#26530,#26531,#26532,#26533,
#26534,#26535,#26536,#26537,#26538,#26539,#26540,#26541,#26542,#26543,#26544,
#26545,#26546,#26547,#26548,#26549,#26550,#26551,#26552,#26553,#26554,#26555,
#26556,#26557,#26558,#26559,#26560,#26561,#26562,#26563,#26564,#26565,#26566,
#26567,#26568,#26569,#26570,#26571,#26572,#26573,#26574,#26575,#26576,#26577,
#26578,#26579,#26580,#26581,#26582,#26583,#26584,#26585,#26586,#26587,#26588,
#26589,#26590,#26591,#26592,#26593,#26594,#26595,#26596,#26597,#26598,#26599,
#26600,#26601,#26602,#26603,#26604,#26605,#26606,#26607,#26608,#26609,#26610,
#26611,#26612,#26613,#26614,#26615,#26616,#26617,#26618,#26619,#26620,#26621,
#26622,#26623,#26624,#26625,#26626,#26627,#26628,#26629,#26630,#26631,#26632,
#26633,#26634,#26635,#26636,#26637,#26638,#26639,#26640,#26641,#26642,#26643,
#26644,#26645,#26646,#26647,#26648,#26649,#26650,#26651,#26652,#26653,#26654,
#26655,#26656,#26657,#26658,#26659,#26660,#26661,#26662,#26663,#26664,#26665,
#26666,#26667,#26668,#26669,#26670,#26671,#26672,#26673,#26674,#26675,#26676,
#26677,#26678,#26679,#26680,#26681,#26682,#26683,#26684,#26685,#26686,#26687,
#26688,#26689,#26690,#26691,#26692,#26693,#26694,#26695,#26696,#26697,#26698,
#26699,#26700,#26701),(#26702,#26703,#26704,#26705,#26706,#26707,#26708,
#26709,#26710,#26711,#26712,#26713,#26714,#26715,#26716,#26717,#26718,#26719,
#26720,#26721,#26722,#26723,#26724,#26725,#26726,#26727,#26728,#26729,#26730,
#26731,#26732,#26733,#26734,#26735,#26736,#26737,#26738,#26739,#26740,#26741,
#26742,#26743,#26744,#26745,#26746,#26747,#26748,#26749,#26750,#26751,#26752,
#26753,#26754,#26755,#26756,#26757,#26758,#26759,#26760,#26761,#26762,#26763,
#26764,#26765,#26766,#26767,#26768,#26769,#26770,#26771,#26772,#26773,#26774,
#26775,#26776,#26777,#26778,#26779,#26780,#26781,#26782,#26783,#26784,#26785,
#26786,#26787,#26788,#26789,#26790,#26791,#26792,#26793,#26794,#26795,#26796,
#26797,#26798,#26799,#26800,#26801,#26802,#26803,#26804,#26805,#26806,#26807,
#26808,#26809,#26810,#26811,#26812,#26813,#26814,#26815,#26816,#26817,#26818,
#26819,#26820,#26821,#26822,#26823,#26824,#26825,#26826,#26827,#26828,#26829,
#26830,#26831,#26832,#26833,#26834,#26835,#26836,#26837,#26838,#26839,#26840,
#26841,#26842,#26843,#26844,#26845,#26846,#26847,#26848,#26849,#26850,#26851,
#26852,#26853,#26854,#26855,#26856,#26857,#26858,#26859,#26860,#26861,#26862,
#26863,#26864,#26865,#26866,#26867,#26868,#26869,#26870,#26871,#26872,#26873,
#26874,#26875,#26876,#26877,#26878,#26879,#26880,#26881,#26882,#26883,#26884,
#26885,#26886,#26887,#26888,#26889,#26890,#26891,#26892,#26893,#26894,#26895,
#26896,#26897,#26898,#26899,#26900,#26901,#26902,#26903,#26904,#26905,#26906,
#26907,#26908,#26909,#26910,#26911,#26912,#26913,#26914,#26915,#26916,#26917,
#26918,#26919,#26920,#26921,#26922,#26923,#26924,#26925,#26926,#26927,#26928,
#26929,#26930,#26931,#26932,#26933,#26934,#26935,#26936,#26937,#26938,#26939,
#26940,#26941,#26942,#26943,#26944,#26945,#26946,#26947,#26948,#26949,#26950,
#26951,#26952,#26953,#26954,#26955,#26956,#26957,#26958,#26959,#26960,#26961,
#26962,#26963,#26964,#26965,#26966,#26967,#26968,#26969,#26970,#26971,#26972,
#26973,#26974,#26975,#26976,#26977,#26978,#26979,#26980,#26981,#26982,#26983,
#26984,#26985,#26986,#26987,#26988,#26989,#26990,#26991,#26992,#26993,#26994,
#26995,#26996,#26997,#26998,#26999,#27000,#27001,#27002,#27003,#27004,#27005,
#27006,#27007,#27008,#27009,#27010,#27011,#27012,#27013,#27014,#27015,#27016,
#27017,#27018,#27019,#27020,#27021,#27022,#27023,#27024,#27025,#27026,#27027,
#27028,#27029,#27030,#27031,#27032,#27033,#27034,#27035,#27036,#27037,#27038,
#27039,#27040,#27041,#27042,#27043,#27044,#27045,#27046,#27047,#27048,#27049,
#27050,#27051,#27052,#27053,#27054,#27055,#27056,#27057,#27058,#27059,#27060,
#27061,#27062,#27063,#27064,#27065,#27066,#27067,#27068,#27069,#27070,#27071,
#27072,#27073,#27074,#27075,#27076,#27077,#27078,#27079,#27080,#27081,#27082,
#27083,#27084,#27085,#27086,#27087,#27088,#27089,#27090,#27091,#27092,#27093,
#27094,#27095,#27096,#27097,#27098,#27099,#27100,#27101,#27102,#27103,#27104,
#27105,#27106,#27107,#27108,#27109,#27110,#27111,#27112,#27113,#27114,#27115,
#27116,#27117,#27118,#27119,#27120,#27121,#27122,#27123,#27124,#27125,#27126,
#27127,#27128,#27129,#27130,#27131,#27132,#27133,#27134,#27135,#27136,#27137,
#27138,#27139,#27140,#27141,#27142,#27143,#27144,#27145,#27146,#27147,#27148,
#27149,#27150,#27151,#27152,#27153,#27154,#27155,#27156,#27157,#27158)),
 .UNSPECIFIED.,.T.,.F.,.F.)
B_SPLINE_SURFACE_WITH_KNOTS((4,3,4),(3,2,2,2,2,2,2,2,2,2,2,2,2,2,2,2,2,
2,2,2,2,2,2,2,2,2,2,2,2,2,2,2,2,2,2,2,2,2,2,2,2,2,2,2,2,2,2,2,2,2,2,2,2,
2,2,2,2,2,2,2,2,2,2,2,2,2,2,2,2,2,2,2,2,2,2,2,2,2,2,2,2,2,2,2,2,2,2,2,2,
2,2,2,2,2,2,2,2,2,2,2,2,2,2,2,2,2,2,2,2,2,2,2,2,2,2,2,2,2,2,2,2,2,2,2,2,
2,2,2,2,2,2,2,2,2,2,2,2,2,2,2,2,2,2,2,2,2,2,2,2,2,2,2,2,2,2,2,2,2,2,2,2,
2,2,2,2,2,2,2,2,2,2,2,2,2,2,2,2,2,2,2,2,2,2,2,2,2,2,2,2,2,2,2,2,2,2,2,2,
2,2,2,2,2,2,2,2,2,2,2,2,2,2,2,2,2,2,2,2,2,2,2,2,2,2,2,2,2,2,2,3),(0.,0.5,
1.),(0.,0.0043859649122807,0.0087719298245614,0.0131578947368421,0.0175438596491228,
0.0219298245614035,0.0263157894736842,0.0307017543859649,0.0350877192982456,
0.0394736842105263,0.043859649122807,0.0482456140350877,0.0526315789473684,
0.0570175438596491,0.0614035087719298,0.0657894736842105,0.0701754385964912,
0.0745614035087719,0.0789473684210526,0.0833333333333333,0.087719298245614,
0.0921052631578947,0.0964912280701754,0.100877192982456,0.105263157894737,
0.109649122807018,0.114035087719298,0.118421052631579,0.12280701754386,
0.12719298245614,0.131578947368421,0.135964912280702,0.140350877192982,
0.144736842105263,0.149122807017544,0.153508771929825,0.157894736842105,
0.162280701754386,0.166666666666667,0.171052631578947,0.175438596491228,
0.179824561403509,0.184210526315789,0.18859649122807,0.192982456140351,
0.197368421052632,0.201754385964912,0.206140350877193,0.210526315789474,
0.214912280701754,0.219298245614035,0.223684210526316,0.228070175438596,
0.232456140350877,0.236842105263158,0.241228070175439,0.245614035087719,
0.25,0.254385964912281,0.258771929824561,0.263157894736842,0.267543859649123,
0.271929824561404,0.276315789473684,0.280701754385965,0.285087719298246,
0.289473684210526,0.293859649122807,0.298245614035088,0.302631578947368,
0.307017543859649,0.31140350877193,0.315789473684211,0.320175438596491,
0.324561403508772,0.328947368421053,0.333333333333333,0.337719298245614,
0.342105263157895,0.346491228070175,0.350877192982456,0.355263157894737,
0.359649122807018,0.364035087719298,0.368421052631579,0.37280701754386,
0.37719298245614,0.381578947368421,0.385964912280702,0.390350877192982,
0.394736842105263,0.399122807017544,0.403508771929825,0.407894736842105,
0.412280701754386,0.416666666666667,0.421052631578947,0.425438596491228,
0.429824561403509,0.434210526315789,0.43859649122807,0.442982456140351,
0.447368421052632,0.451754385964912,0.456140350877193,0.460526315789474,
0.464912280701754,0.469298245614035,0.473684210526316,0.478070175438596,
0.482456140350877,0.486842105263158,0.491228070175439,0.495614035087719,
0.5,0.504385964912281,0.508771929824561,0.513157894736842,0.517543859649123,
0.521929824561403,0.526315789473684,0.530701754385965,0.535087719298246,
0.539473684210526,0.543859649122807,0.548245614035088,0.552631578947368,
0.557017543859649,0.56140350877193,0.565789473684211,0.570175438596491,
0.574561403508772,0.578947368421053,0.583333333333333,0.587719298245614,
0.592105263157895,0.596491228070175,0.600877192982456,0.605263157894737,
0.609649122807018,0.614035087719298,0.618421052631579,0.62280701754386,
0.62719298245614,0.631578947368421,0.635964912280702,0.640350877192982,
0.644736842105263,0.649122807017544,0.653508771929825,0.657894736842105,
0.662280701754386,0.666666666666667,0.671052631578947,0.675438596491228,
0.679824561403509,0.684210526315789,0.68859649122807,0.692982456140351,
0.697368421052632,0.701754385964912,0.706140350877193,0.710526315789474,
0.714912280701754,0.719298245614035,0.723684210526316,0.728070175438597,
0.732456140350877,0.736842105263158,0.741228070175439,0.745614035087719,
0.75,0.754385964912281,0.758771929824561,0.763157894736842,0.767543859649123,
0.771929824561403,0.776315789473684,0.780701754385965,0.785087719298246,
0.789473684210526,0.793859649122807,0.798245614035088,0.802631578947368,
0.807017543859649,0.81140350877193,0.815789473684211,0.820175438596491,
0.824561403508772,0.828947368421053,0.833333333333333,0.837719298245614,
0.842105263157895,0.846491228070175,0.850877192982456,0.855263157894737,
0.859649122807018,0.864035087719298,0.868421052631579,0.87280701754386,
0.87719298245614,0.881578947368421,0.885964912280702,0.890350877192982,
0.894736842105263,0.899122807017544,0.903508771929825,0.907894736842105,
0.912280701754386,0.916666666666667,0.921052631578947,0.925438596491228,
0.929824561403509,0.934210526315789,0.93859649122807,0.942982456140351,
0.947368421052632,0.951754385964912,0.956140350877193,0.960526315789474,
0.964912280701754,0.969298245614035,0.973684210526316,0.978070175438597,
0.982456140350877,0.986842105263158,0.991228070175439,0.995614035087719,
1.),.UNSPECIFIED.)
GEOMETRIC_REPRESENTATION_ITEM()
RATIONAL_B_SPLINE_SURFACE(((1.,0.965925826289068,1.,0.965925826289068,1.,
0.965925826289068,1.,0.965925826289068,1.,0.965925826289068,1.,0.965925826289068,
1.,0.965925826289068,1.,0.965925826289068,1.,0.965925826289068,1.,0.965925826289068,
1.,0.965925826289068,1.,0.965925826289068,1.,0.965925826289068,1.,0.965925826289068,
1.,0.965925826289068,1.,0.965925826289068,1.,0.965925826289068,1.,0.965925826289068,
1.,0.965925826289068,1.,0.965925826289068,1.,0.965925826289068,1.,0.965925826289068,
1.,0.965925826289068,1.,0.965925826289068,1.,0.965925826289068,1.,0.965925826289068,
1.,0.965925826289068,1.,0.965925826289068,1.,0.965925826289068,1.,0.965925826289068,
1.,0.965925826289068,1.,0.965925826289068,1.,0.965925826289068,1.,0.965925826289068,
1.,0.965925826289068,1.,0.965925826289068,1.,0.965925826289068,1.,0.965925826289068,
1.,0.965925826289068,1.,0.965925826289068,1.,0.965925826289068,1.,0.965925826289068,
1.,0.965925826289068,1.,0.965925826289068,1.,0.965925826289068,1.,0.965925826289068,
1.,0.965925826289068,1.,0.965925826289068,1.,0.965925826289068,1.,0.965925826289068,
1.,0.965925826289068,1.,0.965925826289068,1.,0.965925826289068,1.,0.965925826289068,
1.,0.965925826289068,1.,0.965925826289068,1.,0.965925826289068,1.,0.965925826289068,
1.,0.965925826289068,1.,0.965925826289068,1.,0.965925826289068,1.,0.965925826289068,
1.,0.965925826289068,1.,0.965925826289068,1.,0.965925826289068,1.,0.965925826289068,
1.,0.965925826289068,1.,0.965925826289068,1.,0.965925826289068,1.,0.965925826289068,
1.,0.965925826289068,1.,0.965925826289068,1.,0.965925826289068,1.,0.965925826289068,
1.,0.965925826289068,1.,0.965925826289068,1.,0.965925826289068,1.,0.965925826289068,
1.,0.965925826289068,1.,0.965925826289068,1.,0.965925826289068,1.,0.965925826289068,
1.,0.965925826289068,1.,0.965925826289068,1.,0.965925826289068,1.,0.965925826289068,
1.,0.965925826289068,1.,0.965925826289068,1.,0.965925826289068,1.,0.965925826289068,
1.,0.965925826289068,1.,0.965925826289068,1.,0.965925826289068,1.,0.965925826289068,
1.,0.965925826289068,1.,0.965925826289068,1.,0.965925826289068,1.,0.965925826289068,
1.,0.965925826289068,1.,0.965925826289068,1.,0.965925826289068,1.,0.965925826289068,
1.,0.965925826289068,1.,0.965925826289068,1.,0.965925826289068,1.,0.965925826289068,
1.,0.965925826289068,1.,0.965925826289068,1.,0.965925826289068,1.,0.965925826289068,
1.,0.965925826289068,1.,0.965925826289068,1.,0.965925826289068,1.,0.965925826289068,
1.,0.965925826289068,1.,0.965925826289068,1.,0.965925826289068,1.,0.965925826289068,
1.,0.965925826289068,1.,0.965925826289068,1.,0.965925826289068,1.,0.965925826289068,
1.,0.965925826289068,1.,0.965925826289068,1.,0.965925826289068,1.,0.965925826289068,
1.,0.965925826289068,1.,0.965925826289068,1.,0.965925826289068,1.,0.965925826289068,
1.,0.965925826289068,1.,0.965925826289068,1.,0.965925826289068,1.,0.965925826289068,
1.,0.965925826289068,1.,0.965925826289068,1.,0.965925826289068,1.,0.965925826289068,
1.,0.965925826289068,1.,0.965925826289068,1.,0.965925826289068,1.,0.965925826289068,
1.,0.965925826289068,1.,0.965925826289068,1.,0.965925826289068,1.,0.965925826289068,
1.,0.965925826289068,1.,0.965925826289068,1.,0.965925826289068,1.,0.965925826289068,
1.,0.965925826289068,1.,0.965925826289068,1.,0.965925826289068,1.,0.965925826289068,
1.,0.965925826289068,1.,0.965925826289068,1.,0.965925826289068,1.,0.965925826289068,
1.,0.965925826289068,1.,0.965925826289068,1.,0.965925826289068,1.,0.965925826289068,
1.,0.965925826289068,1.,0.965925826289068,1.,0.965925826289068,1.,0.965925826289068,
1.,0.965925826289068,1.,0.965925826289068,1.,0.965925826289068,1.,0.965925826289068,
1.,0.965925826289068,1.,0.965925826289068,1.,0.965925826289068,1.,0.965925826289068,
1.,0.965925826289068,1.,0.965925826289068,1.,0.965925826289068,1.,0.965925826289068,
1.,0.965925826289068,1.,0.965925826289068,1.,0.965925826289068,1.,0.965925826289068,
1.,0.965925826289068,1.,0.965925826289068,1.,0.965925826289068,1.,0.965925826289068,
1.,0.965925826289068,1.,0.965925826289068,1.,0.965925826289068,1.,0.965925826289068,
1.,0.965925826289068,1.,0.965925826289068,1.,0.965925826289068,1.,0.965925826289068,
1.,0.965925826289068,1.,0.965925826289068,1.,0.965925826289068,1.,0.965925826289068,
1.,0.965925826289068,1.,0.965925826289068,1.,0.965925826289068,1.,0.965925826289068,
1.,0.965925826289068,1.,0.965925826289068,1.,0.965925826289068,1.,0.965925826289068,
1.,0.965925826289068,1.,0.965925826289068,1.,0.965925826289068,1.,0.965925826289068,
1.,0.965925826289068,1.,0.965925826289068,1.,0.965925826289068,1.,0.965925826289068,
1.,0.965925826289068,1.,0.965925826289068,1.,0.965925826289068,1.,0.965925826289068,
1.,0.965925826289068,1.,0.965925826289068,1.,0.965925826289068,1.,0.965925826289068,
1.,0.965925826289068,1.,0.965925826289068,1.,0.965925826289068,1.,0.965925826289068,
1.,0.965925826289068,1.,0.965925826289068,1.),(0.333333333333333,0.321975275429689,
0.333333333333333,0.321975275429689,0.333333333333333,0.321975275429689,
0.333333333333333,0.321975275429689,0.333333333333333,0.321975275429689,
0.333333333333333,0.321975275429689,0.333333333333333,0.321975275429689,
0.333333333333333,0.321975275429689,0.333333333333333,0.321975275429689,
0.333333333333333,0.321975275429689,0.333333333333333,0.321975275429689,
0.333333333333333,0.321975275429689,0.333333333333333,0.321975275429689,
0.333333333333333,0.321975275429689,0.333333333333333,0.321975275429689,
0.333333333333333,0.321975275429689,0.333333333333333,0.321975275429689,
0.333333333333333,0.321975275429689,0.333333333333333,0.321975275429689,
0.333333333333333,0.321975275429689,0.333333333333333,0.321975275429689,
0.333333333333333,0.321975275429689,0.333333333333333,0.321975275429689,
0.333333333333333,0.321975275429689,0.333333333333333,0.321975275429689,
0.333333333333333,0.321975275429689,0.333333333333333,0.321975275429689,
0.333333333333333,0.321975275429689,0.333333333333333,0.321975275429689,
0.333333333333333,0.321975275429689,0.333333333333333,0.321975275429689,
0.333333333333333,0.321975275429689,0.333333333333333,0.321975275429689,
0.333333333333333,0.321975275429689,0.333333333333333,0.321975275429689,
0.333333333333333,0.321975275429689,0.333333333333333,0.321975275429689,
0.333333333333333,0.321975275429689,0.333333333333333,0.321975275429689,
0.333333333333333,0.321975275429689,0.333333333333333,0.321975275429689,
0.333333333333333,0.321975275429689,0.333333333333333,0.321975275429689,
0.333333333333333,0.321975275429689,0.333333333333333,0.321975275429689,
0.333333333333333,0.321975275429689,0.333333333333333,0.321975275429689,
0.333333333333333,0.321975275429689,0.333333333333333,0.321975275429689,
0.333333333333333,0.321975275429689,0.333333333333333,0.321975275429689,
0.333333333333333,0.321975275429689,0.333333333333333,0.321975275429689,
0.333333333333333,0.321975275429689,0.333333333333333,0.321975275429689,
0.333333333333333,0.321975275429689,0.333333333333333,0.321975275429689,
0.333333333333333,0.321975275429689,0.333333333333333,0.321975275429689,
0.333333333333333,0.321975275429689,0.333333333333333,0.321975275429689,
0.333333333333333,0.321975275429689,0.333333333333333,0.321975275429689,
0.333333333333333,0.321975275429689,0.333333333333333,0.321975275429689,
0.333333333333333,0.321975275429689,0.333333333333333,0.321975275429689,
0.333333333333333,0.321975275429689,0.333333333333333,0.321975275429689,
0.333333333333333,0.321975275429689,0.333333333333333,0.321975275429689,
0.333333333333333,0.321975275429689,0.333333333333333,0.321975275429689,
0.333333333333333,0.321975275429689,0.333333333333333,0.321975275429689,
0.333333333333333,0.321975275429689,0.333333333333333,0.321975275429689,
0.333333333333333,0.321975275429689,0.333333333333333,0.321975275429689,
0.333333333333333,0.321975275429689,0.333333333333333,0.321975275429689,
0.333333333333333,0.321975275429689,0.333333333333333,0.321975275429689,
0.333333333333333,0.321975275429689,0.333333333333333,0.321975275429689,
0.333333333333333,0.321975275429689,0.333333333333333,0.321975275429689,
0.333333333333333,0.321975275429689,0.333333333333333,0.321975275429689,
0.333333333333333,0.321975275429689,0.333333333333333,0.321975275429689,
0.333333333333333,0.321975275429689,0.333333333333333,0.321975275429689,
0.333333333333333,0.321975275429689,0.333333333333333,0.321975275429689,
0.333333333333333,0.321975275429689,0.333333333333333,0.321975275429689,
0.333333333333333,0.321975275429689,0.333333333333333,0.321975275429689,
0.333333333333333,0.321975275429689,0.333333333333333,0.321975275429689,
0.333333333333333,0.321975275429689,0.333333333333333,0.321975275429689,
0.333333333333333,0.321975275429689,0.333333333333333,0.321975275429689,
0.333333333333333,0.321975275429689,0.333333333333333,0.321975275429689,
0.333333333333333,0.321975275429689,0.333333333333333,0.321975275429689,
0.333333333333333,0.321975275429689,0.333333333333333,0.321975275429689,
0.333333333333333,0.321975275429689,0.333333333333333,0.321975275429689,
0.333333333333333,0.321975275429689,0.333333333333333,0.321975275429689,
0.333333333333333,0.321975275429689,0.333333333333333,0.321975275429689,
0.333333333333333,0.321975275429689,0.333333333333333,0.321975275429689,
0.333333333333333,0.321975275429689,0.333333333333333,0.321975275429689,
0.333333333333333,0.321975275429689,0.333333333333333,0.321975275429689,
0.333333333333333,0.321975275429689,0.333333333333333,0.321975275429689,
0.333333333333333,0.321975275429689,0.333333333333333,0.321975275429689,
0.333333333333333,0.321975275429689,0.333333333333333,0.321975275429689,
0.333333333333333,0.321975275429689,0.333333333333333,0.321975275429689,
0.333333333333333,0.321975275429689,0.333333333333333,0.321975275429689,
0.333333333333333,0.321975275429689,0.333333333333333,0.321975275429689,
0.333333333333333,0.321975275429689,0.333333333333333,0.321975275429689,
0.333333333333333,0.321975275429689,0.333333333333333,0.321975275429689,
0.333333333333333,0.321975275429689,0.333333333333333,0.321975275429689,
0.333333333333333,0.321975275429689,0.333333333333333,0.321975275429689,
0.333333333333333,0.321975275429689,0.333333333333333,0.321975275429689,
0.333333333333333,0.321975275429689,0.333333333333333,0.321975275429689,
0.333333333333333,0.321975275429689,0.333333333333333,0.321975275429689,
0.333333333333333,0.321975275429689,0.333333333333333,0.321975275429689,
0.333333333333333,0.321975275429689,0.333333333333333,0.321975275429689,
0.333333333333333,0.321975275429689,0.333333333333333,0.321975275429689,
0.333333333333333,0.321975275429689,0.333333333333333,0.321975275429689,
0.333333333333333,0.321975275429689,0.333333333333333,0.321975275429689,
0.333333333333333,0.321975275429689,0.333333333333333,0.321975275429689,
0.333333333333333,0.321975275429689,0.333333333333333,0.321975275429689,
0.333333333333333,0.321975275429689,0.333333333333333,0.321975275429689,
0.333333333333333,0.321975275429689,0.333333333333333,0.321975275429689,
0.333333333333333,0.321975275429689,0.333333333333333,0.321975275429689,
0.333333333333333,0.321975275429689,0.333333333333333,0.321975275429689,
0.333333333333333,0.321975275429689,0.333333333333333,0.321975275429689,
0.333333333333333,0.321975275429689,0.333333333333333,0.321975275429689,
0.333333333333333,0.321975275429689,0.333333333333333,0.321975275429689,
0.333333333333333,0.321975275429689,0.333333333333333,0.321975275429689,
0.333333333333333,0.321975275429689,0.333333333333333,0.321975275429689,
0.333333333333333,0.321975275429689,0.333333333333333,0.321975275429689,
0.333333333333333,0.321975275429689,0.333333333333333,0.321975275429689,
0.333333333333333,0.321975275429689,0.333333333333333,0.321975275429689,
0.333333333333333,0.321975275429689,0.333333333333333,0.321975275429689,
0.333333333333333,0.321975275429689,0.333333333333333,0.321975275429689,
0.333333333333333,0.321975275429689,0.333333333333333,0.321975275429689,
0.333333333333333,0.321975275429689,0.333333333333333,0.321975275429689,
0.333333333333333,0.321975275429689,0.333333333333333,0.321975275429689,
0.333333333333333,0.321975275429689,0.333333333333333,0.321975275429689,
0.333333333333333,0.321975275429689,0.333333333333333,0.321975275429689,
0.333333333333333,0.321975275429689,0.333333333333333,0.321975275429689,
0.333333333333333,0.321975275429689,0.333333333333333,0.321975275429689,
0.333333333333333,0.321975275429689,0.333333333333333,0.321975275429689,
0.333333333333333,0.321975275429689,0.333333333333333,0.321975275429689,
0.333333333333333,0.321975275429689,0.333333333333333,0.321975275429689,
0.333333333333333,0.321975275429689,0.333333333333333,0.321975275429689,
0.333333333333333,0.321975275429689,0.333333333333333,0.321975275429689,
0.333333333333333,0.321975275429689,0.333333333333333,0.321975275429689,
0.333333333333333,0.321975275429689,0.333333333333333,0.321975275429689,
0.333333333333333,0.321975275429689,0.333333333333333,0.321975275429689,
0.333333333333333,0.321975275429689,0.333333333333333,0.321975275429689,
0.333333333333333,0.321975275429689,0.333333333333333,0.321975275429689,
0.333333333333333,0.321975275429689,0.333333333333333,0.321975275429689,
0.333333333333333,0.321975275429689,0.333333333333333),(0.333333333333333,
0.321975275429689,0.333333333333333,0.321975275429689,0.333333333333333,
0.321975275429689,0.333333333333333,0.321975275429689,0.333333333333333,
0.321975275429689,0.333333333333333,0.321975275429689,0.333333333333333,
0.321975275429689,0.333333333333333,0.321975275429689,0.333333333333333,
0.321975275429689,0.333333333333333,0.321975275429689,0.333333333333333,
0.321975275429689,0.333333333333333,0.321975275429689,0.333333333333333,
0.321975275429689,0.333333333333333,0.321975275429689,0.333333333333333,
0.321975275429689,0.333333333333333,0.321975275429689,0.333333333333333,
0.321975275429689,0.333333333333333,0.321975275429689,0.333333333333333,
0.321975275429689,0.333333333333333,0.321975275429689,0.333333333333333,
0.321975275429689,0.333333333333333,0.321975275429689,0.333333333333333,
0.321975275429689,0.333333333333333,0.321975275429689,0.333333333333333,
0.321975275429689,0.333333333333333,0.321975275429689,0.333333333333333,
0.321975275429689,0.333333333333333,0.321975275429689,0.333333333333333,
0.321975275429689,0.333333333333333,0.321975275429689,0.333333333333333,
0.321975275429689,0.333333333333333,0.321975275429689,0.333333333333333,
0.321975275429689,0.333333333333333,0.321975275429689,0.333333333333333,
0.321975275429689,0.333333333333333,0.321975275429689,0.333333333333333,
0.321975275429689,0.333333333333333,0.321975275429689,0.333333333333333,
0.321975275429689,0.333333333333333,0.321975275429689,0.333333333333333,
0.321975275429689,0.333333333333333,0.321975275429689,0.333333333333333,
0.321975275429689,0.333333333333333,0.321975275429689,0.333333333333333,
0.321975275429689,0.333333333333333,0.321975275429689,0.333333333333333,
0.321975275429689,0.333333333333333,0.321975275429689,0.333333333333333,
0.321975275429689,0.333333333333333,0.321975275429689,0.333333333333333,
0.321975275429689,0.333333333333333,0.321975275429689,0.333333333333333,
0.321975275429689,0.333333333333333,0.321975275429689,0.333333333333333,
0.321975275429689,0.333333333333333,0.321975275429689,0.333333333333333,
0.321975275429689,0.333333333333333,0.321975275429689,0.333333333333333,
0.321975275429689,0.333333333333333,0.321975275429689,0.333333333333333,
0.321975275429689,0.333333333333333,0.321975275429689,0.333333333333333,
0.321975275429689,0.333333333333333,0.321975275429689,0.333333333333333,
0.321975275429689,0.333333333333333,0.321975275429689,0.333333333333333,
0.321975275429689,0.333333333333333,0.321975275429689,0.333333333333333,
0.321975275429689,0.333333333333333,0.321975275429689,0.333333333333333,
0.321975275429689,0.333333333333333,0.321975275429689,0.333333333333333,
0.321975275429689,0.333333333333333,0.321975275429689,0.333333333333333,
0.321975275429689,0.333333333333333,0.321975275429689,0.333333333333333,
0.321975275429689,0.333333333333333,0.321975275429689,0.333333333333333,
0.321975275429689,0.333333333333333,0.321975275429689,0.333333333333333,
0.321975275429689,0.333333333333333,0.321975275429689,0.333333333333333,
0.321975275429689,0.333333333333333,0.321975275429689,0.333333333333333,
0.321975275429689,0.333333333333333,0.321975275429689,0.333333333333333,
0.321975275429689,0.333333333333333,0.321975275429689,0.333333333333333,
0.321975275429689,0.333333333333333,0.321975275429689,0.333333333333333,
0.321975275429689,0.333333333333333,0.321975275429689,0.333333333333333,
0.321975275429689,0.333333333333333,0.321975275429689,0.333333333333333,
0.321975275429689,0.333333333333333,0.321975275429689,0.333333333333333,
0.321975275429689,0.333333333333333,0.321975275429689,0.333333333333333,
0.321975275429689,0.333333333333333,0.321975275429689,0.333333333333333,
0.321975275429689,0.333333333333333,0.321975275429689,0.333333333333333,
0.321975275429689,0.333333333333333,0.321975275429689,0.333333333333333,
0.321975275429689,0.333333333333333,0.321975275429689,0.333333333333333,
0.321975275429689,0.333333333333333,0.321975275429689,0.333333333333333,
0.321975275429689,0.333333333333333,0.321975275429689,0.333333333333333,
0.321975275429689,0.333333333333333,0.321975275429689,0.333333333333333,
0.321975275429689,0.333333333333333,0.321975275429689,0.333333333333333,
0.321975275429689,0.333333333333333,0.321975275429689,0.333333333333333,
0.321975275429689,0.333333333333333,0.321975275429689,0.333333333333333,
0.321975275429689,0.333333333333333,0.321975275429689,0.333333333333333,
0.321975275429689,0.333333333333333,0.321975275429689,0.333333333333333,
0.321975275429689,0.333333333333333,0.321975275429689,0.333333333333333,
0.321975275429689,0.333333333333333,0.321975275429689,0.333333333333333,
0.321975275429689,0.333333333333333,0.321975275429689,0.333333333333333,
0.321975275429689,0.333333333333333,0.321975275429689,0.333333333333333,
0.321975275429689,0.333333333333333,0.321975275429689,0.333333333333333,
0.321975275429689,0.333333333333333,0.321975275429689,0.333333333333333,
0.321975275429689,0.333333333333333,0.321975275429689,0.333333333333333,
0.321975275429689,0.333333333333333,0.321975275429689,0.333333333333333,
0.321975275429689,0.333333333333333,0.321975275429689,0.333333333333333,
0.321975275429689,0.333333333333333,0.321975275429689,0.333333333333333,
0.321975275429689,0.333333333333333,0.321975275429689,0.333333333333333,
0.321975275429689,0.333333333333333,0.321975275429689,0.333333333333333,
0.321975275429689,0.333333333333333,0.321975275429689,0.333333333333333,
0.321975275429689,0.333333333333333,0.321975275429689,0.333333333333333,
0.321975275429689,0.333333333333333,0.321975275429689,0.333333333333333,
0.321975275429689,0.333333333333333,0.321975275429689,0.333333333333333,
0.321975275429689,0.333333333333333,0.321975275429689,0.333333333333333,
0.321975275429689,0.333333333333333,0.321975275429689,0.333333333333333,
0.321975275429689,0.333333333333333,0.321975275429689,0.333333333333333,
0.321975275429689,0.333333333333333,0.321975275429689,0.333333333333333,
0.321975275429689,0.333333333333333,0.321975275429689,0.333333333333333,
0.321975275429689,0.333333333333333,0.321975275429689,0.333333333333333,
0.321975275429689,0.333333333333333,0.321975275429689,0.333333333333333,
0.321975275429689,0.333333333333333,0.321975275429689,0.333333333333333,
0.321975275429689,0.333333333333333,0.321975275429689,0.333333333333333,
0.321975275429689,0.333333333333333,0.321975275429689,0.333333333333333,
0.321975275429689,0.333333333333333,0.321975275429689,0.333333333333333,
0.321975275429689,0.333333333333333,0.321975275429689,0.333333333333333,
0.321975275429689,0.333333333333333,0.321975275429689,0.333333333333333,
0.321975275429689,0.333333333333333,0.321975275429689,0.333333333333333,
0.321975275429689,0.333333333333333,0.321975275429689,0.333333333333333,
0.321975275429689,0.333333333333333,0.321975275429689,0.333333333333333,
0.321975275429689,0.333333333333333,0.321975275429689,0.333333333333333,
0.321975275429689,0.333333333333333,0.321975275429689,0.333333333333333,
0.321975275429689,0.333333333333333,0.321975275429689,0.333333333333333,
0.321975275429689,0.333333333333333,0.321975275429689,0.333333333333333,
0.321975275429689,0.333333333333333,0.321975275429689,0.333333333333333,
0.321975275429689,0.333333333333333,0.321975275429689,0.333333333333333,
0.321975275429689,0.333333333333333,0.321975275429689,0.333333333333333,
0.321975275429689,0.333333333333333,0.321975275429689,0.333333333333333,
0.321975275429689,0.333333333333333,0.321975275429689,0.333333333333333,
0.321975275429689,0.333333333333333,0.321975275429689,0.333333333333333,
0.321975275429689,0.333333333333333,0.321975275429689,0.333333333333333,
0.321975275429689,0.333333333333333,0.321975275429689,0.333333333333333,
0.321975275429689,0.333333333333333,0.321975275429689,0.333333333333333,
0.321975275429689,0.333333333333333,0.321975275429689,0.333333333333333,
0.321975275429689,0.333333333333333,0.321975275429689,0.333333333333333,
0.321975275429689,0.333333333333333,0.321975275429689,0.333333333333333,
0.321975275429689,0.333333333333333,0.321975275429689,0.333333333333333,
0.321975275429689,0.333333333333333,0.321975275429689,0.333333333333333,
0.321975275429689,0.333333333333333,0.321975275429689,0.333333333333333,
0.321975275429689,0.333333333333333,0.321975275429689,0.333333333333333,
0.321975275429689,0.333333333333333,0.321975275429689,0.333333333333333),
(1.,0.965925826289068,1.,0.965925826289068,1.,0.965925826289068,1.,0.965925826289068,
1.,0.965925826289068,1.,0.965925826289068,1.,0.965925826289068,1.,0.965925826289068,
1.,0.965925826289068,1.,0.965925826289068,1.,0.965925826289068,1.,0.965925826289068,
1.,0.965925826289068,1.,0.965925826289068,1.,0.965925826289068,1.,0.965925826289068,
1.,0.965925826289068,1.,0.965925826289068,1.,0.965925826289068,1.,0.965925826289068,
1.,0.965925826289068,1.,0.965925826289068,1.,0.965925826289068,1.,0.965925826289068,
1.,0.965925826289068,1.,0.965925826289068,1.,0.965925826289068,1.,0.965925826289068,
1.,0.965925826289068,1.,0.965925826289068,1.,0.965925826289068,1.,0.965925826289068,
1.,0.965925826289068,1.,0.965925826289068,1.,0.965925826289068,1.,0.965925826289068,
1.,0.965925826289068,1.,0.965925826289068,1.,0.965925826289068,1.,0.965925826289068,
1.,0.965925826289068,1.,0.965925826289068,1.,0.965925826289068,1.,0.965925826289068,
1.,0.965925826289068,1.,0.965925826289068,1.,0.965925826289068,1.,0.965925826289068,
1.,0.965925826289068,1.,0.965925826289068,1.,0.965925826289068,1.,0.965925826289068,
1.,0.965925826289068,1.,0.965925826289068,1.,0.965925826289068,1.,0.965925826289068,
1.,0.965925826289068,1.,0.965925826289068,1.,0.965925826289068,1.,0.965925826289068,
1.,0.965925826289068,1.,0.965925826289068,1.,0.965925826289068,1.,0.965925826289068,
1.,0.965925826289068,1.,0.965925826289068,1.,0.965925826289068,1.,0.965925826289068,
1.,0.965925826289068,1.,0.965925826289068,1.,0.965925826289068,1.,0.965925826289068,
1.,0.965925826289068,1.,0.965925826289068,1.,0.965925826289068,1.,0.965925826289068,
1.,0.965925826289068,1.,0.965925826289068,1.,0.965925826289068,1.,0.965925826289068,
1.,0.965925826289068,1.,0.965925826289068,1.,0.965925826289068,1.,0.965925826289068,
1.,0.965925826289068,1.,0.965925826289068,1.,0.965925826289068,1.,0.965925826289068,
1.,0.965925826289068,1.,0.965925826289068,1.,0.965925826289068,1.,0.965925826289068,
1.,0.965925826289068,1.,0.965925826289068,1.,0.965925826289068,1.,0.965925826289068,
1.,0.965925826289068,1.,0.965925826289068,1.,0.965925826289068,1.,0.965925826289068,
1.,0.965925826289068,1.,0.965925826289068,1.,0.965925826289068,1.,0.965925826289068,
1.,0.965925826289068,1.,0.965925826289068,1.,0.965925826289068,1.,0.965925826289068,
1.,0.965925826289068,1.,0.965925826289068,1.,0.965925826289068,1.,0.965925826289068,
1.,0.965925826289068,1.,0.965925826289068,1.,0.965925826289068,1.,0.965925826289068,
1.,0.965925826289068,1.,0.965925826289068,1.,0.965925826289068,1.,0.965925826289068,
1.,0.965925826289068,1.,0.965925826289068,1.,0.965925826289068,1.,0.965925826289068,
1.,0.965925826289068,1.,0.965925826289068,1.,0.965925826289068,1.,0.965925826289068,
1.,0.965925826289068,1.,0.965925826289068,1.,0.965925826289068,1.,0.965925826289068,
1.,0.965925826289068,1.,0.965925826289068,1.,0.965925826289068,1.,0.965925826289068,
1.,0.965925826289068,1.,0.965925826289068,1.,0.965925826289068,1.,0.965925826289068,
1.,0.965925826289068,1.,0.965925826289068,1.,0.965925826289068,1.,0.965925826289068,
1.,0.965925826289068,1.,0.965925826289068,1.,0.965925826289068,1.,0.965925826289068,
1.,0.965925826289068,1.,0.965925826289068,1.,0.965925826289068,1.,0.965925826289068,
1.,0.965925826289068,1.,0.965925826289068,1.,0.965925826289068,1.,0.965925826289068,
1.,0.965925826289068,1.,0.965925826289068,1.,0.965925826289068,1.,0.965925826289068,
1.,0.965925826289068,1.,0.965925826289068,1.,0.965925826289068,1.,0.965925826289068,
1.,0.965925826289068,1.,0.965925826289068,1.,0.965925826289068,1.,0.965925826289068,
1.,0.965925826289068,1.,0.965925826289068,1.,0.965925826289068,1.,0.965925826289068,
1.,0.965925826289068,1.,0.965925826289068,1.,0.965925826289068,1.,0.965925826289068,
1.,0.965925826289068,1.,0.965925826289068,1.,0.965925826289068,1.,0.965925826289068,
1.,0.965925826289068,1.,0.965925826289068,1.,0.965925826289068,1.,0.965925826289068,
1.,0.965925826289068,1.,0.965925826289068,1.,0.965925826289068,1.,0.965925826289068,
1.,0.965925826289068,1.,0.965925826289068,1.,0.965925826289068,1.,0.965925826289068,
1.,0.965925826289068,1.,0.965925826289068,1.,0.965925826289068,1.,0.965925826289068,
1.,0.965925826289068,1.,0.965925826289068,1.,0.965925826289068,1.,0.965925826289068,
1.,0.965925826289068,1.,0.965925826289068,1.,0.965925826289068,1.,0.965925826289068,
1.,0.965925826289068,1.,0.965925826289068,1.,0.965925826289068,1.,0.965925826289068,
1.,0.965925826289068,1.,0.965925826289068,1.,0.965925826289068,1.,0.965925826289068,
1.,0.965925826289068,1.,0.965925826289068,1.,0.965925826289068,1.,0.965925826289068,
1.,0.965925826289068,1.,0.965925826289068,1.,0.965925826289068,1.,0.965925826289068,
1.,0.965925826289068,1.,0.965925826289068,1.,0.965925826289068,1.,0.965925826289068,
1.,0.965925826289068,1.,0.965925826289068,1.,0.965925826289068,1.,0.965925826289068,
1.),(0.333333333333333,0.321975275429689,0.333333333333333,0.321975275429689,
0.333333333333333,0.321975275429689,0.333333333333333,0.321975275429689,
0.333333333333333,0.321975275429689,0.333333333333333,0.321975275429689,
0.333333333333333,0.321975275429689,0.333333333333333,0.321975275429689,
0.333333333333333,0.321975275429689,0.333333333333333,0.321975275429689,
0.333333333333333,0.321975275429689,0.333333333333333,0.321975275429689,
0.333333333333333,0.321975275429689,0.333333333333333,0.321975275429689,
0.333333333333333,0.321975275429689,0.333333333333333,0.321975275429689,
0.333333333333333,0.321975275429689,0.333333333333333,0.321975275429689,
0.333333333333333,0.321975275429689,0.333333333333333,0.321975275429689,
0.333333333333333,0.321975275429689,0.333333333333333,0.321975275429689,
0.333333333333333,0.321975275429689,0.333333333333333,0.321975275429689,
0.333333333333333,0.321975275429689,0.333333333333333,0.321975275429689,
0.333333333333333,0.321975275429689,0.333333333333333,0.321975275429689,
0.333333333333333,0.321975275429689,0.333333333333333,0.321975275429689,
0.333333333333333,0.321975275429689,0.333333333333333,0.321975275429689,
0.333333333333333,0.321975275429689,0.333333333333333,0.321975275429689,
0.333333333333333,0.321975275429689,0.333333333333333,0.321975275429689,
0.333333333333333,0.321975275429689,0.333333333333333,0.321975275429689,
0.333333333333333,0.321975275429689,0.333333333333333,0.321975275429689,
0.333333333333333,0.321975275429689,0.333333333333333,0.321975275429689,
0.333333333333333,0.321975275429689,0.333333333333333,0.321975275429689,
0.333333333333333,0.321975275429689,0.333333333333333,0.321975275429689,
0.333333333333333,0.321975275429689,0.333333333333333,0.321975275429689,
0.333333333333333,0.321975275429689,0.333333333333333,0.321975275429689,
0.333333333333333,0.321975275429689,0.333333333333333,0.321975275429689,
0.333333333333333,0.321975275429689,0.333333333333333,0.321975275429689,
0.333333333333333,0.321975275429689,0.333333333333333,0.321975275429689,
0.333333333333333,0.321975275429689,0.333333333333333,0.321975275429689,
0.333333333333333,0.321975275429689,0.333333333333333,0.321975275429689,
0.333333333333333,0.321975275429689,0.333333333333333,0.321975275429689,
0.333333333333333,0.321975275429689,0.333333333333333,0.321975275429689,
0.333333333333333,0.321975275429689,0.333333333333333,0.321975275429689,
0.333333333333333,0.321975275429689,0.333333333333333,0.321975275429689,
0.333333333333333,0.321975275429689,0.333333333333333,0.321975275429689,
0.333333333333333,0.321975275429689,0.333333333333333,0.321975275429689,
0.333333333333333,0.321975275429689,0.333333333333333,0.321975275429689,
0.333333333333333,0.321975275429689,0.333333333333333,0.321975275429689,
0.333333333333333,0.321975275429689,0.333333333333333,0.321975275429689,
0.333333333333333,0.321975275429689,0.333333333333333,0.321975275429689,
0.333333333333333,0.321975275429689,0.333333333333333,0.321975275429689,
0.333333333333333,0.321975275429689,0.333333333333333,0.321975275429689,
0.333333333333333,0.321975275429689,0.333333333333333,0.321975275429689,
0.333333333333333,0.321975275429689,0.333333333333333,0.321975275429689,
0.333333333333333,0.321975275429689,0.333333333333333,0.321975275429689,
0.333333333333333,0.321975275429689,0.333333333333333,0.321975275429689,
0.333333333333333,0.321975275429689,0.333333333333333,0.321975275429689,
0.333333333333333,0.321975275429689,0.333333333333333,0.321975275429689,
0.333333333333333,0.321975275429689,0.333333333333333,0.321975275429689,
0.333333333333333,0.321975275429689,0.333333333333333,0.321975275429689,
0.333333333333333,0.321975275429689,0.333333333333333,0.321975275429689,
0.333333333333333,0.321975275429689,0.333333333333333,0.321975275429689,
0.333333333333333,0.321975275429689,0.333333333333333,0.321975275429689,
0.333333333333333,0.321975275429689,0.333333333333333,0.321975275429689,
0.333333333333333,0.321975275429689,0.333333333333333,0.321975275429689,
0.333333333333333,0.321975275429689,0.333333333333333,0.321975275429689,
0.333333333333333,0.321975275429689,0.333333333333333,0.321975275429689,
0.333333333333333,0.321975275429689,0.333333333333333,0.321975275429689,
0.333333333333333,0.321975275429689,0.333333333333333,0.321975275429689,
0.333333333333333,0.321975275429689,0.333333333333333,0.321975275429689,
0.333333333333333,0.321975275429689,0.333333333333333,0.321975275429689,
0.333333333333333,0.321975275429689,0.333333333333333,0.321975275429689,
0.333333333333333,0.321975275429689,0.333333333333333,0.321975275429689,
0.333333333333333,0.321975275429689,0.333333333333333,0.321975275429689,
0.333333333333333,0.321975275429689,0.333333333333333,0.321975275429689,
0.333333333333333,0.321975275429689,0.333333333333333,0.321975275429689,
0.333333333333333,0.321975275429689,0.333333333333333,0.321975275429689,
0.333333333333333,0.321975275429689,0.333333333333333,0.321975275429689,
0.333333333333333,0.321975275429689,0.333333333333333,0.321975275429689,
0.333333333333333,0.321975275429689,0.333333333333333,0.321975275429689,
0.333333333333333,0.321975275429689,0.333333333333333,0.321975275429689,
0.333333333333333,0.321975275429689,0.333333333333333,0.321975275429689,
0.333333333333333,0.321975275429689,0.333333333333333,0.321975275429689,
0.333333333333333,0.321975275429689,0.333333333333333,0.321975275429689,
0.333333333333333,0.321975275429689,0.333333333333333,0.321975275429689,
0.333333333333333,0.321975275429689,0.333333333333333,0.321975275429689,
0.333333333333333,0.321975275429689,0.333333333333333,0.321975275429689,
0.333333333333333,0.321975275429689,0.333333333333333,0.321975275429689,
0.333333333333333,0.321975275429689,0.333333333333333,0.321975275429689,
0.333333333333333,0.321975275429689,0.333333333333333,0.321975275429689,
0.333333333333333,0.321975275429689,0.333333333333333,0.321975275429689,
0.333333333333333,0.321975275429689,0.333333333333333,0.321975275429689,
0.333333333333333,0.321975275429689,0.333333333333333,0.321975275429689,
0.333333333333333,0.321975275429689,0.333333333333333,0.321975275429689,
0.333333333333333,0.321975275429689,0.333333333333333,0.321975275429689,
0.333333333333333,0.321975275429689,0.333333333333333,0.321975275429689,
0.333333333333333,0.321975275429689,0.333333333333333,0.321975275429689,
0.333333333333333,0.321975275429689,0.333333333333333,0.321975275429689,
0.333333333333333,0.321975275429689,0.333333333333333,0.321975275429689,
0.333333333333333,0.321975275429689,0.333333333333333,0.321975275429689,
0.333333333333333,0.321975275429689,0.333333333333333,0.321975275429689,
0.333333333333333,0.321975275429689,0.333333333333333,0.321975275429689,
0.333333333333333,0.321975275429689,0.333333333333333,0.321975275429689,
0.333333333333333,0.321975275429689,0.333333333333333,0.321975275429689,
0.333333333333333,0.321975275429689,0.333333333333333,0.321975275429689,
0.333333333333333,0.321975275429689,0.333333333333333,0.321975275429689,
0.333333333333333,0.321975275429689,0.333333333333333,0.321975275429689,
0.333333333333333,0.321975275429689,0.333333333333333,0.321975275429689,
0.333333333333333,0.321975275429689,0.333333333333333,0.321975275429689,
0.333333333333333,0.321975275429689,0.333333333333333,0.321975275429689,
0.333333333333333,0.321975275429689,0.333333333333333,0.321975275429689,
0.333333333333333,0.321975275429689,0.333333333333333,0.321975275429689,
0.333333333333333,0.321975275429689,0.333333333333333,0.321975275429689,
0.333333333333333,0.321975275429689,0.333333333333333,0.321975275429689,
0.333333333333333,0.321975275429689,0.333333333333333,0.321975275429689,
0.333333333333333,0.321975275429689,0.333333333333333,0.321975275429689,
0.333333333333333,0.321975275429689,0.333333333333333,0.321975275429689,
0.333333333333333,0.321975275429689,0.333333333333333,0.321975275429689,
0.333333333333333,0.321975275429689,0.333333333333333,0.321975275429689,
0.333333333333333,0.321975275429689,0.333333333333333,0.321975275429689,
0.333333333333333,0.321975275429689,0.333333333333333,0.321975275429689,
0.333333333333333,0.321975275429689,0.333333333333333,0.321975275429689,
0.333333333333333,0.321975275429689,0.333333333333333,0.321975275429689,
0.333333333333333,0.321975275429689,0.333333333333333,0.321975275429689,
0.333333333333333),(0.333333333333333,0.321975275429689,0.333333333333333,
0.321975275429689,0.333333333333333,0.321975275429689,0.333333333333333,
0.321975275429689,0.333333333333333,0.321975275429689,0.333333333333333,
0.321975275429689,0.333333333333333,0.321975275429689,0.333333333333333,
0.321975275429689,0.333333333333333,0.321975275429689,0.333333333333333,
0.321975275429689,0.333333333333333,0.321975275429689,0.333333333333333,
0.321975275429689,0.333333333333333,0.321975275429689,0.333333333333333,
0.321975275429689,0.333333333333333,0.321975275429689,0.333333333333333,
0.321975275429689,0.333333333333333,0.321975275429689,0.333333333333333,
0.321975275429689,0.333333333333333,0.321975275429689,0.333333333333333,
0.321975275429689,0.333333333333333,0.321975275429689,0.333333333333333,
0.321975275429689,0.333333333333333,0.321975275429689,0.333333333333333,
0.321975275429689,0.333333333333333,0.321975275429689,0.333333333333333,
0.321975275429689,0.333333333333333,0.321975275429689,0.333333333333333,
0.321975275429689,0.333333333333333,0.321975275429689,0.333333333333333,
0.321975275429689,0.333333333333333,0.321975275429689,0.333333333333333,
0.321975275429689,0.333333333333333,0.321975275429689,0.333333333333333,
0.321975275429689,0.333333333333333,0.321975275429689,0.333333333333333,
0.321975275429689,0.333333333333333,0.321975275429689,0.333333333333333,
0.321975275429689,0.333333333333333,0.321975275429689,0.333333333333333,
0.321975275429689,0.333333333333333,0.321975275429689,0.333333333333333,
0.321975275429689,0.333333333333333,0.321975275429689,0.333333333333333,
0.321975275429689,0.333333333333333,0.321975275429689,0.333333333333333,
0.321975275429689,0.333333333333333,0.321975275429689,0.333333333333333,
0.321975275429689,0.333333333333333,0.321975275429689,0.333333333333333,
0.321975275429689,0.333333333333333,0.321975275429689,0.333333333333333,
0.321975275429689,0.333333333333333,0.321975275429689,0.333333333333333,
0.321975275429689,0.333333333333333,0.321975275429689,0.333333333333333,
0.321975275429689,0.333333333333333,0.321975275429689,0.333333333333333,
0.321975275429689,0.333333333333333,0.321975275429689,0.333333333333333,
0.321975275429689,0.333333333333333,0.321975275429689,0.333333333333333,
0.321975275429689,0.333333333333333,0.321975275429689,0.333333333333333,
0.321975275429689,0.333333333333333,0.321975275429689,0.333333333333333,
0.321975275429689,0.333333333333333,0.321975275429689,0.333333333333333,
0.321975275429689,0.333333333333333,0.321975275429689,0.333333333333333,
0.321975275429689,0.333333333333333,0.321975275429689,0.333333333333333,
0.321975275429689,0.333333333333333,0.321975275429689,0.333333333333333,
0.321975275429689,0.333333333333333,0.321975275429689,0.333333333333333,
0.321975275429689,0.333333333333333,0.321975275429689,0.333333333333333,
0.321975275429689,0.333333333333333,0.321975275429689,0.333333333333333,
0.321975275429689,0.333333333333333,0.321975275429689,0.333333333333333,
0.321975275429689,0.333333333333333,0.321975275429689,0.333333333333333,
0.321975275429689,0.333333333333333,0.321975275429689,0.333333333333333,
0.321975275429689,0.333333333333333,0.321975275429689,0.333333333333333,
0.321975275429689,0.333333333333333,0.321975275429689,0.333333333333333,
0.321975275429689,0.333333333333333,0.321975275429689,0.333333333333333,
0.321975275429689,0.333333333333333,0.321975275429689,0.333333333333333,
0.321975275429689,0.333333333333333,0.321975275429689,0.333333333333333,
0.321975275429689,0.333333333333333,0.321975275429689,0.333333333333333,
0.321975275429689,0.333333333333333,0.321975275429689,0.333333333333333,
0.321975275429689,0.333333333333333,0.321975275429689,0.333333333333333,
0.321975275429689,0.333333333333333,0.321975275429689,0.333333333333333,
0.321975275429689,0.333333333333333,0.321975275429689,0.333333333333333,
0.321975275429689,0.333333333333333,0.321975275429689,0.333333333333333,
0.321975275429689,0.333333333333333,0.321975275429689,0.333333333333333,
0.321975275429689,0.333333333333333,0.321975275429689,0.333333333333333,
0.321975275429689,0.333333333333333,0.321975275429689,0.333333333333333,
0.321975275429689,0.333333333333333,0.321975275429689,0.333333333333333,
0.321975275429689,0.333333333333333,0.321975275429689,0.333333333333333,
0.321975275429689,0.333333333333333,0.321975275429689,0.333333333333333,
0.321975275429689,0.333333333333333,0.321975275429689,0.333333333333333,
0.321975275429689,0.333333333333333,0.321975275429689,0.333333333333333,
0.321975275429689,0.333333333333333,0.321975275429689,0.333333333333333,
0.321975275429689,0.333333333333333,0.321975275429689,0.333333333333333,
0.321975275429689,0.333333333333333,0.321975275429689,0.333333333333333,
0.321975275429689,0.333333333333333,0.321975275429689,0.333333333333333,
0.321975275429689,0.333333333333333,0.321975275429689,0.333333333333333,
0.321975275429689,0.333333333333333,0.321975275429689,0.333333333333333,
0.321975275429689,0.333333333333333,0.321975275429689,0.333333333333333,
0.321975275429689,0.333333333333333,0.321975275429689,0.333333333333333,
0.321975275429689,0.333333333333333,0.321975275429689,0.333333333333333,
0.321975275429689,0.333333333333333,0.321975275429689,0.333333333333333,
0.321975275429689,0.333333333333333,0.321975275429689,0.333333333333333,
0.321975275429689,0.333333333333333,0.321975275429689,0.333333333333333,
0.321975275429689,0.333333333333333,0.321975275429689,0.333333333333333,
0.321975275429689,0.333333333333333,0.321975275429689,0.333333333333333,
0.321975275429689,0.333333333333333,0.321975275429689,0.333333333333333,
0.321975275429689,0.333333333333333,0.321975275429689,0.333333333333333,
0.321975275429689,0.333333333333333,0.321975275429689,0.333333333333333,
0.321975275429689,0.333333333333333,0.321975275429689,0.333333333333333,
0.321975275429689,0.333333333333333,0.321975275429689,0.333333333333333,
0.321975275429689,0.333333333333333,0.321975275429689,0.333333333333333,
0.321975275429689,0.333333333333333,0.321975275429689,0.333333333333333,
0.321975275429689,0.333333333333333,0.321975275429689,0.333333333333333,
0.321975275429689,0.333333333333333,0.321975275429689,0.333333333333333,
0.321975275429689,0.333333333333333,0.321975275429689,0.333333333333333,
0.321975275429689,0.333333333333333,0.321975275429689,0.333333333333333,
0.321975275429689,0.333333333333333,0.321975275429689,0.333333333333333,
0.321975275429689,0.333333333333333,0.321975275429689,0.333333333333333,
0.321975275429689,0.333333333333333,0.321975275429689,0.333333333333333,
0.321975275429689,0.333333333333333,0.321975275429689,0.333333333333333,
0.321975275429689,0.333333333333333,0.321975275429689,0.333333333333333,
0.321975275429689,0.333333333333333,0.321975275429689,0.333333333333333,
0.321975275429689,0.333333333333333,0.321975275429689,0.333333333333333,
0.321975275429689,0.333333333333333,0.321975275429689,0.333333333333333,
0.321975275429689,0.333333333333333,0.321975275429689,0.333333333333333,
0.321975275429689,0.333333333333333,0.321975275429689,0.333333333333333,
0.321975275429689,0.333333333333333,0.321975275429689,0.333333333333333,
0.321975275429689,0.333333333333333,0.321975275429689,0.333333333333333,
0.321975275429689,0.333333333333333,0.321975275429689,0.333333333333333,
0.321975275429689,0.333333333333333,0.321975275429689,0.333333333333333,
0.321975275429689,0.333333333333333,0.321975275429689,0.333333333333333,
0.321975275429689,0.333333333333333,0.321975275429689,0.333333333333333,
0.321975275429689,0.333333333333333,0.321975275429689,0.333333333333333,
0.321975275429689,0.333333333333333,0.321975275429689,0.333333333333333,
0.321975275429689,0.333333333333333,0.321975275429689,0.333333333333333,
0.321975275429689,0.333333333333333,0.321975275429689,0.333333333333333,
0.321975275429689,0.333333333333333,0.321975275429689,0.333333333333333,
0.321975275429689,0.333333333333333,0.321975275429689,0.333333333333333,
0.321975275429689,0.333333333333333,0.321975275429689,0.333333333333333,
0.321975275429689,0.333333333333333,0.321975275429689,0.333333333333333,
0.321975275429689,0.333333333333333,0.321975275429689,0.333333333333333,
0.321975275429689,0.333333333333333,0.321975275429689,0.333333333333333,
0.321975275429689,0.333333333333333,0.321975275429689,0.333333333333333,
0.321975275429689,0.333333333333333),(1.,0.965925826289068,1.,0.965925826289068,
1.,0.965925826289068,1.,0.965925826289068,1.,0.965925826289068,1.,0.965925826289068,
1.,0.965925826289068,1.,0.965925826289068,1.,0.965925826289068,1.,0.965925826289068,
1.,0.965925826289068,1.,0.965925826289068,1.,0.965925826289068,1.,0.965925826289068,
1.,0.965925826289068,1.,0.965925826289068,1.,0.965925826289068,1.,0.965925826289068,
1.,0.965925826289068,1.,0.965925826289068,1.,0.965925826289068,1.,0.965925826289068,
1.,0.965925826289068,1.,0.965925826289068,1.,0.965925826289068,1.,0.965925826289068,
1.,0.965925826289068,1.,0.965925826289068,1.,0.965925826289068,1.,0.965925826289068,
1.,0.965925826289068,1.,0.965925826289068,1.,0.965925826289068,1.,0.965925826289068,
1.,0.965925826289068,1.,0.965925826289068,1.,0.965925826289068,1.,0.965925826289068,
1.,0.965925826289068,1.,0.965925826289068,1.,0.965925826289068,1.,0.965925826289068,
1.,0.965925826289068,1.,0.965925826289068,1.,0.965925826289068,1.,0.965925826289068,
1.,0.965925826289068,1.,0.965925826289068,1.,0.965925826289068,1.,0.965925826289068,
1.,0.965925826289068,1.,0.965925826289068,1.,0.965925826289068,1.,0.965925826289068,
1.,0.965925826289068,1.,0.965925826289068,1.,0.965925826289068,1.,0.965925826289068,
1.,0.965925826289068,1.,0.965925826289068,1.,0.965925826289068,1.,0.965925826289068,
1.,0.965925826289068,1.,0.965925826289068,1.,0.965925826289068,1.,0.965925826289068,
1.,0.965925826289068,1.,0.965925826289068,1.,0.965925826289068,1.,0.965925826289068,
1.,0.965925826289068,1.,0.965925826289068,1.,0.965925826289068,1.,0.965925826289068,
1.,0.965925826289068,1.,0.965925826289068,1.,0.965925826289068,1.,0.965925826289068,
1.,0.965925826289068,1.,0.965925826289068,1.,0.965925826289068,1.,0.965925826289068,
1.,0.965925826289068,1.,0.965925826289068,1.,0.965925826289068,1.,0.965925826289068,
1.,0.965925826289068,1.,0.965925826289068,1.,0.965925826289068,1.,0.965925826289068,
1.,0.965925826289068,1.,0.965925826289068,1.,0.965925826289068,1.,0.965925826289068,
1.,0.965925826289068,1.,0.965925826289068,1.,0.965925826289068,1.,0.965925826289068,
1.,0.965925826289068,1.,0.965925826289068,1.,0.965925826289068,1.,0.965925826289068,
1.,0.965925826289068,1.,0.965925826289068,1.,0.965925826289068,1.,0.965925826289068,
1.,0.965925826289068,1.,0.965925826289068,1.,0.965925826289068,1.,0.965925826289068,
1.,0.965925826289068,1.,0.965925826289068,1.,0.965925826289068,1.,0.965925826289068,
1.,0.965925826289068,1.,0.965925826289068,1.,0.965925826289068,1.,0.965925826289068,
1.,0.965925826289068,1.,0.965925826289068,1.,0.965925826289068,1.,0.965925826289068,
1.,0.965925826289068,1.,0.965925826289068,1.,0.965925826289068,1.,0.965925826289068,
1.,0.965925826289068,1.,0.965925826289068,1.,0.965925826289068,1.,0.965925826289068,
1.,0.965925826289068,1.,0.965925826289068,1.,0.965925826289068,1.,0.965925826289068,
1.,0.965925826289068,1.,0.965925826289068,1.,0.965925826289068,1.,0.965925826289068,
1.,0.965925826289068,1.,0.965925826289068,1.,0.965925826289068,1.,0.965925826289068,
1.,0.965925826289068,1.,0.965925826289068,1.,0.965925826289068,1.,0.965925826289068,
1.,0.965925826289068,1.,0.965925826289068,1.,0.965925826289068,1.,0.965925826289068,
1.,0.965925826289068,1.,0.965925826289068,1.,0.965925826289068,1.,0.965925826289068,
1.,0.965925826289068,1.,0.965925826289068,1.,0.965925826289068,1.,0.965925826289068,
1.,0.965925826289068,1.,0.965925826289068,1.,0.965925826289068,1.,0.965925826289068,
1.,0.965925826289068,1.,0.965925826289068,1.,0.965925826289068,1.,0.965925826289068,
1.,0.965925826289068,1.,0.965925826289068,1.,0.965925826289068,1.,0.965925826289068,
1.,0.965925826289068,1.,0.965925826289068,1.,0.965925826289068,1.,0.965925826289068,
1.,0.965925826289068,1.,0.965925826289068,1.,0.965925826289068,1.,0.965925826289068,
1.,0.965925826289068,1.,0.965925826289068,1.,0.965925826289068,1.,0.965925826289068,
1.,0.965925826289068,1.,0.965925826289068,1.,0.965925826289068,1.,0.965925826289068,
1.,0.965925826289068,1.,0.965925826289068,1.,0.965925826289068,1.,0.965925826289068,
1.,0.965925826289068,1.,0.965925826289068,1.,0.965925826289068,1.,0.965925826289068,
1.,0.965925826289068,1.,0.965925826289068,1.,0.965925826289068,1.,0.965925826289068,
1.,0.965925826289068,1.,0.965925826289068,1.,0.965925826289068,1.,0.965925826289068,
1.,0.965925826289068,1.,0.965925826289068,1.,0.965925826289068,1.,0.965925826289068,
1.,0.965925826289068,1.,0.965925826289068,1.,0.965925826289068,1.,0.965925826289068,
1.,0.965925826289068,1.,0.965925826289068,1.,0.965925826289068,1.,0.965925826289068,
1.,0.965925826289068,1.,0.965925826289068,1.,0.965925826289068,1.,0.965925826289068,
1.,0.965925826289068,1.,0.965925826289068,1.,0.965925826289068,1.,0.965925826289068,
1.,0.965925826289068,1.,0.965925826289068,1.,0.965925826289068,1.,0.965925826289068,
1.,0.965925826289068,1.,0.965925826289068,1.)))
REPRESENTATION_ITEM('')
SURFACE()
);
#637=B_SPLINE_CURVE_WITH_KNOTS('',3,(#27616,#27617,#27618,#27619,#27620,
#27621,#27622,#27623,#27624,#27625,#27626,#27627,#27628,#27629,#27630,#27631,
#27632,#27633,#27634,#27635,#27636,#27637,#27638,#27639,#27640,#27641,#27642,
#27643,#27644,#27645,#27646,#27647,#27648,#27649,#27650,#27651,#27652,#27653,
#27654,#27655,#27656,#27657,#27658,#27659,#27660,#27661,#27662,#27663,#27664,
#27665,#27666,#27667,#27668,#27669),.UNSPECIFIED.,.F.,.F.,(4,2,2,2,2,2,
2,2,2,2,2,2,2,2,2,2,2,2,2,2,2,2,2,2,2,2,4),(0.,0.211530220655383,0.289081942912891,
0.502162303944745,0.617685523778197,0.735044758583038,1.02805780346695,
1.42592405474646,1.85809441022839,1.99080242607033,2.05848328284043,2.1001327114057,
2.13819962143761,2.18412793694465,2.26153227088293,2.41592184272421,2.86718043954418,
3.43208938067713,4.01802145807674,4.65968133801718,5.38245910771257,5.56242601552907,
6.27810834200945,6.60236241786042,7.05771390645932,7.27425164190709,7.48648678308462),
 .UNSPECIFIED.);
#638=B_SPLINE_CURVE_WITH_KNOTS('',3,(#27670,#27671,#27672,#27673,#27674,
#27675,#27676,#27677,#27678,#27679,#27680,#27681,#27682,#27683,#27684,#27685,
#27686,#27687,#27688,#27689,#27690,#27691,#27692,#27693,#27694,#27695,#27696,
#27697,#27698,#27699,#27700,#27701,#27702,#27703,#27704,#27705,#27706,#27707,
#27708,#27709,#27710,#27711,#27712,#27713,#27714,#27715,#27716,#27717,#27718,
#27719,#27720,#27721,#27722,#27723,#27724,#27725),.UNSPECIFIED.,.F.,.F.,
(4,2,2,2,2,2,2,2,2,2,2,2,2,2,2,2,2,2,2,2,2,2,2,2,2,2,2,4),(0.,0.0508933598535436,
0.102714861816748,0.211107408796559,0.288664279862181,0.501758787708079,
0.617289677349956,0.734656703859758,1.02768920244262,1.42558186882727,1.85778091692665,
1.99049774351539,2.05818309375797,2.09983528751381,2.1379047248868,2.18383608967027,
2.26124556263954,2.41564538471522,2.86693394150261,3.43188038808134,4.01785136669594,
4.65955384773215,5.38237960410595,5.56235846028945,6.27808830236667,6.60236390610103,
7.05774562640548,7.48689591445956),.UNSPECIFIED.);
#914=PLANE('',#10808);
#915=PLANE('',#10810);
#916=PLANE('',#10812);
#917=PLANE('',#10813);
#1341=FACE_OUTER_BOUND('',#1940,.T.);
#1342=FACE_OUTER_BOUND('',#1941,.T.);
#1343=FACE_OUTER_BOUND('',#1942,.T.);
#1344=FACE_OUTER_BOUND('',#1943,.T.);
#1345=FACE_OUTER_BOUND('',#1944,.T.);
#1940=EDGE_LOOP('',(#8068,#8069));
#1941=EDGE_LOOP('',(#8070,#8071));
#1942=EDGE_LOOP('',(#8072,#8073,#8074,#8075,#8076,#8077));
#1943=EDGE_LOOP('',(#8078,#8079));
#1944=EDGE_LOOP('',(#8080,#8081));
#2449=CIRCLE('',#10809,2.);
#2450=CIRCLE('',#10811,2.);
#3077=LINE('',#23954,#3827);
#3078=LINE('',#23958,#3828);
#3827=VECTOR('',#12796,1000.);
#3828=VECTOR('',#12799,1000.);
#4640=VERTEX_POINT('',#23951);
#4641=VERTEX_POINT('',#23952);
#4642=VERTEX_POINT('',#23956);
#4643=VERTEX_POINT('',#23957);
#5847=EDGE_CURVE('',#4640,#4641,#2449,.T.);
#5848=EDGE_CURVE('',#4641,#4640,#3077,.T.);
#5849=EDGE_CURVE('',#4642,#4643,#3078,.T.);
#5850=EDGE_CURVE('',#4642,#4643,#2450,.T.);
#5851=EDGE_CURVE('',#4640,#4642,#202,.T.);
#5852=EDGE_CURVE('',#4642,#4643,#637,.T.);
#5853=EDGE_CURVE('',#4640,#4641,#638,.T.);
#8068=ORIENTED_EDGE('',*,*,#5847,.T.);
#8069=ORIENTED_EDGE('',*,*,#5848,.T.);
#8070=ORIENTED_EDGE('',*,*,#5849,.F.);
#8071=ORIENTED_EDGE('',*,*,#5850,.T.);
#8072=ORIENTED_EDGE('',*,*,#5847,.F.);
#8073=ORIENTED_EDGE('',*,*,#5851,.T.);
#8074=ORIENTED_EDGE('',*,*,#5852,.T.);
#8075=ORIENTED_EDGE('',*,*,#5850,.F.);
#8076=ORIENTED_EDGE('',*,*,#5851,.F.);
#8077=ORIENTED_EDGE('',*,*,#5853,.T.);
#8078=ORIENTED_EDGE('',*,*,#5853,.F.);
#8079=ORIENTED_EDGE('',*,*,#5848,.F.);
#8080=ORIENTED_EDGE('',*,*,#5849,.T.);
#8081=ORIENTED_EDGE('',*,*,#5852,.F.);
#9707=ADVANCED_FACE('',(#1341),#914,.F.);
#9708=ADVANCED_FACE('',(#1342),#915,.T.);
#9709=ADVANCED_FACE('',(#1343),#459,.F.);
#9710=ADVANCED_FACE('',(#1344),#916,.F.);
#9711=ADVANCED_FACE('',(#1345),#917,.F.);
#9954=CLOSED_SHELL('',(#9707,#9708,#9709,#9710,#9711));
#10807=AXIS2_PLACEMENT_3D('',#23949,#12790,#12791);
#10808=AXIS2_PLACEMENT_3D('',#23950,#12792,#12793);
#10809=AXIS2_PLACEMENT_3D('',#23953,#12794,#12795);
#10810=AXIS2_PLACEMENT_3D('',#23955,#12797,#12798);
#10811=AXIS2_PLACEMENT_3D('',#23959,#12800,#12801);
#10812=AXIS2_PLACEMENT_3D('',#27726,#12802,#12803);
#10813=AXIS2_PLACEMENT_3D('',#27727,#12804,#12805);
#12790=DIRECTION('axis',(0.,0.,1.));
#12791=DIRECTION('refdir',(1.,0.,0.));
#12792=DIRECTION('center_axis',(-1.,-1.09403464434161E-29,5.38490012450672E-30));
#12793=DIRECTION('ref_axis',(5.38490012450672E-30,4.73316543132608E-30,
1.));
#12794=DIRECTION('center_axis',(1.,1.09403464434161E-29,5.39106310032879E-30));
#12795=DIRECTION('ref_axis',(5.39106310032879E-30,-6.12323399573724E-17,
-1.));
#12796=DIRECTION('',(-5.38490012450672E-30,1.21234028674329E-16,-1.));
#12797=DIRECTION('center_axis',(-1.,-1.09403464434161E-29,5.38490012450672E-30));
#12798=DIRECTION('ref_axis',(5.38490012450672E-30,4.73316543132608E-30,
1.));
#12799=DIRECTION('',(5.38490012450672E-30,4.73316543132608E-30,1.));
#12800=DIRECTION('center_axis',(-1.,-1.09403464434161E-29,-5.39106310032879E-30));
#12801=DIRECTION('ref_axis',(5.39106310032879E-30,1.17892770941212E-58,
-1.));
#12802=DIRECTION('center_axis',(1.09403464434161E-29,1.,1.21234028674329E-16));
#12803=DIRECTION('ref_axis',(5.38490012450672E-30,-1.21234028674329E-16,
1.));
#12804=DIRECTION('center_axis',(-1.09403464434161E-29,-1.,4.73316543132608E-30));
#12805=DIRECTION('ref_axis',(-5.38490012450672E-30,-4.73316543132608E-30,
-1.));
#23949=CARTESIAN_POINT('',(0.,0.,0.));
#23950=CARTESIAN_POINT('Origin',(5.54667823983524E-29,0.,9.29999999999998));
#23951=CARTESIAN_POINT('',(2.77333911991762E-29,0.,5.29999999999999));
#23952=CARTESIAN_POINT('',(5.54667823983524E-29,0.,9.29999999999998));
#23953=CARTESIAN_POINT('Origin',(4.16000867987643E-29,0.,7.29999999999999));
#23954=CARTESIAN_POINT('',(5.54667823983524E-29,0.,9.29999999999998));
#23955=CARTESIAN_POINT('Origin',(1.03537993810258E-27,90.,9.29999999999998));
#23956=CARTESIAN_POINT('',(1.01689101063646E-27,90.,5.3));
#23957=CARTESIAN_POINT('',(1.03537993810258E-27,90.,9.29999999999998));
#23958=CARTESIAN_POINT('',(1.03537993810258E-27,90.,9.29999999999998));
#23959=CARTESIAN_POINT('Origin',(1.02613547436952E-27,90.,7.3));
#23960=CARTESIAN_POINT('Ctrl Pts',(2.77333911991762E-29,0.,5.29999999999999));
#23961=CARTESIAN_POINT('Ctrl Pts',(-1.42013071988495,0.197368421052638,
5.29999999999998));
#23962=CARTESIAN_POINT('Ctrl Pts',(-2.65,0.394736842105281,4.58993464005751));
#23963=CARTESIAN_POINT('Ctrl Pts',(-3.87986928011504,0.592105263157915,
3.87986928011505));
#23964=CARTESIAN_POINT('Ctrl Pts',(-4.58993464005751,0.789473684210562,
2.65));
#23965=CARTESIAN_POINT('Ctrl Pts',(-5.29999999999999,0.986842105263191,
1.42013071988495));
#23966=CARTESIAN_POINT('Ctrl Pts',(-5.29999999999999,1.18421052631579,3.24531401774024E-16));
#23967=CARTESIAN_POINT('Ctrl Pts',(-5.29999999999999,1.38157894736841,-1.42013071988495));
#23968=CARTESIAN_POINT('Ctrl Pts',(-4.58993464005751,1.57894736842107,-2.64999999999999));
#23969=CARTESIAN_POINT('Ctrl Pts',(-3.87986928011504,1.77631578947369,-3.87986928011504));
#23970=CARTESIAN_POINT('Ctrl Pts',(-2.65,1.97368421052629,-4.58993464005751));
#23971=CARTESIAN_POINT('Ctrl Pts',(-1.42013071988495,2.17105263157891,-5.29999999999999));
#23972=CARTESIAN_POINT('Ctrl Pts',(-6.49062803548097E-16,2.36842105263158,
-5.29999999999999));
#23973=CARTESIAN_POINT('Ctrl Pts',(1.42013071988495,2.56578947368418,-5.29999999999999));
#23974=CARTESIAN_POINT('Ctrl Pts',(2.64999999999999,2.7631578947368,-4.58993464005751));
#23975=CARTESIAN_POINT('Ctrl Pts',(3.87986928011504,2.96052631578946,-3.87986928011505));
#23976=CARTESIAN_POINT('Ctrl Pts',(4.58993464005751,3.15789473684208,-2.65));
#23977=CARTESIAN_POINT('Ctrl Pts',(5.29999999999999,3.35526315789473,-1.42013071988495));
#23978=CARTESIAN_POINT('Ctrl Pts',(5.29999999999999,3.55263157894736,-9.73594205321085E-16));
#23979=CARTESIAN_POINT('Ctrl Pts',(5.29999999999999,3.75000000000001,1.42013071988494));
#23980=CARTESIAN_POINT('Ctrl Pts',(4.58993464005752,3.94736842105264,2.64999999999999));
#23981=CARTESIAN_POINT('Ctrl Pts',(3.87986928011505,4.14473684210529,3.87986928011504));
#23982=CARTESIAN_POINT('Ctrl Pts',(2.65,4.34210526315792,4.58993464005751));
#23983=CARTESIAN_POINT('Ctrl Pts',(1.42013071988495,4.53947368421056,5.29999999999998));
#23984=CARTESIAN_POINT('Ctrl Pts',(8.32001735975286E-29,4.73684210526315,
5.29999999999999));
#23985=CARTESIAN_POINT('Ctrl Pts',(-1.42013071988495,4.93421052631578,5.29999999999999));
#23986=CARTESIAN_POINT('Ctrl Pts',(-2.65,5.13157894736843,4.58993464005751));
#23987=CARTESIAN_POINT('Ctrl Pts',(-3.87986928011504,5.32894736842106,3.87986928011505));
#23988=CARTESIAN_POINT('Ctrl Pts',(-4.58993464005751,5.52631578947371,2.65));
#23989=CARTESIAN_POINT('Ctrl Pts',(-5.29999999999999,5.72368421052634,1.42013071988495));
#23990=CARTESIAN_POINT('Ctrl Pts',(-5.29999999999999,5.92105263157894,3.24531401774024E-16));
#23991=CARTESIAN_POINT('Ctrl Pts',(-5.29999999999999,6.11842105263156,-1.42013071988495));
#23992=CARTESIAN_POINT('Ctrl Pts',(-4.58993464005751,6.31578947368422,-2.64999999999999));
#23993=CARTESIAN_POINT('Ctrl Pts',(-3.87986928011504,6.51315789473683,-3.87986928011504));
#23994=CARTESIAN_POINT('Ctrl Pts',(-2.65,6.71052631578944,-4.58993464005751));
#23995=CARTESIAN_POINT('Ctrl Pts',(-1.42013071988495,6.90789473684211,-5.29999999999999));
#23996=CARTESIAN_POINT('Ctrl Pts',(-6.49062803548043E-16,7.10526315789473,
-5.29999999999999));
#23997=CARTESIAN_POINT('Ctrl Pts',(1.42013071988495,7.30263157894733,-5.29999999999999));
#23998=CARTESIAN_POINT('Ctrl Pts',(2.64999999999999,7.50000000000001,-4.58993464005751));
#23999=CARTESIAN_POINT('Ctrl Pts',(3.87986928011504,7.69736842105261,-3.87986928011505));
#24000=CARTESIAN_POINT('Ctrl Pts',(4.58993464005751,7.89473684210523,-2.65));
#24001=CARTESIAN_POINT('Ctrl Pts',(5.29999999999999,8.09210526315788,-1.42013071988495));
#24002=CARTESIAN_POINT('Ctrl Pts',(5.29999999999999,8.28947368421051,-9.73594205321085E-16));
#24003=CARTESIAN_POINT('Ctrl Pts',(5.29999999999999,8.48684210526316,1.42013071988495));
#24004=CARTESIAN_POINT('Ctrl Pts',(4.58993464005752,8.68421052631579,2.64999999999999));
#24005=CARTESIAN_POINT('Ctrl Pts',(3.87986928011505,8.88157894736843,3.87986928011504));
#24006=CARTESIAN_POINT('Ctrl Pts',(2.65,9.07894736842108,4.58993464005751));
#24007=CARTESIAN_POINT('Ctrl Pts',(1.42013071988495,9.27631578947371,5.29999999999999));
#24008=CARTESIAN_POINT('Ctrl Pts',(1.35585468084861E-28,9.47368421052636,
5.3));
#24009=CARTESIAN_POINT('Ctrl Pts',(-1.42013071988495,9.67105263157899,5.29999999999998));
#24010=CARTESIAN_POINT('Ctrl Pts',(-2.65,9.86842105263158,4.58993464005751));
#24011=CARTESIAN_POINT('Ctrl Pts',(-3.87986928011504,10.0657894736842,3.87986928011504));
#24012=CARTESIAN_POINT('Ctrl Pts',(-4.58993464005751,10.2631578947369,2.65));
#24013=CARTESIAN_POINT('Ctrl Pts',(-5.29999999999999,10.4605263157895,1.42013071988495));
#24014=CARTESIAN_POINT('Ctrl Pts',(-5.29999999999999,10.6578947368421,3.24531401772841E-16));
#24015=CARTESIAN_POINT('Ctrl Pts',(-5.29999999999999,10.8552631578948,-1.42013071988495));
#24016=CARTESIAN_POINT('Ctrl Pts',(-4.58993464005751,11.0526315789474,-2.64999999999999));
#24017=CARTESIAN_POINT('Ctrl Pts',(-3.87986928011504,11.25,-3.87986928011504));
#24018=CARTESIAN_POINT('Ctrl Pts',(-2.65,11.4473684210526,-4.58993464005751));
#24019=CARTESIAN_POINT('Ctrl Pts',(-1.42013071988495,11.6447368421052,-5.29999999999999));
#24020=CARTESIAN_POINT('Ctrl Pts',(-6.49062803547995E-16,11.8421052631579,
-5.29999999999999));
#24021=CARTESIAN_POINT('Ctrl Pts',(1.42013071988495,12.0394736842105,-5.29999999999999));
#24022=CARTESIAN_POINT('Ctrl Pts',(2.64999999999999,12.2368421052632,-4.58993464005751));
#24023=CARTESIAN_POINT('Ctrl Pts',(3.87986928011504,12.4342105263158,-3.87986928011505));
#24024=CARTESIAN_POINT('Ctrl Pts',(4.58993464005751,12.6315789473684,-2.65));
#24025=CARTESIAN_POINT('Ctrl Pts',(5.29999999999999,12.828947368421,-1.42013071988495));
#24026=CARTESIAN_POINT('Ctrl Pts',(5.29999999999999,13.0263157894737,-9.73594205322072E-16));
#24027=CARTESIAN_POINT('Ctrl Pts',(5.29999999999999,13.2236842105263,1.42013071988495));
#24028=CARTESIAN_POINT('Ctrl Pts',(4.58993464005752,13.4210526315789,2.64999999999999));
#24029=CARTESIAN_POINT('Ctrl Pts',(3.87986928011505,13.6184210526316,3.87986928011504));
#24030=CARTESIAN_POINT('Ctrl Pts',(2.65,13.8157894736842,4.58993464005751));
#24031=CARTESIAN_POINT('Ctrl Pts',(1.42013071988495,14.0131578947369,5.29999999999998));
#24032=CARTESIAN_POINT('Ctrl Pts',(1.84889274661175E-28,14.2105263157895,
5.3));
#24033=CARTESIAN_POINT('Ctrl Pts',(-1.42013071988495,14.4078947368421,5.29999999999999));
#24034=CARTESIAN_POINT('Ctrl Pts',(-2.65,14.6052631578947,4.58993464005751));
#24035=CARTESIAN_POINT('Ctrl Pts',(-3.87986928011504,14.8026315789474,3.87986928011504));
#24036=CARTESIAN_POINT('Ctrl Pts',(-4.58993464005751,15.,2.65));
#24037=CARTESIAN_POINT('Ctrl Pts',(-5.29999999999999,15.1973684210526,1.42013071988495));
#24038=CARTESIAN_POINT('Ctrl Pts',(-5.29999999999999,15.3947368421052,3.24531401774024E-16));
#24039=CARTESIAN_POINT('Ctrl Pts',(-5.29999999999999,15.5921052631579,-1.42013071988495));
#24040=CARTESIAN_POINT('Ctrl Pts',(-4.58993464005751,15.7894736842105,-2.64999999999999));
#24041=CARTESIAN_POINT('Ctrl Pts',(-3.87986928011504,15.9868421052631,-3.87986928011504));
#24042=CARTESIAN_POINT('Ctrl Pts',(-2.65,16.1842105263157,-4.58993464005751));
#24043=CARTESIAN_POINT('Ctrl Pts',(-1.42013071988495,16.3815789473684,-5.29999999999999));
#24044=CARTESIAN_POINT('Ctrl Pts',(-6.49062803547949E-16,16.578947368421,
-5.29999999999999));
#24045=CARTESIAN_POINT('Ctrl Pts',(1.42013071988495,16.7763157894737,-5.29999999999999));
#24046=CARTESIAN_POINT('Ctrl Pts',(2.64999999999999,16.9736842105263,-4.58993464005751));
#24047=CARTESIAN_POINT('Ctrl Pts',(3.87986928011504,17.171052631579,-3.87986928011505));
#24048=CARTESIAN_POINT('Ctrl Pts',(4.58993464005751,17.3684210526316,-2.65));
#24049=CARTESIAN_POINT('Ctrl Pts',(5.29999999999999,17.5657894736842,-1.42013071988495));
#24050=CARTESIAN_POINT('Ctrl Pts',(5.29999999999999,17.7631578947368,-9.73594205322269E-16));
#24051=CARTESIAN_POINT('Ctrl Pts',(5.29999999999999,17.9605263157895,1.42013071988494));
#24052=CARTESIAN_POINT('Ctrl Pts',(4.58993464005752,18.1578947368421,2.64999999999999));
#24053=CARTESIAN_POINT('Ctrl Pts',(3.87986928011505,18.3552631578947,3.87986928011504));
#24054=CARTESIAN_POINT('Ctrl Pts',(2.65,18.5526315789474,4.58993464005751));
#24055=CARTESIAN_POINT('Ctrl Pts',(1.42013071988495,18.75,5.29999999999998));
#24056=CARTESIAN_POINT('Ctrl Pts',(2.31111593326468E-28,18.9473684210527,
5.3));
#24057=CARTESIAN_POINT('Ctrl Pts',(-1.42013071988495,19.1447368421053,5.29999999999999));
#24058=CARTESIAN_POINT('Ctrl Pts',(-2.65,19.3421052631579,4.58993464005751));
#24059=CARTESIAN_POINT('Ctrl Pts',(-3.87986928011504,19.5394736842105,3.87986928011504));
#24060=CARTESIAN_POINT('Ctrl Pts',(-4.58993464005751,19.7368421052632,2.65));
#24061=CARTESIAN_POINT('Ctrl Pts',(-5.29999999999999,19.9342105263158,1.42013071988495));
#24062=CARTESIAN_POINT('Ctrl Pts',(-5.29999999999999,20.1315789473684,3.24531401774221E-16));
#24063=CARTESIAN_POINT('Ctrl Pts',(-5.29999999999999,20.328947368421,-1.42013071988495));
#24064=CARTESIAN_POINT('Ctrl Pts',(-4.58993464005751,20.5263157894737,-2.64999999999999));
#24065=CARTESIAN_POINT('Ctrl Pts',(-3.87986928011504,20.7236842105263,-3.87986928011504));
#24066=CARTESIAN_POINT('Ctrl Pts',(-2.65,20.921052631579,-4.58993464005751));
#24067=CARTESIAN_POINT('Ctrl Pts',(-1.42013071988495,21.1184210526315,-5.29999999999999));
#24068=CARTESIAN_POINT('Ctrl Pts',(-6.49062803547894E-16,21.3157894736842,
-5.29999999999999));
#24069=CARTESIAN_POINT('Ctrl Pts',(1.42013071988495,21.5131578947368,-5.29999999999999));
#24070=CARTESIAN_POINT('Ctrl Pts',(2.64999999999999,21.7105263157895,-4.58993464005751));
#24071=CARTESIAN_POINT('Ctrl Pts',(3.87986928011504,21.9078947368421,-3.87986928011505));
#24072=CARTESIAN_POINT('Ctrl Pts',(4.58993464005751,22.1052631578947,-2.65));
#24073=CARTESIAN_POINT('Ctrl Pts',(5.29999999999999,22.3026315789474,-1.42013071988495));
#24074=CARTESIAN_POINT('Ctrl Pts',(5.29999999999999,22.5,-9.73594205320888E-16));
#24075=CARTESIAN_POINT('Ctrl Pts',(5.29999999999999,22.6973684210527,1.42013071988495));
#24076=CARTESIAN_POINT('Ctrl Pts',(4.58993464005752,22.8947368421052,2.64999999999999));
#24077=CARTESIAN_POINT('Ctrl Pts',(3.87986928011505,23.0921052631579,3.87986928011504));
#24078=CARTESIAN_POINT('Ctrl Pts',(2.65,23.2894736842105,4.58993464005751));
#24079=CARTESIAN_POINT('Ctrl Pts',(1.42013071988495,23.4868421052631,5.29999999999999));
#24080=CARTESIAN_POINT('Ctrl Pts',(2.95822839457879E-28,23.6842105263158,
5.3));
#24081=CARTESIAN_POINT('Ctrl Pts',(-1.42013071988495,23.8815789473684,5.29999999999998));
#24082=CARTESIAN_POINT('Ctrl Pts',(-2.65,24.0789473684211,4.58993464005751));
#24083=CARTESIAN_POINT('Ctrl Pts',(-3.87986928011504,24.2763157894737,3.87986928011504));
#24084=CARTESIAN_POINT('Ctrl Pts',(-4.58993464005751,24.4736842105263,2.65));
#24085=CARTESIAN_POINT('Ctrl Pts',(-5.29999999999999,24.671052631579,1.42013071988495));
#24086=CARTESIAN_POINT('Ctrl Pts',(-5.29999999999999,24.8684210526316,3.24531401774024E-16));
#24087=CARTESIAN_POINT('Ctrl Pts',(-5.29999999999999,25.0657894736842,-1.42013071988495));
#24088=CARTESIAN_POINT('Ctrl Pts',(-4.58993464005751,25.2631578947368,-2.64999999999999));
#24089=CARTESIAN_POINT('Ctrl Pts',(-3.87986928011504,25.4605263157895,-3.87986928011504));
#24090=CARTESIAN_POINT('Ctrl Pts',(-2.65,25.6578947368421,-4.58993464005751));
#24091=CARTESIAN_POINT('Ctrl Pts',(-1.42013071988495,25.8552631578947,-5.29999999999999));
#24092=CARTESIAN_POINT('Ctrl Pts',(-6.49062803547834E-16,26.0526315789473,
-5.29999999999999));
#24093=CARTESIAN_POINT('Ctrl Pts',(1.42013071988495,26.25,-5.29999999999999));
#24094=CARTESIAN_POINT('Ctrl Pts',(2.64999999999999,26.4473684210526,-4.58993464005752));
#24095=CARTESIAN_POINT('Ctrl Pts',(3.87986928011504,26.6447368421052,-3.87986928011505));
#24096=CARTESIAN_POINT('Ctrl Pts',(4.58993464005751,26.8421052631579,-2.65));
#24097=CARTESIAN_POINT('Ctrl Pts',(5.29999999999999,27.0394736842105,-1.42013071988495));
#24098=CARTESIAN_POINT('Ctrl Pts',(5.29999999999999,27.2368421052632,-9.73594205320888E-16));
#24099=CARTESIAN_POINT('Ctrl Pts',(5.29999999999999,27.4342105263158,1.42013071988495));
#24100=CARTESIAN_POINT('Ctrl Pts',(4.58993464005752,27.6315789473685,2.64999999999999));
#24101=CARTESIAN_POINT('Ctrl Pts',(3.87986928011505,27.8289473684211,3.87986928011504));
#24102=CARTESIAN_POINT('Ctrl Pts',(2.65,28.0263157894737,4.58993464005751));
#24103=CARTESIAN_POINT('Ctrl Pts',(1.42013071988495,28.2236842105264,5.29999999999998));
#24104=CARTESIAN_POINT('Ctrl Pts',(3.42045158123173E-28,28.421052631579,
5.3));
#24105=CARTESIAN_POINT('Ctrl Pts',(-1.42013071988495,28.6184210526316,5.29999999999999));
#24106=CARTESIAN_POINT('Ctrl Pts',(-2.65,28.8157894736842,4.58993464005751));
#24107=CARTESIAN_POINT('Ctrl Pts',(-3.87986928011504,29.0131578947368,3.87986928011504));
#24108=CARTESIAN_POINT('Ctrl Pts',(-4.58993464005751,29.2105263157895,2.65));
#24109=CARTESIAN_POINT('Ctrl Pts',(-5.29999999999999,29.4078947368421,1.42013071988495));
#24110=CARTESIAN_POINT('Ctrl Pts',(-5.29999999999999,29.6052631578947,3.24531401774024E-16));
#24111=CARTESIAN_POINT('Ctrl Pts',(-5.29999999999999,29.8026315789473,-1.42013071988495));
#24112=CARTESIAN_POINT('Ctrl Pts',(-4.58993464005751,30.,-2.64999999999999));
#24113=CARTESIAN_POINT('Ctrl Pts',(-3.87986928011504,30.1973684210526,-3.87986928011504));
#24114=CARTESIAN_POINT('Ctrl Pts',(-2.65,30.3947368421053,-4.58993464005751));
#24115=CARTESIAN_POINT('Ctrl Pts',(-1.42013071988495,30.5921052631579,-5.29999999999999));
#24116=CARTESIAN_POINT('Ctrl Pts',(-6.49062803547783E-16,30.7894736842105,
-5.29999999999999));
#24117=CARTESIAN_POINT('Ctrl Pts',(1.42013071988495,30.9868421052631,-5.29999999999999));
#24118=CARTESIAN_POINT('Ctrl Pts',(2.64999999999999,31.1842105263158,-4.58993464005752));
#24119=CARTESIAN_POINT('Ctrl Pts',(3.87986928011504,31.3815789473684,-3.87986928011505));
#24120=CARTESIAN_POINT('Ctrl Pts',(4.58993464005751,31.578947368421,-2.65));
#24121=CARTESIAN_POINT('Ctrl Pts',(5.29999999999999,31.7763157894737,-1.42013071988495));
#24122=CARTESIAN_POINT('Ctrl Pts',(5.29999999999999,31.9736842105263,-9.73594205321085E-16));
#24123=CARTESIAN_POINT('Ctrl Pts',(5.29999999999999,32.1710526315789,1.42013071988495));
#24124=CARTESIAN_POINT('Ctrl Pts',(4.58993464005752,32.3684210526316,2.64999999999999));
#24125=CARTESIAN_POINT('Ctrl Pts',(3.87986928011505,32.5657894736842,3.87986928011504));
#24126=CARTESIAN_POINT('Ctrl Pts',(2.65,32.7631578947368,4.58993464005751));
#24127=CARTESIAN_POINT('Ctrl Pts',(1.42013071988495,32.9605263157895,5.29999999999999));
#24128=CARTESIAN_POINT('Ctrl Pts',(3.88267476788467E-28,33.1578947368421,
5.3));
#24129=CARTESIAN_POINT('Ctrl Pts',(-1.42013071988495,33.3552631578948,5.29999999999998));
#24130=CARTESIAN_POINT('Ctrl Pts',(-2.65,33.5526315789474,4.58993464005751));
#24131=CARTESIAN_POINT('Ctrl Pts',(-3.87986928011504,33.75,3.87986928011505));
#24132=CARTESIAN_POINT('Ctrl Pts',(-4.58993464005751,33.9473684210526,2.65));
#24133=CARTESIAN_POINT('Ctrl Pts',(-5.29999999999999,34.1447368421052,1.42013071988495));
#24134=CARTESIAN_POINT('Ctrl Pts',(-5.29999999999999,34.3421052631579,3.24531401774024E-16));
#24135=CARTESIAN_POINT('Ctrl Pts',(-5.29999999999999,34.5394736842105,-1.42013071988495));
#24136=CARTESIAN_POINT('Ctrl Pts',(-4.58993464005751,34.7368421052631,-2.65));
#24137=CARTESIAN_POINT('Ctrl Pts',(-3.87986928011504,34.9342105263158,-3.87986928011504));
#24138=CARTESIAN_POINT('Ctrl Pts',(-2.65,35.1315789473684,-4.58993464005751));
#24139=CARTESIAN_POINT('Ctrl Pts',(-1.42013071988495,35.328947368421,-5.29999999999999));
#24140=CARTESIAN_POINT('Ctrl Pts',(-6.49062803547736E-16,35.5263157894737,
-5.29999999999999));
#24141=CARTESIAN_POINT('Ctrl Pts',(1.42013071988495,35.7236842105263,-5.29999999999999));
#24142=CARTESIAN_POINT('Ctrl Pts',(2.64999999999999,35.9210526315789,-4.58993464005752));
#24143=CARTESIAN_POINT('Ctrl Pts',(3.87986928011504,36.1184210526315,-3.87986928011505));
#24144=CARTESIAN_POINT('Ctrl Pts',(4.58993464005751,36.3157894736842,-2.65));
#24145=CARTESIAN_POINT('Ctrl Pts',(5.29999999999999,36.5131578947368,-1.42013071988495));
#24146=CARTESIAN_POINT('Ctrl Pts',(5.29999999999999,36.7105263157895,-9.73594205322072E-16));
#24147=CARTESIAN_POINT('Ctrl Pts',(5.29999999999999,36.9078947368421,1.42013071988495));
#24148=CARTESIAN_POINT('Ctrl Pts',(4.58993464005752,37.1052631578948,2.64999999999999));
#24149=CARTESIAN_POINT('Ctrl Pts',(3.87986928011505,37.3026315789473,3.87986928011504));
#24150=CARTESIAN_POINT('Ctrl Pts',(2.65,37.5,4.58993464005751));
#24151=CARTESIAN_POINT('Ctrl Pts',(1.42013071988495,37.6973684210526,5.29999999999998));
#24152=CARTESIAN_POINT('Ctrl Pts',(4.42193515231309E-28,37.8947368421053,
5.29999999999999));
#24153=CARTESIAN_POINT('Ctrl Pts',(-1.42013071988495,38.0921052631579,5.29999999999999));
#24154=CARTESIAN_POINT('Ctrl Pts',(-2.65,38.2894736842105,4.58993464005752));
#24155=CARTESIAN_POINT('Ctrl Pts',(-3.87986928011504,38.4868421052632,3.87986928011504));
#24156=CARTESIAN_POINT('Ctrl Pts',(-4.58993464005751,38.6842105263158,2.65));
#24157=CARTESIAN_POINT('Ctrl Pts',(-5.29999999999999,38.8815789473684,1.42013071988495));
#24158=CARTESIAN_POINT('Ctrl Pts',(-5.29999999999999,39.078947368421,3.24531401774024E-16));
#24159=CARTESIAN_POINT('Ctrl Pts',(-5.29999999999999,39.2763157894737,-1.42013071988495));
#24160=CARTESIAN_POINT('Ctrl Pts',(-4.58993464005751,39.4736842105263,-2.64999999999999));
#24161=CARTESIAN_POINT('Ctrl Pts',(-3.87986928011504,39.6710526315789,-3.87986928011504));
#24162=CARTESIAN_POINT('Ctrl Pts',(-2.65,39.8684210526316,-4.58993464005751));
#24163=CARTESIAN_POINT('Ctrl Pts',(-1.42013071988495,40.0657894736842,-5.29999999999999));
#24164=CARTESIAN_POINT('Ctrl Pts',(-6.49062803547683E-16,40.2631578947368,
-5.29999999999999));
#24165=CARTESIAN_POINT('Ctrl Pts',(1.42013071988495,40.4605263157895,-5.29999999999999));
#24166=CARTESIAN_POINT('Ctrl Pts',(2.64999999999999,40.6578947368421,-4.58993464005752));
#24167=CARTESIAN_POINT('Ctrl Pts',(3.87986928011504,40.8552631578947,-3.87986928011505));
#24168=CARTESIAN_POINT('Ctrl Pts',(4.58993464005751,41.0526315789473,-2.65));
#24169=CARTESIAN_POINT('Ctrl Pts',(5.29999999999999,41.25,-1.42013071988495));
#24170=CARTESIAN_POINT('Ctrl Pts',(5.29999999999999,41.4473684210526,-9.73594205322072E-16));
#24171=CARTESIAN_POINT('Ctrl Pts',(5.29999999999999,41.6447368421053,1.42013071988495));
#24172=CARTESIAN_POINT('Ctrl Pts',(4.58993464005752,41.8421052631579,2.64999999999999));
#24173=CARTESIAN_POINT('Ctrl Pts',(3.87986928011505,42.0394736842106,3.87986928011504));
#24174=CARTESIAN_POINT('Ctrl Pts',(2.65,42.2368421052632,4.58993464005751));
#24175=CARTESIAN_POINT('Ctrl Pts',(1.42013071988495,42.4342105263158,5.29999999999999));
#24176=CARTESIAN_POINT('Ctrl Pts',(4.99201041585172E-28,42.6315789473684,
5.29999999999999));
#24177=CARTESIAN_POINT('Ctrl Pts',(-1.42013071988495,42.8289473684211,5.29999999999998));
#24178=CARTESIAN_POINT('Ctrl Pts',(-2.65,43.0263157894737,4.58993464005752));
#24179=CARTESIAN_POINT('Ctrl Pts',(-3.87986928011504,43.2236842105263,3.87986928011504));
#24180=CARTESIAN_POINT('Ctrl Pts',(-4.58993464005751,43.421052631579,2.65));
#24181=CARTESIAN_POINT('Ctrl Pts',(-5.29999999999999,43.6184210526316,1.42013071988495));
#24182=CARTESIAN_POINT('Ctrl Pts',(-5.29999999999999,43.8157894736842,3.24531401774024E-16));
#24183=CARTESIAN_POINT('Ctrl Pts',(-5.29999999999999,44.0131578947368,-1.42013071988495));
#24184=CARTESIAN_POINT('Ctrl Pts',(-4.58993464005751,44.2105263157895,-2.64999999999999));
#24185=CARTESIAN_POINT('Ctrl Pts',(-3.87986928011504,44.4078947368421,-3.87986928011504));
#24186=CARTESIAN_POINT('Ctrl Pts',(-2.65,44.6052631578947,-4.58993464005751));
#24187=CARTESIAN_POINT('Ctrl Pts',(-1.42013071988495,44.8026315789473,-5.29999999999999));
#24188=CARTESIAN_POINT('Ctrl Pts',(-6.49062803547635E-16,45.,-5.29999999999999));
#24189=CARTESIAN_POINT('Ctrl Pts',(1.42013071988495,45.1973684210526,-5.29999999999999));
#24190=CARTESIAN_POINT('Ctrl Pts',(2.64999999999999,45.3947368421053,-4.58993464005752));
#24191=CARTESIAN_POINT('Ctrl Pts',(3.87986928011504,45.5921052631579,-3.87986928011505));
#24192=CARTESIAN_POINT('Ctrl Pts',(4.58993464005751,45.7894736842105,-2.65));
#24193=CARTESIAN_POINT('Ctrl Pts',(5.29999999999999,45.9868421052631,-1.42013071988495));
#24194=CARTESIAN_POINT('Ctrl Pts',(5.29999999999999,46.1842105263158,-9.73594205321085E-16));
#24195=CARTESIAN_POINT('Ctrl Pts',(5.29999999999999,46.3815789473684,1.42013071988495));
#24196=CARTESIAN_POINT('Ctrl Pts',(4.58993464005752,46.5789473684211,2.64999999999999));
#24197=CARTESIAN_POINT('Ctrl Pts',(3.87986928011505,46.7763157894737,3.87986928011504));
#24198=CARTESIAN_POINT('Ctrl Pts',(2.65,46.9736842105263,4.58993464005752));
#24199=CARTESIAN_POINT('Ctrl Pts',(1.42013071988495,47.1710526315789,5.29999999999999));
#24200=CARTESIAN_POINT('Ctrl Pts',(5.54667823983524E-28,47.3684210526316,
5.29999999999999));
#24201=CARTESIAN_POINT('Ctrl Pts',(-1.42013071988495,47.5657894736842,5.29999999999998));
#24202=CARTESIAN_POINT('Ctrl Pts',(-2.65,47.7631578947368,4.58993464005752));
#24203=CARTESIAN_POINT('Ctrl Pts',(-3.87986928011504,47.9605263157895,3.87986928011504));
#24204=CARTESIAN_POINT('Ctrl Pts',(-4.58993464005751,48.1578947368421,2.65));
#24205=CARTESIAN_POINT('Ctrl Pts',(-5.29999999999999,48.3552631578947,1.42013071988495));
#24206=CARTESIAN_POINT('Ctrl Pts',(-5.29999999999999,48.5526315789474,3.24531401773827E-16));
#24207=CARTESIAN_POINT('Ctrl Pts',(-5.29999999999999,48.75,-1.42013071988495));
#24208=CARTESIAN_POINT('Ctrl Pts',(-4.58993464005751,48.9473684210526,-2.64999999999999));
#24209=CARTESIAN_POINT('Ctrl Pts',(-3.87986928011504,49.1447368421053,-3.87986928011504));
#24210=CARTESIAN_POINT('Ctrl Pts',(-2.65,49.3421052631579,-4.58993464005751));
#24211=CARTESIAN_POINT('Ctrl Pts',(-1.42013071988495,49.5394736842105,-5.29999999999999));
#24212=CARTESIAN_POINT('Ctrl Pts',(-6.49062803547579E-16,49.7368421052631,
-5.29999999999999));
#24213=CARTESIAN_POINT('Ctrl Pts',(1.42013071988495,49.9342105263158,-5.29999999999999));
#24214=CARTESIAN_POINT('Ctrl Pts',(2.64999999999999,50.1315789473684,-4.58993464005752));
#24215=CARTESIAN_POINT('Ctrl Pts',(3.87986928011504,50.328947368421,-3.87986928011505));
#24216=CARTESIAN_POINT('Ctrl Pts',(4.58993464005751,50.5263157894737,-2.65));
#24217=CARTESIAN_POINT('Ctrl Pts',(5.29999999999999,50.7236842105263,-1.42013071988495));
#24218=CARTESIAN_POINT('Ctrl Pts',(5.29999999999999,50.9210526315789,-9.73594205321085E-16));
#24219=CARTESIAN_POINT('Ctrl Pts',(5.29999999999999,51.1184210526316,1.42013071988495));
#24220=CARTESIAN_POINT('Ctrl Pts',(4.58993464005752,51.3157894736842,2.64999999999999));
#24221=CARTESIAN_POINT('Ctrl Pts',(3.87986928011505,51.5131578947368,3.87986928011504));
#24222=CARTESIAN_POINT('Ctrl Pts',(2.65,51.7105263157895,4.58993464005752));
#24223=CARTESIAN_POINT('Ctrl Pts',(1.42013071988495,51.9078947368421,5.29999999999998));
#24224=CARTESIAN_POINT('Ctrl Pts',(6.00890142648818E-28,52.1052631578948,
5.29999999999999));
#24225=CARTESIAN_POINT('Ctrl Pts',(-1.42013071988495,52.3026315789474,5.29999999999999));
#24226=CARTESIAN_POINT('Ctrl Pts',(-2.65,52.5,4.58993464005752));
#24227=CARTESIAN_POINT('Ctrl Pts',(-3.87986928011504,52.6973684210526,3.87986928011504));
#24228=CARTESIAN_POINT('Ctrl Pts',(-4.58993464005751,52.8947368421053,2.65));
#24229=CARTESIAN_POINT('Ctrl Pts',(-5.29999999999999,53.0921052631579,1.42013071988495));
#24230=CARTESIAN_POINT('Ctrl Pts',(-5.29999999999999,53.2894736842105,3.245314017757E-16));
#24231=CARTESIAN_POINT('Ctrl Pts',(-5.29999999999999,53.4868421052631,-1.42013071988495));
#24232=CARTESIAN_POINT('Ctrl Pts',(-4.58993464005751,53.6842105263158,-2.64999999999999));
#24233=CARTESIAN_POINT('Ctrl Pts',(-3.87986928011504,53.8815789473684,-3.87986928011504));
#24234=CARTESIAN_POINT('Ctrl Pts',(-2.65,54.0789473684211,-4.58993464005751));
#24235=CARTESIAN_POINT('Ctrl Pts',(-1.42013071988495,54.2763157894737,-5.29999999999999));
#24236=CARTESIAN_POINT('Ctrl Pts',(-6.4906280354753E-16,54.4736842105263,
-5.29999999999999));
#24237=CARTESIAN_POINT('Ctrl Pts',(1.42013071988495,54.6710526315789,-5.29999999999999));
#24238=CARTESIAN_POINT('Ctrl Pts',(2.64999999999999,54.8684210526316,-4.58993464005752));
#24239=CARTESIAN_POINT('Ctrl Pts',(3.87986928011504,55.0657894736842,-3.87986928011505));
#24240=CARTESIAN_POINT('Ctrl Pts',(4.58993464005751,55.2631578947368,-2.65));
#24241=CARTESIAN_POINT('Ctrl Pts',(5.29999999999999,55.4605263157895,-1.42013071988495));
#24242=CARTESIAN_POINT('Ctrl Pts',(5.29999999999999,55.6578947368421,-9.73594205321578E-16));
#24243=CARTESIAN_POINT('Ctrl Pts',(5.29999999999999,55.8552631578947,1.42013071988495));
#24244=CARTESIAN_POINT('Ctrl Pts',(4.58993464005752,56.0526315789474,2.64999999999999));
#24245=CARTESIAN_POINT('Ctrl Pts',(3.87986928011505,56.25,3.87986928011504));
#24246=CARTESIAN_POINT('Ctrl Pts',(2.65,56.4473684210526,4.58993464005752));
#24247=CARTESIAN_POINT('Ctrl Pts',(1.42013071988495,56.6447368421052,5.29999999999999));
#24248=CARTESIAN_POINT('Ctrl Pts',(6.5635692504717E-28,56.8421052631579,
5.29999999999999));
#24249=CARTESIAN_POINT('Ctrl Pts',(-1.42013071988495,57.0394736842105,5.29999999999998));
#24250=CARTESIAN_POINT('Ctrl Pts',(-2.65,57.2368421052632,4.58993464005752));
#24251=CARTESIAN_POINT('Ctrl Pts',(-3.87986928011504,57.4342105263158,3.87986928011504));
#24252=CARTESIAN_POINT('Ctrl Pts',(-4.58993464005751,57.6315789473684,2.65));
#24253=CARTESIAN_POINT('Ctrl Pts',(-5.29999999999999,57.8289473684211,1.42013071988495));
#24254=CARTESIAN_POINT('Ctrl Pts',(-5.29999999999999,58.0263157894737,3.24531401775207E-16));
#24255=CARTESIAN_POINT('Ctrl Pts',(-5.29999999999999,58.2236842105263,-1.42013071988495));
#24256=CARTESIAN_POINT('Ctrl Pts',(-4.58993464005751,58.4210526315789,-2.64999999999999));
#24257=CARTESIAN_POINT('Ctrl Pts',(-3.87986928011504,58.6184210526315,-3.87986928011504));
#24258=CARTESIAN_POINT('Ctrl Pts',(-2.65,58.8157894736842,-4.58993464005751));
#24259=CARTESIAN_POINT('Ctrl Pts',(-1.42013071988495,59.0131578947368,-5.29999999999999));
#24260=CARTESIAN_POINT('Ctrl Pts',(-6.49062803547473E-16,59.2105263157894,
-5.29999999999999));
#24261=CARTESIAN_POINT('Ctrl Pts',(1.42013071988495,59.4078947368421,-5.29999999999999));
#24262=CARTESIAN_POINT('Ctrl Pts',(2.64999999999999,59.6052631578947,-4.58993464005752));
#24263=CARTESIAN_POINT('Ctrl Pts',(3.87986928011504,59.8026315789473,-3.87986928011505));
#24264=CARTESIAN_POINT('Ctrl Pts',(4.58993464005751,60.,-2.65));
#24265=CARTESIAN_POINT('Ctrl Pts',(5.29999999999999,60.1973684210526,-1.42013071988495));
#24266=CARTESIAN_POINT('Ctrl Pts',(5.29999999999999,60.3947368421052,-9.73594205321184E-16));
#24267=CARTESIAN_POINT('Ctrl Pts',(5.29999999999999,60.5921052631579,1.42013071988495));
#24268=CARTESIAN_POINT('Ctrl Pts',(4.58993464005752,60.7894736842105,2.64999999999999));
#24269=CARTESIAN_POINT('Ctrl Pts',(3.87986928011505,60.9868421052632,3.87986928011504));
#24270=CARTESIAN_POINT('Ctrl Pts',(2.65,61.1842105263158,4.58993464005752));
#24271=CARTESIAN_POINT('Ctrl Pts',(1.42013071988495,61.3815789473684,5.29999999999998));
#24272=CARTESIAN_POINT('Ctrl Pts',(7.02579243712464E-28,61.5789473684211,
5.29999999999999));
#24273=CARTESIAN_POINT('Ctrl Pts',(-1.42013071988495,61.7763157894737,5.29999999999999));
#24274=CARTESIAN_POINT('Ctrl Pts',(-2.65,61.9736842105264,4.58993464005752));
#24275=CARTESIAN_POINT('Ctrl Pts',(-3.87986928011504,62.171052631579,3.87986928011505));
#24276=CARTESIAN_POINT('Ctrl Pts',(-4.58993464005751,62.3684210526316,2.65));
#24277=CARTESIAN_POINT('Ctrl Pts',(-5.29999999999999,62.5657894736842,1.42013071988495));
#24278=CARTESIAN_POINT('Ctrl Pts',(-5.29999999999999,62.7631578947368,3.24531401775109E-16));
#24279=CARTESIAN_POINT('Ctrl Pts',(-5.29999999999999,62.9605263157895,-1.42013071988495));
#24280=CARTESIAN_POINT('Ctrl Pts',(-4.58993464005751,63.1578947368421,-2.64999999999999));
#24281=CARTESIAN_POINT('Ctrl Pts',(-3.87986928011504,63.3552631578947,-3.87986928011504));
#24282=CARTESIAN_POINT('Ctrl Pts',(-2.65,63.5526315789474,-4.58993464005751));
#24283=CARTESIAN_POINT('Ctrl Pts',(-1.42013071988495,63.75,-5.29999999999999));
#24284=CARTESIAN_POINT('Ctrl Pts',(-6.49062803547422E-16,63.9473684210526,
-5.29999999999999));
#24285=CARTESIAN_POINT('Ctrl Pts',(1.42013071988495,64.1447368421053,-5.29999999999999));
#24286=CARTESIAN_POINT('Ctrl Pts',(2.64999999999999,64.3421052631579,-4.58993464005752));
#24287=CARTESIAN_POINT('Ctrl Pts',(3.87986928011504,64.5394736842105,-3.87986928011505));
#24288=CARTESIAN_POINT('Ctrl Pts',(4.58993464005751,64.7368421052632,-2.65));
#24289=CARTESIAN_POINT('Ctrl Pts',(5.29999999999999,64.9342105263157,-1.42013071988495));
#24290=CARTESIAN_POINT('Ctrl Pts',(5.29999999999999,65.1315789473684,-9.73594205320987E-16));
#24291=CARTESIAN_POINT('Ctrl Pts',(5.29999999999999,65.328947368421,1.42013071988495));
#24292=CARTESIAN_POINT('Ctrl Pts',(4.58993464005752,65.5263157894737,2.64999999999999));
#24293=CARTESIAN_POINT('Ctrl Pts',(3.87986928011505,65.7236842105264,3.87986928011504));
#24294=CARTESIAN_POINT('Ctrl Pts',(2.65,65.9210526315789,4.58993464005752));
#24295=CARTESIAN_POINT('Ctrl Pts',(1.42013071988495,66.1184210526315,5.29999999999999));
#24296=CARTESIAN_POINT('Ctrl Pts',(7.48801562377757E-28,66.3157894736842,
5.29999999999999));
#24297=CARTESIAN_POINT('Ctrl Pts',(-1.42013071988495,66.5131578947368,5.29999999999998));
#24298=CARTESIAN_POINT('Ctrl Pts',(-2.65,66.7105263157894,4.58993464005752));
#24299=CARTESIAN_POINT('Ctrl Pts',(-3.87986928011504,66.9078947368421,3.87986928011504));
#24300=CARTESIAN_POINT('Ctrl Pts',(-4.58993464005751,67.1052631578947,2.65));
#24301=CARTESIAN_POINT('Ctrl Pts',(-5.29999999999999,67.3026315789474,1.42013071988495));
#24302=CARTESIAN_POINT('Ctrl Pts',(-5.29999999999999,67.5,3.24531401774714E-16));
#24303=CARTESIAN_POINT('Ctrl Pts',(-5.29999999999999,67.6973684210526,-1.42013071988495));
#24304=CARTESIAN_POINT('Ctrl Pts',(-4.58993464005751,67.8947368421052,-2.64999999999999));
#24305=CARTESIAN_POINT('Ctrl Pts',(-3.87986928011504,68.0921052631578,-3.87986928011504));
#24306=CARTESIAN_POINT('Ctrl Pts',(-2.65,68.2894736842105,-4.58993464005751));
#24307=CARTESIAN_POINT('Ctrl Pts',(-1.42013071988495,68.4868421052632,-5.29999999999999));
#24308=CARTESIAN_POINT('Ctrl Pts',(-6.49062803547376E-16,68.6842105263158,
-5.29999999999999));
#24309=CARTESIAN_POINT('Ctrl Pts',(1.42013071988495,68.8815789473684,-5.29999999999999));
#24310=CARTESIAN_POINT('Ctrl Pts',(2.64999999999999,69.078947368421,-4.58993464005752));
#24311=CARTESIAN_POINT('Ctrl Pts',(3.87986928011504,69.2763157894736,-3.87986928011505));
#24312=CARTESIAN_POINT('Ctrl Pts',(4.58993464005751,69.4736842105263,-2.65));
#24313=CARTESIAN_POINT('Ctrl Pts',(5.29999999999999,69.6710526315789,-1.42013071988495));
#24314=CARTESIAN_POINT('Ctrl Pts',(5.29999999999999,69.8684210526316,-9.73594205320888E-16));
#24315=CARTESIAN_POINT('Ctrl Pts',(5.29999999999999,70.0657894736842,1.42013071988495));
#24316=CARTESIAN_POINT('Ctrl Pts',(4.58993464005752,70.2631578947369,2.64999999999999));
#24317=CARTESIAN_POINT('Ctrl Pts',(3.87986928011505,70.4605263157895,3.87986928011504));
#24318=CARTESIAN_POINT('Ctrl Pts',(2.65,70.6578947368421,4.58993464005752));
#24319=CARTESIAN_POINT('Ctrl Pts',(1.42013071988495,70.8552631578947,5.29999999999998));
#24320=CARTESIAN_POINT('Ctrl Pts',(7.96564624998561E-28,71.0526315789473,
5.29999999999999));
#24321=CARTESIAN_POINT('Ctrl Pts',(-1.42013071988495,71.2499999999999,5.29999999999999));
#24322=CARTESIAN_POINT('Ctrl Pts',(-2.65,71.4473684210526,4.58993464005751));
#24323=CARTESIAN_POINT('Ctrl Pts',(-3.87986928011504,71.6447368421053,3.87986928011504));
#24324=CARTESIAN_POINT('Ctrl Pts',(-4.58993464005751,71.8421052631579,2.65));
#24325=CARTESIAN_POINT('Ctrl Pts',(-5.29999999999999,72.0394736842105,1.42013071988495));
#24326=CARTESIAN_POINT('Ctrl Pts',(-5.29999999999999,72.2368421052632,3.24531401775306E-16));
#24327=CARTESIAN_POINT('Ctrl Pts',(-5.29999999999999,72.4342105263157,-1.42013071988495));
#24328=CARTESIAN_POINT('Ctrl Pts',(-4.58993464005751,72.6315789473684,-2.64999999999999));
#24329=CARTESIAN_POINT('Ctrl Pts',(-3.87986928011504,72.828947368421,-3.87986928011504));
#24330=CARTESIAN_POINT('Ctrl Pts',(-2.65,73.0263157894737,-4.58993464005751));
#24331=CARTESIAN_POINT('Ctrl Pts',(-1.42013071988495,73.2236842105263,-5.29999999999999));
#24332=CARTESIAN_POINT('Ctrl Pts',(-6.4906280354732E-16,73.421052631579,
-5.29999999999999));
#24333=CARTESIAN_POINT('Ctrl Pts',(1.42013071988495,73.6184210526315,-5.29999999999999));
#24334=CARTESIAN_POINT('Ctrl Pts',(2.64999999999999,73.8157894736842,-4.58993464005751));
#24335=CARTESIAN_POINT('Ctrl Pts',(3.87986928011504,74.0131578947368,-3.87986928011505));
#24336=CARTESIAN_POINT('Ctrl Pts',(4.58993464005751,74.2105263157895,-2.65));
#24337=CARTESIAN_POINT('Ctrl Pts',(5.29999999999999,74.4078947368421,-1.42013071988495));
#24338=CARTESIAN_POINT('Ctrl Pts',(5.29999999999999,74.6052631578947,-9.73594205321085E-16));
#24339=CARTESIAN_POINT('Ctrl Pts',(5.29999999999999,74.8026315789473,1.42013071988495));
#24340=CARTESIAN_POINT('Ctrl Pts',(4.58993464005752,75.,2.64999999999999));
#24341=CARTESIAN_POINT('Ctrl Pts',(3.87986928011505,75.1973684210526,3.87986928011504));
#24342=CARTESIAN_POINT('Ctrl Pts',(2.65,75.3947368421052,4.58993464005751));
#24343=CARTESIAN_POINT('Ctrl Pts',(1.42013071988495,75.5921052631578,5.29999999999998));
#24344=CARTESIAN_POINT('Ctrl Pts',(8.68979590907521E-28,75.7894736842105,
5.29999999999999));
#24345=CARTESIAN_POINT('Ctrl Pts',(-1.42013071988495,75.9868421052631,5.29999999999999));
#24346=CARTESIAN_POINT('Ctrl Pts',(-2.65,76.1842105263158,4.58993464005751));
#24347=CARTESIAN_POINT('Ctrl Pts',(-3.87986928011504,76.3815789473684,3.87986928011504));
#24348=CARTESIAN_POINT('Ctrl Pts',(-4.58993464005751,76.5789473684211,2.65));
#24349=CARTESIAN_POINT('Ctrl Pts',(-5.29999999999999,76.7763157894737,1.42013071988495));
#24350=CARTESIAN_POINT('Ctrl Pts',(-5.29999999999999,76.9736842105263,3.24531401774615E-16));
#24351=CARTESIAN_POINT('Ctrl Pts',(-5.29999999999999,77.1710526315789,-1.42013071988495));
#24352=CARTESIAN_POINT('Ctrl Pts',(-4.58993464005751,77.3684210526315,-2.64999999999999));
#24353=CARTESIAN_POINT('Ctrl Pts',(-3.87986928011504,77.5657894736842,-3.87986928011504));
#24354=CARTESIAN_POINT('Ctrl Pts',(-2.65,77.7631578947368,-4.58993464005751));
#24355=CARTESIAN_POINT('Ctrl Pts',(-1.42013071988495,77.9605263157895,-5.29999999999999));
#24356=CARTESIAN_POINT('Ctrl Pts',(-6.49062803547265E-16,78.1578947368421,
-5.29999999999999));
#24357=CARTESIAN_POINT('Ctrl Pts',(1.42013071988495,78.3552631578948,-5.29999999999999));
#24358=CARTESIAN_POINT('Ctrl Pts',(2.64999999999999,78.5526315789474,-4.58993464005751));
#24359=CARTESIAN_POINT('Ctrl Pts',(3.87986928011504,78.7499999999999,-3.87986928011505));
#24360=CARTESIAN_POINT('Ctrl Pts',(4.58993464005751,78.9473684210526,-2.65));
#24361=CARTESIAN_POINT('Ctrl Pts',(5.29999999999999,79.1447368421052,-1.42013071988495));
#24362=CARTESIAN_POINT('Ctrl Pts',(5.29999999999999,79.3421052631579,-9.73594205320987E-16));
#24363=CARTESIAN_POINT('Ctrl Pts',(5.29999999999999,79.5394736842105,1.42013071988495));
#24364=CARTESIAN_POINT('Ctrl Pts',(4.58993464005752,79.7368421052632,2.64999999999999));
#24365=CARTESIAN_POINT('Ctrl Pts',(3.87986928011505,79.9342105263158,3.87986928011504));
#24366=CARTESIAN_POINT('Ctrl Pts',(2.65,80.1315789473684,4.58993464005751));
#24367=CARTESIAN_POINT('Ctrl Pts',(1.42013071988495,80.328947368421,5.29999999999999));
#24368=CARTESIAN_POINT('Ctrl Pts',(9.15201909572814E-28,80.5263157894736,
5.3));
#24369=CARTESIAN_POINT('Ctrl Pts',(-1.42013071988495,80.7236842105263,5.29999999999998));
#24370=CARTESIAN_POINT('Ctrl Pts',(-2.65,80.9210526315789,4.58993464005751));
#24371=CARTESIAN_POINT('Ctrl Pts',(-3.87986928011504,81.1184210526315,3.87986928011504));
#24372=CARTESIAN_POINT('Ctrl Pts',(-4.58993464005751,81.3157894736842,2.64999999999999));
#24373=CARTESIAN_POINT('Ctrl Pts',(-5.29999999999999,81.5131578947368,1.42013071988495));
#24374=CARTESIAN_POINT('Ctrl Pts',(-5.29999999999999,81.7105263157895,3.24531401775207E-16));
#24375=CARTESIAN_POINT('Ctrl Pts',(-5.29999999999999,81.9078947368421,-1.42013071988495));
#24376=CARTESIAN_POINT('Ctrl Pts',(-4.58993464005751,82.1052631578947,-2.64999999999999));
#24377=CARTESIAN_POINT('Ctrl Pts',(-3.87986928011504,82.3026315789473,-3.87986928011504));
#24378=CARTESIAN_POINT('Ctrl Pts',(-2.65,82.5,-4.58993464005751));
#24379=CARTESIAN_POINT('Ctrl Pts',(-1.42013071988495,82.6973684210527,-5.29999999999999));
#24380=CARTESIAN_POINT('Ctrl Pts',(-6.49062803547219E-16,82.8947368421053,
-5.29999999999999));
#24381=CARTESIAN_POINT('Ctrl Pts',(1.42013071988495,83.0921052631579,-5.29999999999999));
#24382=CARTESIAN_POINT('Ctrl Pts',(2.64999999999999,83.2894736842105,-4.58993464005751));
#24383=CARTESIAN_POINT('Ctrl Pts',(3.87986928011504,83.4868421052631,-3.87986928011505));
#24384=CARTESIAN_POINT('Ctrl Pts',(4.58993464005751,83.6842105263158,-2.65));
#24385=CARTESIAN_POINT('Ctrl Pts',(5.29999999999999,83.8815789473684,-1.42013071988495));
#24386=CARTESIAN_POINT('Ctrl Pts',(5.29999999999999,84.078947368421,-9.73594205321184E-16));
#24387=CARTESIAN_POINT('Ctrl Pts',(5.29999999999999,84.2763157894736,1.42013071988495));
#24388=CARTESIAN_POINT('Ctrl Pts',(4.58993464005752,84.4736842105263,2.64999999999999));
#24389=CARTESIAN_POINT('Ctrl Pts',(3.87986928011505,84.6710526315789,3.87986928011504));
#24390=CARTESIAN_POINT('Ctrl Pts',(2.65,84.8684210526316,4.58993464005751));
#24391=CARTESIAN_POINT('Ctrl Pts',(1.42013071988495,85.0657894736842,5.29999999999998));
#24392=CARTESIAN_POINT('Ctrl Pts',(9.61424228238108E-28,85.2631578947368,
5.3));
#24393=CARTESIAN_POINT('Ctrl Pts',(-1.42013071988495,85.4605263157894,5.29999999999999));
#24394=CARTESIAN_POINT('Ctrl Pts',(-2.65,85.6578947368421,4.58993464005751));
#24395=CARTESIAN_POINT('Ctrl Pts',(-3.87986928011504,85.8552631578947,3.87986928011504));
#24396=CARTESIAN_POINT('Ctrl Pts',(-4.58993464005751,86.0526315789474,2.65));
#24397=CARTESIAN_POINT('Ctrl Pts',(-5.29999999999999,86.25,1.42013071988495));
#24398=CARTESIAN_POINT('Ctrl Pts',(-5.29999999999999,86.4473684210526,3.24531401775207E-16));
#24399=CARTESIAN_POINT('Ctrl Pts',(-5.29999999999999,86.6447368421052,-1.42013071988495));
#24400=CARTESIAN_POINT('Ctrl Pts',(-4.58993464005751,86.8421052631579,-2.64999999999999));
#24401=CARTESIAN_POINT('Ctrl Pts',(-3.87986928011504,87.0394736842105,-3.87986928011504));
#24402=CARTESIAN_POINT('Ctrl Pts',(-2.65,87.2368421052631,-4.58993464005751));
#24403=CARTESIAN_POINT('Ctrl Pts',(-1.42013071988495,87.4342105263158,-5.29999999999999));
#24404=CARTESIAN_POINT('Ctrl Pts',(-6.49062803547173E-16,87.6315789473684,
-5.29999999999999));
#24405=CARTESIAN_POINT('Ctrl Pts',(1.42013071988495,87.828947368421,-5.29999999999999));
#24406=CARTESIAN_POINT('Ctrl Pts',(2.64999999999999,88.0263157894737,-4.58993464005751));
#24407=CARTESIAN_POINT('Ctrl Pts',(3.87986928011504,88.2236842105263,-3.87986928011505));
#24408=CARTESIAN_POINT('Ctrl Pts',(4.58993464005751,88.4210526315789,-2.65));
#24409=CARTESIAN_POINT('Ctrl Pts',(5.29999999999999,88.6184210526316,-1.42013071988495));
#24410=CARTESIAN_POINT('Ctrl Pts',(5.29999999999999,88.8157894736842,-9.73594205321085E-16));
#24411=CARTESIAN_POINT('Ctrl Pts',(5.29999999999999,89.0131578947368,1.42013071988495));
#24412=CARTESIAN_POINT('Ctrl Pts',(4.58993464005752,89.2105263157895,2.64999999999999));
#24413=CARTESIAN_POINT('Ctrl Pts',(3.87986928011505,89.4078947368421,3.87986928011504));
#24414=CARTESIAN_POINT('Ctrl Pts',(2.65,89.6052631578947,4.58993464005751));
#24415=CARTESIAN_POINT('Ctrl Pts',(1.42013071988495,89.8026315789473,5.29999999999999));
#24416=CARTESIAN_POINT('Ctrl Pts',(1.01689101063646E-27,89.9999999999999,
5.3));
#24417=CARTESIAN_POINT('Ctrl Pts',(6.93334779979405E-29,4.00000000000002,
5.29999999999999));
#24418=CARTESIAN_POINT('Ctrl Pts',(-1.42013071988495,4.19736842105264,5.29999999999999));
#24419=CARTESIAN_POINT('Ctrl Pts',(-2.65,4.3947368421053,4.58993464005751));
#24420=CARTESIAN_POINT('Ctrl Pts',(-3.87986928011504,4.5921052631579,3.87986928011504));
#24421=CARTESIAN_POINT('Ctrl Pts',(-4.58993464005752,4.78947368421054,2.65));
#24422=CARTESIAN_POINT('Ctrl Pts',(-5.29999999999999,4.98684210526316,1.42013071988495));
#24423=CARTESIAN_POINT('Ctrl Pts',(-5.29999999999999,5.18421052631578,3.24531401773092E-16));
#24424=CARTESIAN_POINT('Ctrl Pts',(-5.29999999999999,5.38157894736842,-1.42013071988495));
#24425=CARTESIAN_POINT('Ctrl Pts',(-4.58993464005752,5.57894736842106,-2.65));
#24426=CARTESIAN_POINT('Ctrl Pts',(-3.87986928011504,5.77631578947368,-3.87986928011504));
#24427=CARTESIAN_POINT('Ctrl Pts',(-2.65,5.9736842105263,-4.58993464005752));
#24428=CARTESIAN_POINT('Ctrl Pts',(-1.42013071988495,6.17105263157895,-5.29999999999999));
#24429=CARTESIAN_POINT('Ctrl Pts',(-6.49062803548048E-16,6.36842105263158,
-5.29999999999999));
#24430=CARTESIAN_POINT('Ctrl Pts',(1.42013071988495,6.56578947368421,-5.29999999999999));
#24431=CARTESIAN_POINT('Ctrl Pts',(2.65,6.76315789473682,-4.58993464005752));
#24432=CARTESIAN_POINT('Ctrl Pts',(3.87986928011504,6.96052631578947,-3.87986928011504));
#24433=CARTESIAN_POINT('Ctrl Pts',(4.58993464005752,7.1578947368421,-2.65));
#24434=CARTESIAN_POINT('Ctrl Pts',(5.29999999999999,7.35526315789473,-1.42013071988495));
#24435=CARTESIAN_POINT('Ctrl Pts',(5.29999999999999,7.55263157894738,-9.73594205321327E-16));
#24436=CARTESIAN_POINT('Ctrl Pts',(5.29999999999999,7.75,1.42013071988495));
#24437=CARTESIAN_POINT('Ctrl Pts',(4.58993464005752,7.94736842105266,2.64999999999999));
#24438=CARTESIAN_POINT('Ctrl Pts',(3.87986928011504,8.14473684210526,3.87986928011504));
#24439=CARTESIAN_POINT('Ctrl Pts',(2.65,8.3421052631579,4.58993464005751));
#24440=CARTESIAN_POINT('Ctrl Pts',(1.42013071988495,8.53947368421056,5.29999999999999));
#24441=CARTESIAN_POINT('Ctrl Pts',(1.24800260396293E-28,8.73684210526318,
5.29999999999999));
#24442=CARTESIAN_POINT('Ctrl Pts',(-1.42013071988495,8.93421052631582,5.29999999999999));
#24443=CARTESIAN_POINT('Ctrl Pts',(-2.65,9.13157894736842,4.58993464005752));
#24444=CARTESIAN_POINT('Ctrl Pts',(-3.87986928011504,9.32894736842109,3.87986928011504));
#24445=CARTESIAN_POINT('Ctrl Pts',(-4.58993464005752,9.5263157894737,2.65));
#24446=CARTESIAN_POINT('Ctrl Pts',(-5.29999999999999,9.7236842105263,1.42013071988495));
#24447=CARTESIAN_POINT('Ctrl Pts',(-5.29999999999999,9.92105263157894,3.24531401773092E-16));
#24448=CARTESIAN_POINT('Ctrl Pts',(-5.29999999999999,10.1184210526316,-1.42013071988495));
#24449=CARTESIAN_POINT('Ctrl Pts',(-4.58993464005752,10.3157894736842,-2.65));
#24450=CARTESIAN_POINT('Ctrl Pts',(-3.87986928011504,10.5131578947368,-3.87986928011504));
#24451=CARTESIAN_POINT('Ctrl Pts',(-2.65,10.7105263157895,-4.58993464005752));
#24452=CARTESIAN_POINT('Ctrl Pts',(-1.42013071988495,10.9078947368421,-5.29999999999999));
#24453=CARTESIAN_POINT('Ctrl Pts',(-6.49062803548001E-16,11.1052631578947,
-5.3));
#24454=CARTESIAN_POINT('Ctrl Pts',(1.42013071988495,11.3026315789474,-5.29999999999999));
#24455=CARTESIAN_POINT('Ctrl Pts',(2.65,11.5,-4.58993464005752));
#24456=CARTESIAN_POINT('Ctrl Pts',(3.87986928011504,11.6973684210526,-3.87986928011504));
#24457=CARTESIAN_POINT('Ctrl Pts',(4.58993464005752,11.8947368421053,-2.65));
#24458=CARTESIAN_POINT('Ctrl Pts',(5.29999999999999,12.0921052631579,-1.42013071988495));
#24459=CARTESIAN_POINT('Ctrl Pts',(5.29999999999999,12.2894736842105,-9.73594205321327E-16));
#24460=CARTESIAN_POINT('Ctrl Pts',(5.29999999999999,12.4868421052632,1.42013071988495));
#24461=CARTESIAN_POINT('Ctrl Pts',(4.58993464005752,12.6842105263158,2.64999999999999));
#24462=CARTESIAN_POINT('Ctrl Pts',(3.87986928011504,12.8815789473684,3.87986928011504));
#24463=CARTESIAN_POINT('Ctrl Pts',(2.65,13.0789473684211,4.58993464005752));
#24464=CARTESIAN_POINT('Ctrl Pts',(1.42013071988495,13.2763157894737,5.29999999999999));
#24465=CARTESIAN_POINT('Ctrl Pts',(1.80267042794645E-28,13.4736842105263,
5.29999999999999));
#24466=CARTESIAN_POINT('Ctrl Pts',(-1.42013071988495,13.671052631579,5.29999999999999));
#24467=CARTESIAN_POINT('Ctrl Pts',(-2.65,13.8684210526316,4.58993464005752));
#24468=CARTESIAN_POINT('Ctrl Pts',(-3.87986928011504,14.0657894736842,3.87986928011504));
#24469=CARTESIAN_POINT('Ctrl Pts',(-4.58993464005752,14.2631578947369,2.65));
#24470=CARTESIAN_POINT('Ctrl Pts',(-5.29999999999999,14.4605263157895,1.42013071988495));
#24471=CARTESIAN_POINT('Ctrl Pts',(-5.29999999999999,14.6578947368421,3.2453140177324E-16));
#24472=CARTESIAN_POINT('Ctrl Pts',(-5.29999999999999,14.8552631578947,-1.42013071988495));
#24473=CARTESIAN_POINT('Ctrl Pts',(-4.58993464005752,15.0526315789473,-2.64999999999999));
#24474=CARTESIAN_POINT('Ctrl Pts',(-3.87986928011504,15.25,-3.87986928011504));
#24475=CARTESIAN_POINT('Ctrl Pts',(-2.65,15.4473684210526,-4.58993464005752));
#24476=CARTESIAN_POINT('Ctrl Pts',(-1.42013071988495,15.6447368421052,-5.29999999999999));
#24477=CARTESIAN_POINT('Ctrl Pts',(-6.49062803547951E-16,15.8421052631579,
-5.29999999999999));
#24478=CARTESIAN_POINT('Ctrl Pts',(1.42013071988495,16.0394736842105,-5.29999999999999));
#24479=CARTESIAN_POINT('Ctrl Pts',(2.65,16.2368421052631,-4.58993464005752));
#24480=CARTESIAN_POINT('Ctrl Pts',(3.87986928011504,16.4342105263158,-3.87986928011504));
#24481=CARTESIAN_POINT('Ctrl Pts',(4.58993464005752,16.6315789473684,-2.65));
#24482=CARTESIAN_POINT('Ctrl Pts',(5.29999999999999,16.8289473684211,-1.42013071988495));
#24483=CARTESIAN_POINT('Ctrl Pts',(5.29999999999999,17.0263157894737,-9.73594205321327E-16));
#24484=CARTESIAN_POINT('Ctrl Pts',(5.29999999999999,17.2236842105263,1.42013071988494));
#24485=CARTESIAN_POINT('Ctrl Pts',(4.58993464005752,17.4210526315789,2.64999999999999));
#24486=CARTESIAN_POINT('Ctrl Pts',(3.87986928011504,17.6184210526316,3.87986928011504));
#24487=CARTESIAN_POINT('Ctrl Pts',(2.65,17.8157894736842,4.58993464005751));
#24488=CARTESIAN_POINT('Ctrl Pts',(1.42013071988495,18.0131578947369,5.29999999999999));
#24489=CARTESIAN_POINT('Ctrl Pts',(2.28800477393204E-28,18.2105263157895,
5.29999999999999));
#24490=CARTESIAN_POINT('Ctrl Pts',(-1.42013071988495,18.4078947368421,5.29999999999999));
#24491=CARTESIAN_POINT('Ctrl Pts',(-2.65,18.6052631578947,4.58993464005751));
#24492=CARTESIAN_POINT('Ctrl Pts',(-3.87986928011504,18.8026315789474,3.87986928011505));
#24493=CARTESIAN_POINT('Ctrl Pts',(-4.58993464005752,19.,2.65));
#24494=CARTESIAN_POINT('Ctrl Pts',(-5.29999999999999,19.1973684210526,1.42013071988495));
#24495=CARTESIAN_POINT('Ctrl Pts',(-5.29999999999999,19.3947368421053,3.2453140177324E-16));
#24496=CARTESIAN_POINT('Ctrl Pts',(-5.29999999999999,19.5921052631579,-1.42013071988495));
#24497=CARTESIAN_POINT('Ctrl Pts',(-4.58993464005752,19.7894736842105,-2.64999999999999));
#24498=CARTESIAN_POINT('Ctrl Pts',(-3.87986928011504,19.9868421052632,-3.87986928011504));
#24499=CARTESIAN_POINT('Ctrl Pts',(-2.65,20.1842105263158,-4.58993464005752));
#24500=CARTESIAN_POINT('Ctrl Pts',(-1.42013071988495,20.3815789473684,-5.29999999999999));
#24501=CARTESIAN_POINT('Ctrl Pts',(-6.49062803547903E-16,20.578947368421,
-5.29999999999999));
#24502=CARTESIAN_POINT('Ctrl Pts',(1.42013071988495,20.7763157894736,-5.29999999999999));
#24503=CARTESIAN_POINT('Ctrl Pts',(2.65,20.9736842105263,-4.58993464005752));
#24504=CARTESIAN_POINT('Ctrl Pts',(3.87986928011504,21.171052631579,-3.87986928011504));
#24505=CARTESIAN_POINT('Ctrl Pts',(4.58993464005752,21.3684210526315,-2.65));
#24506=CARTESIAN_POINT('Ctrl Pts',(5.29999999999999,21.5657894736842,-1.42013071988495));
#24507=CARTESIAN_POINT('Ctrl Pts',(5.29999999999999,21.7631578947368,-9.73594205321327E-16));
#24508=CARTESIAN_POINT('Ctrl Pts',(5.29999999999999,21.9605263157895,1.42013071988495));
#24509=CARTESIAN_POINT('Ctrl Pts',(4.58993464005752,22.1578947368421,2.64999999999999));
#24510=CARTESIAN_POINT('Ctrl Pts',(3.87986928011504,22.3552631578947,3.87986928011504));
#24511=CARTESIAN_POINT('Ctrl Pts',(2.65,22.5526315789474,4.58993464005752));
#24512=CARTESIAN_POINT('Ctrl Pts',(1.42013071988495,22.75,5.29999999999999));
#24513=CARTESIAN_POINT('Ctrl Pts',(2.77333911991762E-28,22.9473684210526,
5.29999999999999));
#24514=CARTESIAN_POINT('Ctrl Pts',(-1.42013071988495,23.1447368421053,5.29999999999999));
#24515=CARTESIAN_POINT('Ctrl Pts',(-2.65,23.3421052631579,4.58993464005752));
#24516=CARTESIAN_POINT('Ctrl Pts',(-3.87986928011504,23.5394736842105,3.87986928011504));
#24517=CARTESIAN_POINT('Ctrl Pts',(-4.58993464005752,23.7368421052632,2.65));
#24518=CARTESIAN_POINT('Ctrl Pts',(-5.29999999999999,23.9342105263158,1.42013071988495));
#24519=CARTESIAN_POINT('Ctrl Pts',(-5.29999999999999,24.1315789473684,3.2453140177324E-16));
#24520=CARTESIAN_POINT('Ctrl Pts',(-5.29999999999999,24.328947368421,-1.42013071988495));
#24521=CARTESIAN_POINT('Ctrl Pts',(-4.58993464005752,24.5263157894737,-2.65));
#24522=CARTESIAN_POINT('Ctrl Pts',(-3.87986928011504,24.7236842105263,-3.87986928011504));
#24523=CARTESIAN_POINT('Ctrl Pts',(-2.65,24.9210526315789,-4.58993464005752));
#24524=CARTESIAN_POINT('Ctrl Pts',(-1.42013071988495,25.1184210526316,-5.29999999999999));
#24525=CARTESIAN_POINT('Ctrl Pts',(-6.49062803547847E-16,25.3157894736842,
-5.3));
#24526=CARTESIAN_POINT('Ctrl Pts',(1.42013071988495,25.5131578947368,-5.29999999999999));
#24527=CARTESIAN_POINT('Ctrl Pts',(2.65,25.7105263157895,-4.58993464005752));
#24528=CARTESIAN_POINT('Ctrl Pts',(3.87986928011504,25.9078947368421,-3.87986928011504));
#24529=CARTESIAN_POINT('Ctrl Pts',(4.58993464005752,26.1052631578947,-2.65));
#24530=CARTESIAN_POINT('Ctrl Pts',(5.29999999999999,26.3026315789474,-1.42013071988495));
#24531=CARTESIAN_POINT('Ctrl Pts',(5.29999999999999,26.5,-9.73594205321327E-16));
#24532=CARTESIAN_POINT('Ctrl Pts',(5.29999999999999,26.6973684210526,1.42013071988495));
#24533=CARTESIAN_POINT('Ctrl Pts',(4.58993464005752,26.8947368421053,2.64999999999999));
#24534=CARTESIAN_POINT('Ctrl Pts',(3.87986928011504,27.0921052631579,3.87986928011504));
#24535=CARTESIAN_POINT('Ctrl Pts',(2.65,27.2894736842106,4.58993464005751));
#24536=CARTESIAN_POINT('Ctrl Pts',(1.42013071988495,27.4868421052632,5.29999999999999));
#24537=CARTESIAN_POINT('Ctrl Pts',(3.33956252356747E-28,27.6842105263158,
5.29999999999999));
#24538=CARTESIAN_POINT('Ctrl Pts',(-1.42013071988495,27.8815789473684,5.29999999999999));
#24539=CARTESIAN_POINT('Ctrl Pts',(-2.65,28.0789473684211,4.58993464005751));
#24540=CARTESIAN_POINT('Ctrl Pts',(-3.87986928011504,28.2763157894737,3.87986928011504));
#24541=CARTESIAN_POINT('Ctrl Pts',(-4.58993464005752,28.4736842105263,2.65));
#24542=CARTESIAN_POINT('Ctrl Pts',(-5.29999999999999,28.671052631579,1.42013071988495));
#24543=CARTESIAN_POINT('Ctrl Pts',(-5.29999999999999,28.8684210526316,3.24531401773092E-16));
#24544=CARTESIAN_POINT('Ctrl Pts',(-5.29999999999999,29.0657894736842,-1.42013071988495));
#24545=CARTESIAN_POINT('Ctrl Pts',(-4.58993464005752,29.2631578947368,-2.65));
#24546=CARTESIAN_POINT('Ctrl Pts',(-3.87986928011504,29.4605263157895,-3.87986928011504));
#24547=CARTESIAN_POINT('Ctrl Pts',(-2.65,29.6578947368421,-4.58993464005752));
#24548=CARTESIAN_POINT('Ctrl Pts',(-1.42013071988495,29.8552631578947,-5.29999999999999));
#24549=CARTESIAN_POINT('Ctrl Pts',(-6.49062803547792E-16,30.0526315789473,
-5.29999999999999));
#24550=CARTESIAN_POINT('Ctrl Pts',(1.42013071988495,30.25,-5.29999999999999));
#24551=CARTESIAN_POINT('Ctrl Pts',(2.65,30.4473684210526,-4.58993464005752));
#24552=CARTESIAN_POINT('Ctrl Pts',(3.87986928011504,30.6447368421052,-3.87986928011504));
#24553=CARTESIAN_POINT('Ctrl Pts',(4.58993464005752,30.8421052631579,-2.65));
#24554=CARTESIAN_POINT('Ctrl Pts',(5.29999999999999,31.0394736842105,-1.42013071988495));
#24555=CARTESIAN_POINT('Ctrl Pts',(5.29999999999999,31.2368421052632,-9.73594205321327E-16));
#24556=CARTESIAN_POINT('Ctrl Pts',(5.29999999999999,31.4342105263158,1.42013071988495));
#24557=CARTESIAN_POINT('Ctrl Pts',(4.58993464005752,31.6315789473684,2.64999999999999));
#24558=CARTESIAN_POINT('Ctrl Pts',(3.87986928011504,31.8289473684211,3.87986928011504));
#24559=CARTESIAN_POINT('Ctrl Pts',(2.65,32.0263157894737,4.58993464005751));
#24560=CARTESIAN_POINT('Ctrl Pts',(1.42013071988495,32.2236842105263,5.29999999999999));
#24561=CARTESIAN_POINT('Ctrl Pts',(3.87111918821834E-28,32.421052631579,
5.29999999999999));
#24562=CARTESIAN_POINT('Ctrl Pts',(-1.42013071988495,32.6184210526316,5.29999999999999));
#24563=CARTESIAN_POINT('Ctrl Pts',(-2.65,32.8157894736842,4.58993464005752));
#24564=CARTESIAN_POINT('Ctrl Pts',(-3.87986928011504,33.0131578947369,3.87986928011504));
#24565=CARTESIAN_POINT('Ctrl Pts',(-4.58993464005752,33.2105263157895,2.65));
#24566=CARTESIAN_POINT('Ctrl Pts',(-5.29999999999999,33.4078947368421,1.42013071988495));
#24567=CARTESIAN_POINT('Ctrl Pts',(-5.29999999999999,33.6052631578947,3.24531401773092E-16));
#24568=CARTESIAN_POINT('Ctrl Pts',(-5.29999999999999,33.8026315789473,-1.42013071988495));
#24569=CARTESIAN_POINT('Ctrl Pts',(-4.58993464005752,34.,-2.65));
#24570=CARTESIAN_POINT('Ctrl Pts',(-3.87986928011504,34.1973684210526,-3.87986928011504));
#24571=CARTESIAN_POINT('Ctrl Pts',(-2.65,34.3947368421052,-4.58993464005752));
#24572=CARTESIAN_POINT('Ctrl Pts',(-1.42013071988495,34.5921052631579,-5.29999999999999));
#24573=CARTESIAN_POINT('Ctrl Pts',(-6.49062803547743E-16,34.7894736842105,
-5.3));
#24574=CARTESIAN_POINT('Ctrl Pts',(1.42013071988495,34.9868421052631,-5.29999999999999));
#24575=CARTESIAN_POINT('Ctrl Pts',(2.65,35.1842105263157,-4.58993464005752));
#24576=CARTESIAN_POINT('Ctrl Pts',(3.87986928011504,35.3815789473684,-3.87986928011505));
#24577=CARTESIAN_POINT('Ctrl Pts',(4.58993464005752,35.578947368421,-2.65));
#24578=CARTESIAN_POINT('Ctrl Pts',(5.29999999999999,35.7763157894737,-1.42013071988495));
#24579=CARTESIAN_POINT('Ctrl Pts',(5.29999999999999,35.9736842105263,-9.73594205321179E-16));
#24580=CARTESIAN_POINT('Ctrl Pts',(5.29999999999999,36.171052631579,1.42013071988494));
#24581=CARTESIAN_POINT('Ctrl Pts',(4.58993464005752,36.3684210526316,2.64999999999999));
#24582=CARTESIAN_POINT('Ctrl Pts',(3.87986928011504,36.5657894736842,3.87986928011504));
#24583=CARTESIAN_POINT('Ctrl Pts',(2.65,36.7631578947368,4.58993464005752));
#24584=CARTESIAN_POINT('Ctrl Pts',(1.42013071988495,36.9605263157895,5.29999999999999));
#24585=CARTESIAN_POINT('Ctrl Pts',(4.36800911387025E-28,37.1578947368421,
5.29999999999999));
#24586=CARTESIAN_POINT('Ctrl Pts',(-1.42013071988495,37.3552631578947,5.29999999999999));
#24587=CARTESIAN_POINT('Ctrl Pts',(-2.65,37.5526315789474,4.58993464005752));
#24588=CARTESIAN_POINT('Ctrl Pts',(-3.87986928011504,37.75,3.87986928011504));
#24589=CARTESIAN_POINT('Ctrl Pts',(-4.58993464005752,37.9473684210526,2.65));
#24590=CARTESIAN_POINT('Ctrl Pts',(-5.29999999999999,38.1447368421053,1.42013071988495));
#24591=CARTESIAN_POINT('Ctrl Pts',(-5.29999999999999,38.3421052631579,3.2453140177324E-16));
#24592=CARTESIAN_POINT('Ctrl Pts',(-5.29999999999999,38.5394736842105,-1.42013071988495));
#24593=CARTESIAN_POINT('Ctrl Pts',(-4.58993464005752,38.7368421052632,-2.65));
#24594=CARTESIAN_POINT('Ctrl Pts',(-3.87986928011504,38.9342105263158,-3.87986928011504));
#24595=CARTESIAN_POINT('Ctrl Pts',(-2.65,39.1315789473684,-4.58993464005752));
#24596=CARTESIAN_POINT('Ctrl Pts',(-1.42013071988495,39.328947368421,-5.29999999999999));
#24597=CARTESIAN_POINT('Ctrl Pts',(-6.49062803547689E-16,39.5263157894736,
-5.29999999999999));
#24598=CARTESIAN_POINT('Ctrl Pts',(1.42013071988495,39.7236842105263,-5.29999999999999));
#24599=CARTESIAN_POINT('Ctrl Pts',(2.65,39.9210526315789,-4.58993464005752));
#24600=CARTESIAN_POINT('Ctrl Pts',(3.87986928011504,40.1184210526316,-3.87986928011504));
#24601=CARTESIAN_POINT('Ctrl Pts',(4.58993464005752,40.3157894736842,-2.65));
#24602=CARTESIAN_POINT('Ctrl Pts',(5.29999999999999,40.5131578947368,-1.42013071988495));
#24603=CARTESIAN_POINT('Ctrl Pts',(5.29999999999999,40.7105263157895,-9.73594205321179E-16));
#24604=CARTESIAN_POINT('Ctrl Pts',(5.29999999999999,40.9078947368421,1.42013071988495));
#24605=CARTESIAN_POINT('Ctrl Pts',(4.58993464005752,41.1052631578947,2.64999999999999));
#24606=CARTESIAN_POINT('Ctrl Pts',(3.87986928011504,41.3026315789474,3.87986928011504));
#24607=CARTESIAN_POINT('Ctrl Pts',(2.65,41.5,4.58993464005751));
#24608=CARTESIAN_POINT('Ctrl Pts',(1.42013071988495,41.6973684210527,5.29999999999999));
#24609=CARTESIAN_POINT('Ctrl Pts',(4.92267693785377E-28,41.8947368421053,
5.29999999999999));
#24610=CARTESIAN_POINT('Ctrl Pts',(-1.42013071988495,42.0921052631579,5.29999999999999));
#24611=CARTESIAN_POINT('Ctrl Pts',(-2.65,42.2894736842105,4.58993464005752));
#24612=CARTESIAN_POINT('Ctrl Pts',(-3.87986928011504,42.4868421052632,3.87986928011504));
#24613=CARTESIAN_POINT('Ctrl Pts',(-4.58993464005752,42.6842105263158,2.65));
#24614=CARTESIAN_POINT('Ctrl Pts',(-5.29999999999999,42.8815789473684,1.42013071988495));
#24615=CARTESIAN_POINT('Ctrl Pts',(-5.29999999999999,43.078947368421,3.2453140177324E-16));
#24616=CARTESIAN_POINT('Ctrl Pts',(-5.29999999999999,43.2763157894737,-1.42013071988495));
#24617=CARTESIAN_POINT('Ctrl Pts',(-4.58993464005752,43.4736842105263,-2.64999999999999));
#24618=CARTESIAN_POINT('Ctrl Pts',(-3.87986928011504,43.6710526315789,-3.87986928011504));
#24619=CARTESIAN_POINT('Ctrl Pts',(-2.65,43.8684210526316,-4.58993464005752));
#24620=CARTESIAN_POINT('Ctrl Pts',(-1.42013071988495,44.0657894736842,-5.29999999999999));
#24621=CARTESIAN_POINT('Ctrl Pts',(-6.4906280354764E-16,44.2631578947368,
-5.3));
#24622=CARTESIAN_POINT('Ctrl Pts',(1.42013071988495,44.4605263157895,-5.29999999999999));
#24623=CARTESIAN_POINT('Ctrl Pts',(2.65,44.6578947368421,-4.58993464005752));
#24624=CARTESIAN_POINT('Ctrl Pts',(3.87986928011504,44.8552631578947,-3.87986928011504));
#24625=CARTESIAN_POINT('Ctrl Pts',(4.58993464005752,45.0526315789473,-2.65));
#24626=CARTESIAN_POINT('Ctrl Pts',(5.29999999999999,45.25,-1.42013071988495));
#24627=CARTESIAN_POINT('Ctrl Pts',(5.29999999999999,45.4473684210526,-9.73594205321327E-16));
#24628=CARTESIAN_POINT('Ctrl Pts',(5.29999999999999,45.6447368421053,1.42013071988495));
#24629=CARTESIAN_POINT('Ctrl Pts',(4.58993464005752,45.8421052631579,2.64999999999999));
#24630=CARTESIAN_POINT('Ctrl Pts',(3.87986928011504,46.0394736842105,3.87986928011504));
#24631=CARTESIAN_POINT('Ctrl Pts',(2.65,46.2368421052632,4.58993464005752));
#24632=CARTESIAN_POINT('Ctrl Pts',(1.42013071988495,46.4342105263158,5.29999999999999));
#24633=CARTESIAN_POINT('Ctrl Pts',(5.40801128383936E-28,46.6315789473685,
5.29999999999999));
#24634=CARTESIAN_POINT('Ctrl Pts',(-1.42013071988495,46.8289473684211,5.29999999999999));
#24635=CARTESIAN_POINT('Ctrl Pts',(-2.65,47.0263157894737,4.58993464005752));
#24636=CARTESIAN_POINT('Ctrl Pts',(-3.87986928011504,47.2236842105263,3.87986928011504));
#24637=CARTESIAN_POINT('Ctrl Pts',(-4.58993464005752,47.421052631579,2.65));
#24638=CARTESIAN_POINT('Ctrl Pts',(-5.29999999999999,47.6184210526316,1.42013071988495));
#24639=CARTESIAN_POINT('Ctrl Pts',(-5.29999999999999,47.8157894736842,3.2453140177324E-16));
#24640=CARTESIAN_POINT('Ctrl Pts',(-5.29999999999999,48.0131578947369,-1.42013071988495));
#24641=CARTESIAN_POINT('Ctrl Pts',(-4.58993464005752,48.2105263157895,-2.64999999999999));
#24642=CARTESIAN_POINT('Ctrl Pts',(-3.87986928011504,48.4078947368421,-3.87986928011504));
#24643=CARTESIAN_POINT('Ctrl Pts',(-2.65,48.6052631578947,-4.58993464005752));
#24644=CARTESIAN_POINT('Ctrl Pts',(-1.42013071988495,48.8026315789473,-5.29999999999999));
#24645=CARTESIAN_POINT('Ctrl Pts',(-6.49062803547591E-16,49.,-5.29999999999999));
#24646=CARTESIAN_POINT('Ctrl Pts',(1.42013071988495,49.1973684210526,-5.29999999999999));
#24647=CARTESIAN_POINT('Ctrl Pts',(2.65,49.3947368421053,-4.58993464005752));
#24648=CARTESIAN_POINT('Ctrl Pts',(3.87986928011504,49.5921052631579,-3.87986928011504));
#24649=CARTESIAN_POINT('Ctrl Pts',(4.58993464005752,49.7894736842105,-2.65));
#24650=CARTESIAN_POINT('Ctrl Pts',(5.29999999999999,49.9868421052632,-1.42013071988495));
#24651=CARTESIAN_POINT('Ctrl Pts',(5.29999999999999,50.1842105263158,-9.73594205321327E-16));
#24652=CARTESIAN_POINT('Ctrl Pts',(5.29999999999999,50.3815789473684,1.42013071988495));
#24653=CARTESIAN_POINT('Ctrl Pts',(4.58993464005752,50.5789473684211,2.64999999999999));
#24654=CARTESIAN_POINT('Ctrl Pts',(3.87986928011504,50.7763157894737,3.87986928011504));
#24655=CARTESIAN_POINT('Ctrl Pts',(2.65,50.9736842105264,4.58993464005751));
#24656=CARTESIAN_POINT('Ctrl Pts',(1.42013071988495,51.171052631579,5.29999999999999));
#24657=CARTESIAN_POINT('Ctrl Pts',(5.90490120949126E-28,51.3684210526317,
5.29999999999999));
#24658=CARTESIAN_POINT('Ctrl Pts',(-1.42013071988495,51.5657894736843,5.29999999999999));
#24659=CARTESIAN_POINT('Ctrl Pts',(-2.65,51.7631578947368,4.58993464005751));
#24660=CARTESIAN_POINT('Ctrl Pts',(-3.87986928011504,51.9605263157895,3.87986928011504));
#24661=CARTESIAN_POINT('Ctrl Pts',(-4.58993464005752,52.1578947368421,2.65));
#24662=CARTESIAN_POINT('Ctrl Pts',(-5.29999999999999,52.3552631578947,1.42013071988495));
#24663=CARTESIAN_POINT('Ctrl Pts',(-5.29999999999999,52.5526315789474,3.24531401773979E-16));
#24664=CARTESIAN_POINT('Ctrl Pts',(-5.29999999999999,52.75,-1.42013071988495));
#24665=CARTESIAN_POINT('Ctrl Pts',(-4.58993464005752,52.9473684210526,-2.65));
#24666=CARTESIAN_POINT('Ctrl Pts',(-3.87986928011504,53.1447368421053,-3.87986928011504));
#24667=CARTESIAN_POINT('Ctrl Pts',(-2.65,53.3421052631578,-4.58993464005752));
#24668=CARTESIAN_POINT('Ctrl Pts',(-1.42013071988495,53.5394736842104,-5.29999999999999));
#24669=CARTESIAN_POINT('Ctrl Pts',(-6.49062803547537E-16,53.7368421052631,
-5.29999999999999));
#24670=CARTESIAN_POINT('Ctrl Pts',(1.42013071988495,53.9342105263157,-5.29999999999999));
#24671=CARTESIAN_POINT('Ctrl Pts',(2.65,54.1315789473684,-4.58993464005752));
#24672=CARTESIAN_POINT('Ctrl Pts',(3.87986928011504,54.3289473684211,-3.87986928011504));
#24673=CARTESIAN_POINT('Ctrl Pts',(4.58993464005752,54.5263157894736,-2.65));
#24674=CARTESIAN_POINT('Ctrl Pts',(5.29999999999999,54.7236842105263,-1.42013071988495));
#24675=CARTESIAN_POINT('Ctrl Pts',(5.29999999999999,54.9210526315789,-9.73594205321327E-16));
#24676=CARTESIAN_POINT('Ctrl Pts',(5.29999999999999,55.1184210526316,1.42013071988495));
#24677=CARTESIAN_POINT('Ctrl Pts',(4.58993464005752,55.3157894736842,2.64999999999999));
#24678=CARTESIAN_POINT('Ctrl Pts',(3.87986928011504,55.5131578947368,3.87986928011504));
#24679=CARTESIAN_POINT('Ctrl Pts',(2.65,55.7105263157895,4.58993464005752));
#24680=CARTESIAN_POINT('Ctrl Pts',(1.42013071988495,55.9078947368422,5.29999999999999));
#24681=CARTESIAN_POINT('Ctrl Pts',(6.44801345380847E-28,56.1052631578948,
5.29999999999999));
#24682=CARTESIAN_POINT('Ctrl Pts',(-1.42013071988495,56.3026315789474,5.29999999999999));
#24683=CARTESIAN_POINT('Ctrl Pts',(-2.65,56.5000000000001,4.58993464005752));
#24684=CARTESIAN_POINT('Ctrl Pts',(-3.87986928011504,56.6973684210526,3.87986928011504));
#24685=CARTESIAN_POINT('Ctrl Pts',(-4.58993464005752,56.8947368421053,2.65));
#24686=CARTESIAN_POINT('Ctrl Pts',(-5.29999999999999,57.0921052631579,1.42013071988495));
#24687=CARTESIAN_POINT('Ctrl Pts',(-5.29999999999999,57.2894736842105,3.24531401773979E-16));
#24688=CARTESIAN_POINT('Ctrl Pts',(-5.29999999999999,57.4868421052631,-1.42013071988495));
#24689=CARTESIAN_POINT('Ctrl Pts',(-4.58993464005752,57.6842105263158,-2.65));
#24690=CARTESIAN_POINT('Ctrl Pts',(-3.87986928011504,57.8815789473684,-3.87986928011504));
#24691=CARTESIAN_POINT('Ctrl Pts',(-2.65,58.078947368421,-4.58993464005752));
#24692=CARTESIAN_POINT('Ctrl Pts',(-1.42013071988495,58.2763157894737,-5.29999999999999));
#24693=CARTESIAN_POINT('Ctrl Pts',(-6.49062803547481E-16,58.4736842105263,
-5.3));
#24694=CARTESIAN_POINT('Ctrl Pts',(1.42013071988495,58.6710526315789,-5.29999999999999));
#24695=CARTESIAN_POINT('Ctrl Pts',(2.65,58.8684210526315,-4.58993464005752));
#24696=CARTESIAN_POINT('Ctrl Pts',(3.87986928011504,59.0657894736842,-3.87986928011504));
#24697=CARTESIAN_POINT('Ctrl Pts',(4.58993464005752,59.2631578947368,-2.65));
#24698=CARTESIAN_POINT('Ctrl Pts',(5.29999999999999,59.4605263157895,-1.42013071988495));
#24699=CARTESIAN_POINT('Ctrl Pts',(5.29999999999999,59.6578947368421,-9.73594205321179E-16));
#24700=CARTESIAN_POINT('Ctrl Pts',(5.29999999999999,59.8552631578947,1.42013071988494));
#24701=CARTESIAN_POINT('Ctrl Pts',(4.58993464005752,60.0526315789474,2.64999999999999));
#24702=CARTESIAN_POINT('Ctrl Pts',(3.87986928011504,60.25,3.87986928011504));
#24703=CARTESIAN_POINT('Ctrl Pts',(2.65,60.4473684210527,4.58993464005752));
#24704=CARTESIAN_POINT('Ctrl Pts',(1.42013071988495,60.6447368421053,5.29999999999999));
#24705=CARTESIAN_POINT('Ctrl Pts',(7.00268127779199E-28,60.8421052631579,
5.29999999999999));
#24706=CARTESIAN_POINT('Ctrl Pts',(-1.42013071988495,61.0394736842105,5.29999999999999));
#24707=CARTESIAN_POINT('Ctrl Pts',(-2.65,61.2368421052632,4.58993464005751));
#24708=CARTESIAN_POINT('Ctrl Pts',(-3.87986928011504,61.4342105263158,3.87986928011505));
#24709=CARTESIAN_POINT('Ctrl Pts',(-4.58993464005752,61.6315789473684,2.65));
#24710=CARTESIAN_POINT('Ctrl Pts',(-5.29999999999999,61.828947368421,1.42013071988495));
#24711=CARTESIAN_POINT('Ctrl Pts',(-5.29999999999999,62.0263157894737,3.24531401773831E-16));
#24712=CARTESIAN_POINT('Ctrl Pts',(-5.29999999999999,62.2236842105263,-1.42013071988495));
#24713=CARTESIAN_POINT('Ctrl Pts',(-4.58993464005752,62.4210526315789,-2.65));
#24714=CARTESIAN_POINT('Ctrl Pts',(-3.87986928011504,62.6184210526316,-3.87986928011504));
#24715=CARTESIAN_POINT('Ctrl Pts',(-2.65,62.8157894736841,-4.58993464005752));
#24716=CARTESIAN_POINT('Ctrl Pts',(-1.42013071988495,63.0131578947368,-5.29999999999999));
#24717=CARTESIAN_POINT('Ctrl Pts',(-6.49062803547431E-16,63.2105263157894,
-5.29999999999999));
#24718=CARTESIAN_POINT('Ctrl Pts',(1.42013071988495,63.407894736842,-5.29999999999999));
#24719=CARTESIAN_POINT('Ctrl Pts',(2.65,63.6052631578947,-4.58993464005752));
#24720=CARTESIAN_POINT('Ctrl Pts',(3.87986928011504,63.8026315789474,-3.87986928011504));
#24721=CARTESIAN_POINT('Ctrl Pts',(4.58993464005752,64.,-2.65));
#24722=CARTESIAN_POINT('Ctrl Pts',(5.29999999999999,64.1973684210526,-1.42013071988495));
#24723=CARTESIAN_POINT('Ctrl Pts',(5.29999999999999,64.3947368421052,-9.73594205321179E-16));
#24724=CARTESIAN_POINT('Ctrl Pts',(5.29999999999999,64.5921052631579,1.42013071988495));
#24725=CARTESIAN_POINT('Ctrl Pts',(4.58993464005752,64.7894736842105,2.64999999999999));
#24726=CARTESIAN_POINT('Ctrl Pts',(3.87986928011504,64.9868421052632,3.87986928011504));
#24727=CARTESIAN_POINT('Ctrl Pts',(2.65,65.1842105263158,4.58993464005751));
#24728=CARTESIAN_POINT('Ctrl Pts',(1.42013071988495,65.3815789473685,5.29999999999999));
#24729=CARTESIAN_POINT('Ctrl Pts',(7.41868214577963E-28,65.5789473684211,
5.29999999999999));
#24730=CARTESIAN_POINT('Ctrl Pts',(-1.42013071988495,65.7763157894737,5.29999999999999));
#24731=CARTESIAN_POINT('Ctrl Pts',(-2.65,65.9736842105264,4.58993464005752));
#24732=CARTESIAN_POINT('Ctrl Pts',(-3.87986928011504,66.1710526315789,3.87986928011504));
#24733=CARTESIAN_POINT('Ctrl Pts',(-4.58993464005752,66.3684210526316,2.65));
#24734=CARTESIAN_POINT('Ctrl Pts',(-5.29999999999999,66.5657894736842,1.42013071988495));
#24735=CARTESIAN_POINT('Ctrl Pts',(-5.29999999999999,66.7631578947368,3.24531401773831E-16));
#24736=CARTESIAN_POINT('Ctrl Pts',(-5.29999999999999,66.9605263157895,-1.42013071988495));
#24737=CARTESIAN_POINT('Ctrl Pts',(-4.58993464005752,67.1578947368421,-2.65));
#24738=CARTESIAN_POINT('Ctrl Pts',(-3.87986928011504,67.3552631578947,-3.87986928011504));
#24739=CARTESIAN_POINT('Ctrl Pts',(-2.65,67.5526315789473,-4.58993464005752));
#24740=CARTESIAN_POINT('Ctrl Pts',(-1.42013071988495,67.75,-5.29999999999999));
#24741=CARTESIAN_POINT('Ctrl Pts',(-6.49062803547383E-16,67.9473684210526,
-5.3));
#24742=CARTESIAN_POINT('Ctrl Pts',(1.42013071988495,68.1447368421052,-5.29999999999999));
#24743=CARTESIAN_POINT('Ctrl Pts',(2.65,68.3421052631578,-4.58993464005752));
#24744=CARTESIAN_POINT('Ctrl Pts',(3.87986928011504,68.5394736842105,-3.87986928011504));
#24745=CARTESIAN_POINT('Ctrl Pts',(4.58993464005752,68.7368421052631,-2.65));
#24746=CARTESIAN_POINT('Ctrl Pts',(5.29999999999999,68.9342105263158,-1.42013071988495));
#24747=CARTESIAN_POINT('Ctrl Pts',(5.29999999999999,69.1315789473684,-9.73594205321179E-16));
#24748=CARTESIAN_POINT('Ctrl Pts',(5.29999999999999,69.3289473684211,1.42013071988495));
#24749=CARTESIAN_POINT('Ctrl Pts',(4.58993464005752,69.5263157894736,2.64999999999999));
#24750=CARTESIAN_POINT('Ctrl Pts',(3.87986928011504,69.7236842105263,3.87986928011504));
#24751=CARTESIAN_POINT('Ctrl Pts',(2.65,69.9210526315789,4.58993464005752));
#24752=CARTESIAN_POINT('Ctrl Pts',(1.42013071988495,70.1184210526316,5.29999999999999));
#24753=CARTESIAN_POINT('Ctrl Pts',(7.97334996976316E-28,70.3157894736842,
5.29999999999999));
#24754=CARTESIAN_POINT('Ctrl Pts',(-1.42013071988495,70.5131578947368,5.29999999999999));
#24755=CARTESIAN_POINT('Ctrl Pts',(-2.65,70.7105263157895,4.58993464005752));
#24756=CARTESIAN_POINT('Ctrl Pts',(-3.87986928011504,70.9078947368421,3.87986928011504));
#24757=CARTESIAN_POINT('Ctrl Pts',(-4.58993464005752,71.1052631578947,2.65));
#24758=CARTESIAN_POINT('Ctrl Pts',(-5.29999999999999,71.3026315789474,1.42013071988495));
#24759=CARTESIAN_POINT('Ctrl Pts',(-5.29999999999999,71.5,3.24531401773831E-16));
#24760=CARTESIAN_POINT('Ctrl Pts',(-5.29999999999999,71.6973684210526,-1.42013071988495));
#24761=CARTESIAN_POINT('Ctrl Pts',(-4.58993464005752,71.8947368421052,-2.65));
#24762=CARTESIAN_POINT('Ctrl Pts',(-3.87986928011504,72.0921052631579,-3.87986928011504));
#24763=CARTESIAN_POINT('Ctrl Pts',(-2.65,72.2894736842104,-4.58993464005752));
#24764=CARTESIAN_POINT('Ctrl Pts',(-1.42013071988495,72.4868421052631,-5.29999999999999));
#24765=CARTESIAN_POINT('Ctrl Pts',(-6.49062803547328E-16,72.6842105263157,
-5.29999999999999));
#24766=CARTESIAN_POINT('Ctrl Pts',(1.42013071988495,72.8815789473684,-5.29999999999999));
#24767=CARTESIAN_POINT('Ctrl Pts',(2.65,73.078947368421,-4.58993464005752));
#24768=CARTESIAN_POINT('Ctrl Pts',(3.87986928011504,73.2763157894737,-3.87986928011504));
#24769=CARTESIAN_POINT('Ctrl Pts',(4.58993464005752,73.4736842105263,-2.65));
#24770=CARTESIAN_POINT('Ctrl Pts',(5.29999999999999,73.6710526315789,-1.42013071988495));
#24771=CARTESIAN_POINT('Ctrl Pts',(5.29999999999999,73.8684210526316,-9.73594205321179E-16));
#24772=CARTESIAN_POINT('Ctrl Pts',(5.29999999999999,74.0657894736842,1.42013071988495));
#24773=CARTESIAN_POINT('Ctrl Pts',(4.58993464005752,74.2631578947368,2.64999999999999));
#24774=CARTESIAN_POINT('Ctrl Pts',(3.87986928011504,74.4605263157895,3.87986928011504));
#24775=CARTESIAN_POINT('Ctrl Pts',(2.65,74.6578947368421,4.58993464005751));
#24776=CARTESIAN_POINT('Ctrl Pts',(1.42013071988495,74.8552631578948,5.29999999999999));
#24777=CARTESIAN_POINT('Ctrl Pts',(8.539573373413E-28,75.0526315789474,
5.29999999999999));
#24778=CARTESIAN_POINT('Ctrl Pts',(-1.42013071988495,75.2500000000001,5.29999999999999));
#24779=CARTESIAN_POINT('Ctrl Pts',(-2.65,75.4473684210526,4.58993464005751));
#24780=CARTESIAN_POINT('Ctrl Pts',(-3.87986928011504,75.6447368421053,3.87986928011504));
#24781=CARTESIAN_POINT('Ctrl Pts',(-4.58993464005752,75.8421052631579,2.65));
#24782=CARTESIAN_POINT('Ctrl Pts',(-5.29999999999999,76.0394736842105,1.42013071988495));
#24783=CARTESIAN_POINT('Ctrl Pts',(-5.29999999999999,76.2368421052631,3.24531401773831E-16));
#24784=CARTESIAN_POINT('Ctrl Pts',(-5.29999999999999,76.4342105263158,-1.42013071988495));
#24785=CARTESIAN_POINT('Ctrl Pts',(-4.58993464005752,76.6315789473684,-2.64999999999999));
#24786=CARTESIAN_POINT('Ctrl Pts',(-3.87986928011504,76.828947368421,-3.87986928011504));
#24787=CARTESIAN_POINT('Ctrl Pts',(-2.65,77.0263157894736,-4.58993464005752));
#24788=CARTESIAN_POINT('Ctrl Pts',(-1.42013071988495,77.2236842105262,-5.29999999999999));
#24789=CARTESIAN_POINT('Ctrl Pts',(-6.49062803547279E-16,77.4210526315788,
-5.3));
#24790=CARTESIAN_POINT('Ctrl Pts',(1.42013071988495,77.6184210526316,-5.29999999999999));
#24791=CARTESIAN_POINT('Ctrl Pts',(2.65,77.8157894736841,-4.58993464005752));
#24792=CARTESIAN_POINT('Ctrl Pts',(3.87986928011504,78.0131578947368,-3.87986928011505));
#24793=CARTESIAN_POINT('Ctrl Pts',(4.58993464005752,78.2105263157895,-2.65));
#24794=CARTESIAN_POINT('Ctrl Pts',(5.29999999999999,78.4078947368421,-1.42013071988495));
#24795=CARTESIAN_POINT('Ctrl Pts',(5.29999999999999,78.6052631578947,-9.73594205321327E-16));
#24796=CARTESIAN_POINT('Ctrl Pts',(5.29999999999999,78.8026315789474,1.42013071988494));
#24797=CARTESIAN_POINT('Ctrl Pts',(4.58993464005752,79.,2.64999999999999));
#24798=CARTESIAN_POINT('Ctrl Pts',(3.87986928011504,79.1973684210527,3.87986928011504));
#24799=CARTESIAN_POINT('Ctrl Pts',(2.65,79.3947368421053,4.58993464005752));
#24800=CARTESIAN_POINT('Ctrl Pts',(1.42013071988495,79.5921052631579,5.29999999999999));
#24801=CARTESIAN_POINT('Ctrl Pts',(9.07113003806388E-28,79.7894736842106,
5.29999999999999));
#24802=CARTESIAN_POINT('Ctrl Pts',(-1.42013071988495,79.9868421052632,5.29999999999999));
#24803=CARTESIAN_POINT('Ctrl Pts',(-2.65,80.1842105263158,4.58993464005752));
#24804=CARTESIAN_POINT('Ctrl Pts',(-3.87986928011504,80.3815789473684,3.87986928011504));
#24805=CARTESIAN_POINT('Ctrl Pts',(-4.58993464005752,80.578947368421,2.65));
#24806=CARTESIAN_POINT('Ctrl Pts',(-5.29999999999999,80.7763157894737,1.42013071988495));
#24807=CARTESIAN_POINT('Ctrl Pts',(-5.29999999999999,80.9736842105263,3.24531401773831E-16));
#24808=CARTESIAN_POINT('Ctrl Pts',(-5.29999999999999,81.171052631579,-1.42013071988495));
#24809=CARTESIAN_POINT('Ctrl Pts',(-4.58993464005752,81.3684210526315,-2.64999999999999));
#24810=CARTESIAN_POINT('Ctrl Pts',(-3.87986928011504,81.5657894736842,-3.87986928011504));
#24811=CARTESIAN_POINT('Ctrl Pts',(-2.65,81.7631578947368,-4.58993464005752));
#24812=CARTESIAN_POINT('Ctrl Pts',(-1.42013071988495,81.9605263157895,-5.29999999999999));
#24813=CARTESIAN_POINT('Ctrl Pts',(-6.49062803547223E-16,82.1578947368421,
-5.29999999999999));
#24814=CARTESIAN_POINT('Ctrl Pts',(1.42013071988495,82.3552631578947,-5.29999999999999));
#24815=CARTESIAN_POINT('Ctrl Pts',(2.65,82.5526315789474,-4.58993464005752));
#24816=CARTESIAN_POINT('Ctrl Pts',(3.87986928011504,82.75,-3.87986928011504));
#24817=CARTESIAN_POINT('Ctrl Pts',(4.58993464005752,82.9473684210526,-2.65));
#24818=CARTESIAN_POINT('Ctrl Pts',(5.29999999999999,83.1447368421053,-1.42013071988495));
#24819=CARTESIAN_POINT('Ctrl Pts',(5.29999999999999,83.3421052631579,-9.73594205321327E-16));
#24820=CARTESIAN_POINT('Ctrl Pts',(5.29999999999999,83.5394736842105,1.42013071988495));
#24821=CARTESIAN_POINT('Ctrl Pts',(4.58993464005752,83.7368421052632,2.64999999999999));
#24822=CARTESIAN_POINT('Ctrl Pts',(3.87986928011504,83.9342105263158,3.87986928011504));
#24823=CARTESIAN_POINT('Ctrl Pts',(2.65,84.1315789473685,4.58993464005751));
#24824=CARTESIAN_POINT('Ctrl Pts',(1.42013071988495,84.3289473684211,5.29999999999999));
#24825=CARTESIAN_POINT('Ctrl Pts',(9.56801996371578E-28,84.5263157894737,
5.29999999999999));
#24826=CARTESIAN_POINT('Ctrl Pts',(-1.42013071988495,84.7236842105264,5.29999999999999));
#24827=CARTESIAN_POINT('Ctrl Pts',(-2.65,84.921052631579,4.58993464005751));
#24828=CARTESIAN_POINT('Ctrl Pts',(-3.87986928011504,85.1184210526316,3.87986928011504));
#24829=CARTESIAN_POINT('Ctrl Pts',(-4.58993464005752,85.3157894736842,2.65));
#24830=CARTESIAN_POINT('Ctrl Pts',(-5.29999999999999,85.5131578947368,1.42013071988495));
#24831=CARTESIAN_POINT('Ctrl Pts',(-5.29999999999999,85.7105263157894,3.24531401773979E-16));
#24832=CARTESIAN_POINT('Ctrl Pts',(-5.29999999999999,85.9078947368421,-1.42013071988495));
#24833=CARTESIAN_POINT('Ctrl Pts',(-4.58993464005752,86.1052631578947,-2.65));
#24834=CARTESIAN_POINT('Ctrl Pts',(-3.87986928011504,86.3026315789474,-3.87986928011504));
#24835=CARTESIAN_POINT('Ctrl Pts',(-2.65,86.5,-4.58993464005752));
#24836=CARTESIAN_POINT('Ctrl Pts',(-1.42013071988495,86.6973684210525,-5.29999999999999));
#24837=CARTESIAN_POINT('Ctrl Pts',(-6.49062803547175E-16,86.8947368421052,
-5.29999999999999));
#24838=CARTESIAN_POINT('Ctrl Pts',(1.42013071988495,87.0921052631578,-5.29999999999999));
#24839=CARTESIAN_POINT('Ctrl Pts',(2.65,87.2894736842105,-4.58993464005752));
#24840=CARTESIAN_POINT('Ctrl Pts',(3.87986928011504,87.4868421052632,-3.87986928011504));
#24841=CARTESIAN_POINT('Ctrl Pts',(4.58993464005752,87.6842105263158,-2.65));
#24842=CARTESIAN_POINT('Ctrl Pts',(5.29999999999999,87.8815789473684,-1.42013071988495));
#24843=CARTESIAN_POINT('Ctrl Pts',(5.29999999999999,88.078947368421,-9.73594205322067E-16));
#24844=CARTESIAN_POINT('Ctrl Pts',(5.29999999999999,88.2763157894737,1.42013071988495));
#24845=CARTESIAN_POINT('Ctrl Pts',(4.58993464005752,88.4736842105263,2.64999999999999));
#24846=CARTESIAN_POINT('Ctrl Pts',(3.87986928011504,88.6710526315789,3.87986928011504));
#24847=CARTESIAN_POINT('Ctrl Pts',(2.65,88.8684210526316,4.58993464005752));
#24848=CARTESIAN_POINT('Ctrl Pts',(1.42013071988495,89.0657894736842,5.29999999999999));
#24849=CARTESIAN_POINT('Ctrl Pts',(1.00533543097014E-27,89.2631578947369,
5.29999999999999));
#24850=CARTESIAN_POINT('Ctrl Pts',(-1.42013071988495,89.4605263157895,5.29999999999999));
#24851=CARTESIAN_POINT('Ctrl Pts',(-2.65,89.6578947368422,4.58993464005752));
#24852=CARTESIAN_POINT('Ctrl Pts',(-3.87986928011504,89.8552631578947,3.87986928011504));
#24853=CARTESIAN_POINT('Ctrl Pts',(-4.58993464005752,90.0526315789474,2.65));
#24854=CARTESIAN_POINT('Ctrl Pts',(-5.29999999999999,90.25,1.42013071988495));
#24855=CARTESIAN_POINT('Ctrl Pts',(-5.29999999999999,90.4473684210526,3.24531401774127E-16));
#24856=CARTESIAN_POINT('Ctrl Pts',(-5.29999999999999,90.6447368421053,-1.42013071988495));
#24857=CARTESIAN_POINT('Ctrl Pts',(-4.58993464005752,90.8421052631579,-2.65));
#24858=CARTESIAN_POINT('Ctrl Pts',(-3.87986928011504,91.0394736842105,-3.87986928011504));
#24859=CARTESIAN_POINT('Ctrl Pts',(-2.65,91.2368421052631,-4.58993464005752));
#24860=CARTESIAN_POINT('Ctrl Pts',(-1.42013071988495,91.4342105263158,-5.29999999999999));
#24861=CARTESIAN_POINT('Ctrl Pts',(-6.49062803547121E-16,91.6315789473684,
-5.3));
#24862=CARTESIAN_POINT('Ctrl Pts',(1.42013071988495,91.828947368421,-5.29999999999999));
#24863=CARTESIAN_POINT('Ctrl Pts',(2.65,92.0263157894737,-4.58993464005752));
#24864=CARTESIAN_POINT('Ctrl Pts',(3.87986928011504,92.2236842105263,-3.87986928011504));
#24865=CARTESIAN_POINT('Ctrl Pts',(4.58993464005752,92.4210526315789,-2.65));
#24866=CARTESIAN_POINT('Ctrl Pts',(5.29999999999999,92.6184210526316,-1.42013071988495));
#24867=CARTESIAN_POINT('Ctrl Pts',(5.29999999999999,92.8157894736842,-9.73594205322067E-16));
#24868=CARTESIAN_POINT('Ctrl Pts',(5.29999999999999,93.0131578947368,1.42013071988495));
#24869=CARTESIAN_POINT('Ctrl Pts',(4.58993464005752,93.2105263157895,2.64999999999999));
#24870=CARTESIAN_POINT('Ctrl Pts',(3.87986928011504,93.4078947368421,3.87986928011504));
#24871=CARTESIAN_POINT('Ctrl Pts',(2.65,93.6052631578947,4.58993464005752));
#24872=CARTESIAN_POINT('Ctrl Pts',(1.42013071988495,93.8026315789474,5.29999999999999));
#24873=CARTESIAN_POINT('Ctrl Pts',(1.06080221336849E-27,94.,5.29999999999999));
#24874=CARTESIAN_POINT('Ctrl Pts',(9.70668691971167E-29,3.99999999999997,
9.29999999999999));
#24875=CARTESIAN_POINT('Ctrl Pts',(-2.49192748960944,4.19736842105264,9.29999999999998));
#24876=CARTESIAN_POINT('Ctrl Pts',(-4.64999999999999,4.39473684210525,8.05403625519527));
#24877=CARTESIAN_POINT('Ctrl Pts',(-6.80807251039054,4.59210526315785,6.80807251039054));
#24878=CARTESIAN_POINT('Ctrl Pts',(-8.05403625519527,4.78947368421054,4.64999999999999));
#24879=CARTESIAN_POINT('Ctrl Pts',(-9.29999999999998,4.98684210526316,2.49192748960944));
#24880=CARTESIAN_POINT('Ctrl Pts',(-9.29999999999999,5.18421052631578,5.69460761603425E-16));
#24881=CARTESIAN_POINT('Ctrl Pts',(-9.29999999999998,5.38157894736842,-2.49192748960943));
#24882=CARTESIAN_POINT('Ctrl Pts',(-8.05403625519527,5.57894736842102,-4.64999999999999));
#24883=CARTESIAN_POINT('Ctrl Pts',(-6.80807251039054,5.77631578947368,-6.80807251039054));
#24884=CARTESIAN_POINT('Ctrl Pts',(-4.65,5.97368421052634,-8.05403625519526));
#24885=CARTESIAN_POINT('Ctrl Pts',(-2.49192748960944,6.17105263157895,-9.29999999999998));
#24886=CARTESIAN_POINT('Ctrl Pts',(-1.13892152320701E-15,6.36842105263158,
-9.29999999999999));
#24887=CARTESIAN_POINT('Ctrl Pts',(2.49192748960943,6.56578947368421,-9.29999999999999));
#24888=CARTESIAN_POINT('Ctrl Pts',(4.64999999999999,6.76315789473686,-8.05403625519527));
#24889=CARTESIAN_POINT('Ctrl Pts',(6.80807251039054,6.96052631578947,-6.80807251039055));
#24890=CARTESIAN_POINT('Ctrl Pts',(8.05403625519526,7.1578947368421,-4.65));
#24891=CARTESIAN_POINT('Ctrl Pts',(9.29999999999998,7.35526315789473,-2.49192748960945));
#24892=CARTESIAN_POINT('Ctrl Pts',(9.29999999999999,7.55263157894738,-1.70838228481055E-15));
#24893=CARTESIAN_POINT('Ctrl Pts',(9.29999999999999,7.75,2.49192748960943));
#24894=CARTESIAN_POINT('Ctrl Pts',(8.05403625519527,7.94736842105266,4.64999999999998));
#24895=CARTESIAN_POINT('Ctrl Pts',(6.80807251039055,8.14473684210526,6.80807251039054));
#24896=CARTESIAN_POINT('Ctrl Pts',(4.65,8.3421052631579,8.05403625519527));
#24897=CARTESIAN_POINT('Ctrl Pts',(2.49192748960945,8.53947368421052,9.29999999999998));
#24898=CARTESIAN_POINT('Ctrl Pts',(1.38666955995881E-28,8.73684210526314,
9.29999999999999));
#24899=CARTESIAN_POINT('Ctrl Pts',(-2.49192748960944,8.93421052631578,9.29999999999998));
#24900=CARTESIAN_POINT('Ctrl Pts',(-4.64999999999999,9.13157894736842,8.05403625519527));
#24901=CARTESIAN_POINT('Ctrl Pts',(-6.80807251039054,9.32894736842104,6.80807251039054));
#24902=CARTESIAN_POINT('Ctrl Pts',(-8.05403625519527,9.5263157894737,4.64999999999999));
#24903=CARTESIAN_POINT('Ctrl Pts',(-9.29999999999998,9.7236842105263,2.49192748960944));
#24904=CARTESIAN_POINT('Ctrl Pts',(-9.29999999999999,9.92105263157894,5.69460761603425E-16));
#24905=CARTESIAN_POINT('Ctrl Pts',(-9.29999999999998,10.1184210526316,-2.49192748960944));
#24906=CARTESIAN_POINT('Ctrl Pts',(-8.05403625519527,10.3157894736842,-4.64999999999999));
#24907=CARTESIAN_POINT('Ctrl Pts',(-6.80807251039054,10.5131578947369,-6.80807251039054));
#24908=CARTESIAN_POINT('Ctrl Pts',(-4.65,10.7105263157895,-8.05403625519526));
#24909=CARTESIAN_POINT('Ctrl Pts',(-2.49192748960944,10.9078947368421,-9.29999999999998));
#24910=CARTESIAN_POINT('Ctrl Pts',(-1.13892152320697E-15,11.1052631578947,
-9.29999999999999));
#24911=CARTESIAN_POINT('Ctrl Pts',(2.49192748960943,11.3026315789474,-9.29999999999999));
#24912=CARTESIAN_POINT('Ctrl Pts',(4.64999999999999,11.5,-8.05403625519527));
#24913=CARTESIAN_POINT('Ctrl Pts',(6.80807251039054,11.6973684210527,-6.80807251039055));
#24914=CARTESIAN_POINT('Ctrl Pts',(8.05403625519526,11.8947368421053,-4.65));
#24915=CARTESIAN_POINT('Ctrl Pts',(9.29999999999998,12.0921052631579,-2.49192748960945));
#24916=CARTESIAN_POINT('Ctrl Pts',(9.29999999999999,12.2894736842105,-1.70838228481055E-15));
#24917=CARTESIAN_POINT('Ctrl Pts',(9.29999999999999,12.4868421052632,2.49192748960943));
#24918=CARTESIAN_POINT('Ctrl Pts',(8.05403625519527,12.6842105263158,4.64999999999999));
#24919=CARTESIAN_POINT('Ctrl Pts',(6.80807251039055,12.8815789473684,6.80807251039054));
#24920=CARTESIAN_POINT('Ctrl Pts',(4.65,13.078947368421,8.05403625519526));
#24921=CARTESIAN_POINT('Ctrl Pts',(2.49192748960945,13.2763157894737,9.29999999999998));
#24922=CARTESIAN_POINT('Ctrl Pts',(1.99911528227395E-28,13.4736842105263,
9.29999999999999));
#24923=CARTESIAN_POINT('Ctrl Pts',(-2.49192748960944,13.6710526315789,9.29999999999998));
#24924=CARTESIAN_POINT('Ctrl Pts',(-4.64999999999999,13.8684210526316,8.05403625519527));
#24925=CARTESIAN_POINT('Ctrl Pts',(-6.80807251039054,14.0657894736842,6.80807251039054));
#24926=CARTESIAN_POINT('Ctrl Pts',(-8.05403625519527,14.2631578947369,4.64999999999999));
#24927=CARTESIAN_POINT('Ctrl Pts',(-9.29999999999998,14.4605263157895,2.49192748960944));
#24928=CARTESIAN_POINT('Ctrl Pts',(-9.29999999999999,14.6578947368421,5.69460761603425E-16));
#24929=CARTESIAN_POINT('Ctrl Pts',(-9.29999999999998,14.8552631578947,-2.49192748960944));
#24930=CARTESIAN_POINT('Ctrl Pts',(-8.05403625519527,15.0526315789473,-4.64999999999999));
#24931=CARTESIAN_POINT('Ctrl Pts',(-6.80807251039054,15.25,-6.80807251039054));
#24932=CARTESIAN_POINT('Ctrl Pts',(-4.65,15.4473684210526,-8.05403625519526));
#24933=CARTESIAN_POINT('Ctrl Pts',(-2.49192748960944,15.6447368421053,-9.29999999999998));
#24934=CARTESIAN_POINT('Ctrl Pts',(-1.13892152320691E-15,15.8421052631579,
-9.29999999999999));
#24935=CARTESIAN_POINT('Ctrl Pts',(2.49192748960943,16.0394736842105,-9.29999999999999));
#24936=CARTESIAN_POINT('Ctrl Pts',(4.64999999999999,16.2368421052632,-8.05403625519527));
#24937=CARTESIAN_POINT('Ctrl Pts',(6.80807251039054,16.4342105263158,-6.80807251039055));
#24938=CARTESIAN_POINT('Ctrl Pts',(8.05403625519526,16.6315789473684,-4.65));
#24939=CARTESIAN_POINT('Ctrl Pts',(9.29999999999998,16.828947368421,-2.49192748960944));
#24940=CARTESIAN_POINT('Ctrl Pts',(9.29999999999999,17.0263157894737,-1.70838228481055E-15));
#24941=CARTESIAN_POINT('Ctrl Pts',(9.29999999999999,17.2236842105263,2.49192748960943));
#24942=CARTESIAN_POINT('Ctrl Pts',(8.05403625519527,17.4210526315789,4.64999999999998));
#24943=CARTESIAN_POINT('Ctrl Pts',(6.80807251039055,17.6184210526315,6.80807251039054));
#24944=CARTESIAN_POINT('Ctrl Pts',(4.65,17.8157894736842,8.05403625519526));
#24945=CARTESIAN_POINT('Ctrl Pts',(2.49192748960945,18.0131578947368,9.29999999999998));
#24946=CARTESIAN_POINT('Ctrl Pts',(2.5653386859238E-28,18.2105263157895,
9.29999999999999));
#24947=CARTESIAN_POINT('Ctrl Pts',(-2.49192748960944,18.4078947368421,9.29999999999998));
#24948=CARTESIAN_POINT('Ctrl Pts',(-4.64999999999999,18.6052631578947,8.05403625519527));
#24949=CARTESIAN_POINT('Ctrl Pts',(-6.80807251039054,18.8026315789473,6.80807251039054));
#24950=CARTESIAN_POINT('Ctrl Pts',(-8.05403625519527,19.,4.64999999999999));
#24951=CARTESIAN_POINT('Ctrl Pts',(-9.29999999999998,19.1973684210526,2.49192748960944));
#24952=CARTESIAN_POINT('Ctrl Pts',(-9.29999999999999,19.3947368421053,5.69460761603572E-16));
#24953=CARTESIAN_POINT('Ctrl Pts',(-9.29999999999998,19.5921052631579,-2.49192748960944));
#24954=CARTESIAN_POINT('Ctrl Pts',(-8.05403625519527,19.7894736842105,-4.64999999999999));
#24955=CARTESIAN_POINT('Ctrl Pts',(-6.80807251039054,19.9868421052632,-6.80807251039054));
#24956=CARTESIAN_POINT('Ctrl Pts',(-4.65,20.1842105263158,-8.05403625519526));
#24957=CARTESIAN_POINT('Ctrl Pts',(-2.49192748960944,20.3815789473684,-9.29999999999998));
#24958=CARTESIAN_POINT('Ctrl Pts',(-1.13892152320687E-15,20.5789473684211,
-9.29999999999998));
#24959=CARTESIAN_POINT('Ctrl Pts',(2.49192748960943,20.7763157894737,-9.29999999999999));
#24960=CARTESIAN_POINT('Ctrl Pts',(4.64999999999999,20.9736842105263,-8.05403625519526));
#24961=CARTESIAN_POINT('Ctrl Pts',(6.80807251039054,21.171052631579,-6.80807251039055));
#24962=CARTESIAN_POINT('Ctrl Pts',(8.05403625519526,21.3684210526315,-4.65));
#24963=CARTESIAN_POINT('Ctrl Pts',(9.29999999999998,21.5657894736842,-2.49192748960944));
#24964=CARTESIAN_POINT('Ctrl Pts',(9.29999999999999,21.7631578947368,-1.70838228481055E-15));
#24965=CARTESIAN_POINT('Ctrl Pts',(9.29999999999999,21.9605263157895,2.49192748960943));
#24966=CARTESIAN_POINT('Ctrl Pts',(8.05403625519527,22.1578947368421,4.64999999999998));
#24967=CARTESIAN_POINT('Ctrl Pts',(6.80807251039055,22.3552631578947,6.80807251039054));
#24968=CARTESIAN_POINT('Ctrl Pts',(4.65,22.5526315789473,8.05403625519526));
#24969=CARTESIAN_POINT('Ctrl Pts',(2.49192748960945,22.75,9.29999999999998));
#24970=CARTESIAN_POINT('Ctrl Pts',(3.02756187257673E-28,22.9473684210526,
9.29999999999999));
#24971=CARTESIAN_POINT('Ctrl Pts',(-2.49192748960944,23.1447368421053,9.29999999999998));
#24972=CARTESIAN_POINT('Ctrl Pts',(-4.64999999999999,23.3421052631579,8.05403625519527));
#24973=CARTESIAN_POINT('Ctrl Pts',(-6.80807251039054,23.5394736842105,6.80807251039054));
#24974=CARTESIAN_POINT('Ctrl Pts',(-8.05403625519527,23.7368421052632,4.64999999999999));
#24975=CARTESIAN_POINT('Ctrl Pts',(-9.29999999999998,23.9342105263158,2.49192748960944));
#24976=CARTESIAN_POINT('Ctrl Pts',(-9.29999999999999,24.1315789473684,5.69460761603572E-16));
#24977=CARTESIAN_POINT('Ctrl Pts',(-9.29999999999998,24.328947368421,-2.49192748960944));
#24978=CARTESIAN_POINT('Ctrl Pts',(-8.05403625519527,24.5263157894737,-4.64999999999999));
#24979=CARTESIAN_POINT('Ctrl Pts',(-6.80807251039054,24.7236842105264,-6.80807251039054));
#24980=CARTESIAN_POINT('Ctrl Pts',(-4.65,24.921052631579,-8.05403625519526));
#24981=CARTESIAN_POINT('Ctrl Pts',(-2.49192748960944,25.1184210526316,-9.29999999999998));
#24982=CARTESIAN_POINT('Ctrl Pts',(-1.13892152320681E-15,25.3157894736842,
-9.29999999999999));
#24983=CARTESIAN_POINT('Ctrl Pts',(2.49192748960943,25.5131578947368,-9.29999999999999));
#24984=CARTESIAN_POINT('Ctrl Pts',(4.64999999999999,25.7105263157895,-8.05403625519527));
#24985=CARTESIAN_POINT('Ctrl Pts',(6.80807251039054,25.9078947368421,-6.80807251039055));
#24986=CARTESIAN_POINT('Ctrl Pts',(8.05403625519526,26.1052631578947,-4.65));
#24987=CARTESIAN_POINT('Ctrl Pts',(9.29999999999998,26.3026315789474,-2.49192748960944));
#24988=CARTESIAN_POINT('Ctrl Pts',(9.29999999999999,26.5,-1.70838228481055E-15));
#24989=CARTESIAN_POINT('Ctrl Pts',(9.29999999999999,26.6973684210526,2.49192748960943));
#24990=CARTESIAN_POINT('Ctrl Pts',(8.05403625519527,26.8947368421053,4.64999999999998));
#24991=CARTESIAN_POINT('Ctrl Pts',(6.80807251039055,27.0921052631579,6.80807251039054));
#24992=CARTESIAN_POINT('Ctrl Pts',(4.65,27.2894736842105,8.05403625519527));
#24993=CARTESIAN_POINT('Ctrl Pts',(2.49192748960945,27.4868421052631,9.29999999999998));
#24994=CARTESIAN_POINT('Ctrl Pts',(3.53600737789497E-28,27.6842105263158,
9.29999999999999));
#24995=CARTESIAN_POINT('Ctrl Pts',(-2.49192748960944,27.8815789473684,9.29999999999998));
#24996=CARTESIAN_POINT('Ctrl Pts',(-4.64999999999999,28.078947368421,8.05403625519527));
#24997=CARTESIAN_POINT('Ctrl Pts',(-6.80807251039054,28.2763157894736,6.80807251039054));
#24998=CARTESIAN_POINT('Ctrl Pts',(-8.05403625519527,28.4736842105263,4.64999999999999));
#24999=CARTESIAN_POINT('Ctrl Pts',(-9.29999999999998,28.671052631579,2.49192748960944));
#25000=CARTESIAN_POINT('Ctrl Pts',(-9.29999999999999,28.8684210526316,5.69460761603425E-16));
#25001=CARTESIAN_POINT('Ctrl Pts',(-9.29999999999998,29.0657894736842,-2.49192748960944));
#25002=CARTESIAN_POINT('Ctrl Pts',(-8.05403625519527,29.2631578947368,-4.64999999999999));
#25003=CARTESIAN_POINT('Ctrl Pts',(-6.80807251039054,29.4605263157895,-6.80807251039054));
#25004=CARTESIAN_POINT('Ctrl Pts',(-4.65,29.6578947368421,-8.05403625519526));
#25005=CARTESIAN_POINT('Ctrl Pts',(-2.49192748960944,29.8552631578948,-9.29999999999998));
#25006=CARTESIAN_POINT('Ctrl Pts',(-1.13892152320675E-15,30.0526315789474,
-9.29999999999999));
#25007=CARTESIAN_POINT('Ctrl Pts',(2.49192748960943,30.25,-9.29999999999999));
#25008=CARTESIAN_POINT('Ctrl Pts',(4.64999999999999,30.4473684210526,-8.05403625519527));
#25009=CARTESIAN_POINT('Ctrl Pts',(6.80807251039054,30.6447368421053,-6.80807251039055));
#25010=CARTESIAN_POINT('Ctrl Pts',(8.05403625519526,30.8421052631579,-4.65));
#25011=CARTESIAN_POINT('Ctrl Pts',(9.29999999999998,31.0394736842105,-2.49192748960944));
#25012=CARTESIAN_POINT('Ctrl Pts',(9.29999999999999,31.2368421052632,-1.70838228481055E-15));
#25013=CARTESIAN_POINT('Ctrl Pts',(9.29999999999999,31.4342105263158,2.49192748960943));
#25014=CARTESIAN_POINT('Ctrl Pts',(8.05403625519527,31.6315789473684,4.64999999999998));
#25015=CARTESIAN_POINT('Ctrl Pts',(6.80807251039055,31.828947368421,6.80807251039054));
#25016=CARTESIAN_POINT('Ctrl Pts',(4.65,32.0263157894737,8.05403625519526));
#25017=CARTESIAN_POINT('Ctrl Pts',(2.49192748960945,32.2236842105263,9.29999999999998));
#25018=CARTESIAN_POINT('Ctrl Pts',(4.02134172388055E-28,32.421052631579,
9.29999999999999));
#25019=CARTESIAN_POINT('Ctrl Pts',(-2.49192748960944,32.6184210526315,9.29999999999998));
#25020=CARTESIAN_POINT('Ctrl Pts',(-4.64999999999999,32.8157894736842,8.05403625519527));
#25021=CARTESIAN_POINT('Ctrl Pts',(-6.80807251039054,33.0131578947368,6.80807251039054));
#25022=CARTESIAN_POINT('Ctrl Pts',(-8.05403625519527,33.2105263157895,4.64999999999999));
#25023=CARTESIAN_POINT('Ctrl Pts',(-9.29999999999998,33.4078947368421,2.49192748960944));
#25024=CARTESIAN_POINT('Ctrl Pts',(-9.29999999999999,33.6052631578947,5.69460761603425E-16));
#25025=CARTESIAN_POINT('Ctrl Pts',(-9.29999999999998,33.8026315789473,-2.49192748960943));
#25026=CARTESIAN_POINT('Ctrl Pts',(-8.05403625519527,34.,-4.64999999999999));
#25027=CARTESIAN_POINT('Ctrl Pts',(-6.80807251039054,34.1973684210527,-6.80807251039054));
#25028=CARTESIAN_POINT('Ctrl Pts',(-4.65,34.3947368421053,-8.05403625519526));
#25029=CARTESIAN_POINT('Ctrl Pts',(-2.49192748960944,34.5921052631579,-9.29999999999998));
#25030=CARTESIAN_POINT('Ctrl Pts',(-1.13892152320671E-15,34.7894736842105,
-9.29999999999998));
#25031=CARTESIAN_POINT('Ctrl Pts',(2.49192748960943,34.9868421052632,-9.29999999999999));
#25032=CARTESIAN_POINT('Ctrl Pts',(4.64999999999999,35.1842105263158,-8.05403625519526));
#25033=CARTESIAN_POINT('Ctrl Pts',(6.80807251039054,35.3815789473684,-6.80807251039055));
#25034=CARTESIAN_POINT('Ctrl Pts',(8.05403625519526,35.578947368421,-4.65));
#25035=CARTESIAN_POINT('Ctrl Pts',(9.29999999999998,35.7763157894737,-2.49192748960944));
#25036=CARTESIAN_POINT('Ctrl Pts',(9.29999999999999,35.9736842105263,-1.70838228481055E-15));
#25037=CARTESIAN_POINT('Ctrl Pts',(9.29999999999999,36.171052631579,2.49192748960943));
#25038=CARTESIAN_POINT('Ctrl Pts',(8.05403625519527,36.3684210526316,4.64999999999999));
#25039=CARTESIAN_POINT('Ctrl Pts',(6.80807251039055,36.5657894736842,6.80807251039054));
#25040=CARTESIAN_POINT('Ctrl Pts',(4.65,36.7631578947368,8.05403625519526));
#25041=CARTESIAN_POINT('Ctrl Pts',(2.49192748960945,36.9605263157895,9.29999999999998));
#25042=CARTESIAN_POINT('Ctrl Pts',(4.63378744619569E-28,37.1578947368421,
9.29999999999999));
#25043=CARTESIAN_POINT('Ctrl Pts',(-2.49192748960944,37.3552631578947,9.29999999999998));
#25044=CARTESIAN_POINT('Ctrl Pts',(-4.64999999999999,37.5526315789473,8.05403625519527));
#25045=CARTESIAN_POINT('Ctrl Pts',(-6.80807251039054,37.7499999999999,6.80807251039054));
#25046=CARTESIAN_POINT('Ctrl Pts',(-8.05403625519527,37.9473684210526,4.64999999999999));
#25047=CARTESIAN_POINT('Ctrl Pts',(-9.29999999999998,38.1447368421053,2.49192748960944));
#25048=CARTESIAN_POINT('Ctrl Pts',(-9.29999999999999,38.3421052631579,5.69460761603425E-16));
#25049=CARTESIAN_POINT('Ctrl Pts',(-9.29999999999998,38.5394736842105,-2.49192748960943));
#25050=CARTESIAN_POINT('Ctrl Pts',(-8.05403625519527,38.7368421052631,-4.64999999999999));
#25051=CARTESIAN_POINT('Ctrl Pts',(-6.80807251039054,38.9342105263158,-6.80807251039054));
#25052=CARTESIAN_POINT('Ctrl Pts',(-4.65,39.1315789473684,-8.05403625519526));
#25053=CARTESIAN_POINT('Ctrl Pts',(-2.49192748960944,39.328947368421,-9.29999999999998));
#25054=CARTESIAN_POINT('Ctrl Pts',(-1.13892152320665E-15,39.5263157894737,
-9.29999999999999));
#25055=CARTESIAN_POINT('Ctrl Pts',(2.49192748960943,39.7236842105263,-9.29999999999999));
#25056=CARTESIAN_POINT('Ctrl Pts',(4.64999999999999,39.921052631579,-8.05403625519527));
#25057=CARTESIAN_POINT('Ctrl Pts',(6.80807251039054,40.1184210526316,-6.80807251039055));
#25058=CARTESIAN_POINT('Ctrl Pts',(8.05403625519526,40.3157894736842,-4.65));
#25059=CARTESIAN_POINT('Ctrl Pts',(9.29999999999998,40.5131578947368,-2.49192748960944));
#25060=CARTESIAN_POINT('Ctrl Pts',(9.29999999999999,40.7105263157895,-1.70838228481055E-15));
#25061=CARTESIAN_POINT('Ctrl Pts',(9.29999999999999,40.9078947368421,2.49192748960943));
#25062=CARTESIAN_POINT('Ctrl Pts',(8.05403625519527,41.1052631578948,4.64999999999998));
#25063=CARTESIAN_POINT('Ctrl Pts',(6.80807251039055,41.3026315789473,6.80807251039054));
#25064=CARTESIAN_POINT('Ctrl Pts',(4.65,41.5,8.05403625519527));
#25065=CARTESIAN_POINT('Ctrl Pts',(2.49192748960945,41.6973684210526,9.29999999999998));
#25066=CARTESIAN_POINT('Ctrl Pts',(5.1306773718476E-28,41.8947368421053,
9.29999999999999));
#25067=CARTESIAN_POINT('Ctrl Pts',(-2.49192748960944,42.0921052631579,9.29999999999998));
#25068=CARTESIAN_POINT('Ctrl Pts',(-4.64999999999999,42.2894736842105,8.05403625519527));
#25069=CARTESIAN_POINT('Ctrl Pts',(-6.80807251039054,42.4868421052631,6.80807251039054));
#25070=CARTESIAN_POINT('Ctrl Pts',(-8.05403625519527,42.6842105263158,4.64999999999999));
#25071=CARTESIAN_POINT('Ctrl Pts',(-9.29999999999998,42.8815789473684,2.49192748960944));
#25072=CARTESIAN_POINT('Ctrl Pts',(-9.29999999999999,43.078947368421,5.69460761603425E-16));
#25073=CARTESIAN_POINT('Ctrl Pts',(-9.29999999999998,43.2763157894737,-2.49192748960943));
#25074=CARTESIAN_POINT('Ctrl Pts',(-8.05403625519527,43.4736842105263,-4.64999999999999));
#25075=CARTESIAN_POINT('Ctrl Pts',(-6.80807251039054,43.671052631579,-6.80807251039054));
#25076=CARTESIAN_POINT('Ctrl Pts',(-4.65,43.8684210526316,-8.05403625519526));
#25077=CARTESIAN_POINT('Ctrl Pts',(-2.49192748960944,44.0657894736842,-9.29999999999998));
#25078=CARTESIAN_POINT('Ctrl Pts',(-1.13892152320661E-15,44.2631578947368,
-9.29999999999999));
#25079=CARTESIAN_POINT('Ctrl Pts',(2.49192748960943,44.4605263157895,-9.29999999999999));
#25080=CARTESIAN_POINT('Ctrl Pts',(4.64999999999999,44.6578947368421,-8.05403625519527));
#25081=CARTESIAN_POINT('Ctrl Pts',(6.80807251039054,44.8552631578948,-6.80807251039055));
#25082=CARTESIAN_POINT('Ctrl Pts',(8.05403625519526,45.0526315789473,-4.65));
#25083=CARTESIAN_POINT('Ctrl Pts',(9.29999999999998,45.25,-2.49192748960945));
#25084=CARTESIAN_POINT('Ctrl Pts',(9.29999999999999,45.4473684210526,-1.70838228481055E-15));
#25085=CARTESIAN_POINT('Ctrl Pts',(9.29999999999999,45.6447368421053,2.49192748960943));
#25086=CARTESIAN_POINT('Ctrl Pts',(8.05403625519527,45.8421052631579,4.64999999999999));
#25087=CARTESIAN_POINT('Ctrl Pts',(6.80807251039055,46.0394736842105,6.80807251039054));
#25088=CARTESIAN_POINT('Ctrl Pts',(4.65,46.2368421052631,8.05403625519526));
#25089=CARTESIAN_POINT('Ctrl Pts',(2.49192748960945,46.4342105263158,9.29999999999998));
#25090=CARTESIAN_POINT('Ctrl Pts',(5.61601171783318E-28,46.6315789473684,
9.29999999999999));
#25091=CARTESIAN_POINT('Ctrl Pts',(-2.49192748960944,46.828947368421,9.29999999999998));
#25092=CARTESIAN_POINT('Ctrl Pts',(-4.64999999999999,47.0263157894737,8.05403625519527));
#25093=CARTESIAN_POINT('Ctrl Pts',(-6.80807251039054,47.2236842105263,6.80807251039054));
#25094=CARTESIAN_POINT('Ctrl Pts',(-8.05403625519527,47.421052631579,4.64999999999999));
#25095=CARTESIAN_POINT('Ctrl Pts',(-9.29999999999998,47.6184210526316,2.49192748960944));
#25096=CARTESIAN_POINT('Ctrl Pts',(-9.29999999999999,47.8157894736842,5.69460761603572E-16));
#25097=CARTESIAN_POINT('Ctrl Pts',(-9.29999999999998,48.0131578947368,-2.49192748960943));
#25098=CARTESIAN_POINT('Ctrl Pts',(-8.05403625519527,48.2105263157894,-4.64999999999999));
#25099=CARTESIAN_POINT('Ctrl Pts',(-6.80807251039054,48.4078947368421,-6.80807251039054));
#25100=CARTESIAN_POINT('Ctrl Pts',(-4.65,48.6052631578947,-8.05403625519526));
#25101=CARTESIAN_POINT('Ctrl Pts',(-2.49192748960944,48.8026315789474,-9.29999999999998));
#25102=CARTESIAN_POINT('Ctrl Pts',(-1.13892152320655E-15,49.,-9.29999999999998));
#25103=CARTESIAN_POINT('Ctrl Pts',(2.49192748960943,49.1973684210527,-9.29999999999999));
#25104=CARTESIAN_POINT('Ctrl Pts',(4.64999999999999,49.3947368421053,-8.05403625519527));
#25105=CARTESIAN_POINT('Ctrl Pts',(6.80807251039054,49.5921052631579,-6.80807251039055));
#25106=CARTESIAN_POINT('Ctrl Pts',(8.05403625519526,49.7894736842104,-4.65));
#25107=CARTESIAN_POINT('Ctrl Pts',(9.29999999999998,49.9868421052631,-2.49192748960945));
#25108=CARTESIAN_POINT('Ctrl Pts',(9.29999999999999,50.1842105263158,-1.70838228481055E-15));
#25109=CARTESIAN_POINT('Ctrl Pts',(9.29999999999999,50.3815789473684,2.49192748960943));
#25110=CARTESIAN_POINT('Ctrl Pts',(8.05403625519527,50.5789473684211,4.64999999999998));
#25111=CARTESIAN_POINT('Ctrl Pts',(6.80807251039055,50.7763157894736,6.80807251039054));
#25112=CARTESIAN_POINT('Ctrl Pts',(4.65,50.9736842105263,8.05403625519526));
#25113=CARTESIAN_POINT('Ctrl Pts',(2.49192748960945,51.1710526315789,9.29999999999998));
#25114=CARTESIAN_POINT('Ctrl Pts',(6.1706795418167E-28,51.3684210526316,
9.29999999999999));
#25115=CARTESIAN_POINT('Ctrl Pts',(-2.49192748960944,51.5657894736842,9.29999999999998));
#25116=CARTESIAN_POINT('Ctrl Pts',(-4.64999999999999,51.7631578947368,8.05403625519527));
#25117=CARTESIAN_POINT('Ctrl Pts',(-6.80807251039054,51.9605263157894,6.80807251039054));
#25118=CARTESIAN_POINT('Ctrl Pts',(-8.05403625519527,52.1578947368421,4.64999999999999));
#25119=CARTESIAN_POINT('Ctrl Pts',(-9.29999999999998,52.3552631578947,2.49192748960944));
#25120=CARTESIAN_POINT('Ctrl Pts',(-9.29999999999999,52.5526315789474,5.69460761603572E-16));
#25121=CARTESIAN_POINT('Ctrl Pts',(-9.29999999999998,52.75,-2.49192748960944));
#25122=CARTESIAN_POINT('Ctrl Pts',(-8.05403625519527,52.9473684210526,-4.64999999999999));
#25123=CARTESIAN_POINT('Ctrl Pts',(-6.80807251039054,53.1447368421053,-6.80807251039054));
#25124=CARTESIAN_POINT('Ctrl Pts',(-4.65,53.3421052631579,-8.05403625519526));
#25125=CARTESIAN_POINT('Ctrl Pts',(-2.49192748960944,53.5394736842105,-9.29999999999998));
#25126=CARTESIAN_POINT('Ctrl Pts',(-1.1389215232065E-15,53.7368421052632,
-9.29999999999999));
#25127=CARTESIAN_POINT('Ctrl Pts',(2.49192748960943,53.9342105263158,-9.29999999999999));
#25128=CARTESIAN_POINT('Ctrl Pts',(4.64999999999999,54.1315789473684,-8.05403625519526));
#25129=CARTESIAN_POINT('Ctrl Pts',(6.80807251039054,54.3289473684211,-6.80807251039055));
#25130=CARTESIAN_POINT('Ctrl Pts',(8.05403625519526,54.5263157894736,-4.65));
#25131=CARTESIAN_POINT('Ctrl Pts',(9.29999999999998,54.7236842105263,-2.49192748960944));
#25132=CARTESIAN_POINT('Ctrl Pts',(9.29999999999999,54.9210526315789,-1.7083822848104E-15));
#25133=CARTESIAN_POINT('Ctrl Pts',(9.29999999999999,55.1184210526316,2.49192748960943));
#25134=CARTESIAN_POINT('Ctrl Pts',(8.05403625519527,55.3157894736842,4.64999999999998));
#25135=CARTESIAN_POINT('Ctrl Pts',(6.80807251039055,55.5131578947368,6.80807251039054));
#25136=CARTESIAN_POINT('Ctrl Pts',(4.65,55.7105263157895,8.05403625519526));
#25137=CARTESIAN_POINT('Ctrl Pts',(2.49192748960945,55.9078947368421,9.29999999999998));
#25138=CARTESIAN_POINT('Ctrl Pts',(6.59823598947067E-28,56.1052631578947,
9.29999999999999));
#25139=CARTESIAN_POINT('Ctrl Pts',(-2.49192748960944,56.3026315789474,9.29999999999998));
#25140=CARTESIAN_POINT('Ctrl Pts',(-4.64999999999999,56.5,8.05403625519527));
#25141=CARTESIAN_POINT('Ctrl Pts',(-6.80807251039054,56.6973684210526,6.80807251039054));
#25142=CARTESIAN_POINT('Ctrl Pts',(-8.05403625519527,56.8947368421053,4.64999999999999));
#25143=CARTESIAN_POINT('Ctrl Pts',(-9.29999999999998,57.0921052631579,2.49192748960944));
#25144=CARTESIAN_POINT('Ctrl Pts',(-9.29999999999999,57.2894736842105,5.69460761603572E-16));
#25145=CARTESIAN_POINT('Ctrl Pts',(-9.29999999999998,57.4868421052631,-2.49192748960944));
#25146=CARTESIAN_POINT('Ctrl Pts',(-8.05403625519527,57.6842105263157,-4.64999999999999));
#25147=CARTESIAN_POINT('Ctrl Pts',(-6.80807251039054,57.8815789473684,-6.80807251039054));
#25148=CARTESIAN_POINT('Ctrl Pts',(-4.65,58.0789473684211,-8.05403625519526));
#25149=CARTESIAN_POINT('Ctrl Pts',(-2.49192748960944,58.2763157894737,-9.29999999999998));
#25150=CARTESIAN_POINT('Ctrl Pts',(-1.13892152320645E-15,58.4736842105264,
-9.29999999999999));
#25151=CARTESIAN_POINT('Ctrl Pts',(2.49192748960943,58.671052631579,-9.29999999999999));
#25152=CARTESIAN_POINT('Ctrl Pts',(4.64999999999999,58.8684210526316,-8.05403625519527));
#25153=CARTESIAN_POINT('Ctrl Pts',(6.80807251039054,59.0657894736842,-6.80807251039055));
#25154=CARTESIAN_POINT('Ctrl Pts',(8.05403625519526,59.2631578947368,-4.65));
#25155=CARTESIAN_POINT('Ctrl Pts',(9.29999999999998,59.4605263157895,-2.49192748960944));
#25156=CARTESIAN_POINT('Ctrl Pts',(9.29999999999999,59.6578947368421,-1.7083822848104E-15));
#25157=CARTESIAN_POINT('Ctrl Pts',(9.29999999999999,59.8552631578947,2.49192748960943));
#25158=CARTESIAN_POINT('Ctrl Pts',(8.05403625519527,60.0526315789474,4.64999999999999));
#25159=CARTESIAN_POINT('Ctrl Pts',(6.80807251039055,60.25,6.80807251039054));
#25160=CARTESIAN_POINT('Ctrl Pts',(4.65,60.4473684210526,8.05403625519526));
#25161=CARTESIAN_POINT('Ctrl Pts',(2.49192748960945,60.6447368421052,9.29999999999998));
#25162=CARTESIAN_POINT('Ctrl Pts',(7.18757055245316E-28,60.8421052631579,
9.29999999999999));
#25163=CARTESIAN_POINT('Ctrl Pts',(-2.49192748960944,61.0394736842105,9.29999999999998));
#25164=CARTESIAN_POINT('Ctrl Pts',(-4.64999999999999,61.2368421052631,8.05403625519527));
#25165=CARTESIAN_POINT('Ctrl Pts',(-6.80807251039054,61.4342105263157,6.80807251039054));
#25166=CARTESIAN_POINT('Ctrl Pts',(-8.05403625519527,61.6315789473685,4.64999999999999));
#25167=CARTESIAN_POINT('Ctrl Pts',(-9.29999999999998,61.8289473684211,2.49192748960944));
#25168=CARTESIAN_POINT('Ctrl Pts',(-9.29999999999999,62.0263157894737,5.69460761603425E-16));
#25169=CARTESIAN_POINT('Ctrl Pts',(-9.29999999999998,62.2236842105263,-2.49192748960944));
#25170=CARTESIAN_POINT('Ctrl Pts',(-8.05403625519527,62.4210526315789,-4.64999999999999));
#25171=CARTESIAN_POINT('Ctrl Pts',(-6.80807251039054,62.6184210526316,-6.80807251039054));
#25172=CARTESIAN_POINT('Ctrl Pts',(-4.65,62.8157894736842,-8.05403625519526));
#25173=CARTESIAN_POINT('Ctrl Pts',(-2.49192748960944,63.0131578947368,-9.29999999999998));
#25174=CARTESIAN_POINT('Ctrl Pts',(-1.13892152320639E-15,63.2105263157895,
-9.29999999999999));
#25175=CARTESIAN_POINT('Ctrl Pts',(2.49192748960943,63.4078947368421,-9.29999999999999));
#25176=CARTESIAN_POINT('Ctrl Pts',(4.64999999999999,63.6052631578947,-8.05403625519527));
#25177=CARTESIAN_POINT('Ctrl Pts',(6.80807251039054,63.8026315789474,-6.80807251039055));
#25178=CARTESIAN_POINT('Ctrl Pts',(8.05403625519526,64.,-4.65));
#25179=CARTESIAN_POINT('Ctrl Pts',(9.29999999999998,64.1973684210526,-2.49192748960944));
#25180=CARTESIAN_POINT('Ctrl Pts',(9.29999999999999,64.3947368421052,-1.7083822848104E-15));
#25181=CARTESIAN_POINT('Ctrl Pts',(9.29999999999999,64.5921052631579,2.49192748960943));
#25182=CARTESIAN_POINT('Ctrl Pts',(8.05403625519527,64.7894736842105,4.64999999999998));
#25183=CARTESIAN_POINT('Ctrl Pts',(6.80807251039055,64.9868421052631,6.80807251039053));
#25184=CARTESIAN_POINT('Ctrl Pts',(4.65,65.1842105263158,8.05403625519526));
#25185=CARTESIAN_POINT('Ctrl Pts',(2.49192748960945,65.3815789473684,9.29999999999998));
#25186=CARTESIAN_POINT('Ctrl Pts',(7.69601605777139E-28,65.578947368421,
9.29999999999999));
#25187=CARTESIAN_POINT('Ctrl Pts',(-2.49192748960944,65.7763157894737,9.29999999999999));
#25188=CARTESIAN_POINT('Ctrl Pts',(-4.64999999999999,65.9736842105263,8.05403625519527));
#25189=CARTESIAN_POINT('Ctrl Pts',(-6.80807251039054,66.1710526315789,6.80807251039055));
#25190=CARTESIAN_POINT('Ctrl Pts',(-8.05403625519527,66.3684210526316,4.64999999999999));
#25191=CARTESIAN_POINT('Ctrl Pts',(-9.29999999999998,66.5657894736842,2.49192748960944));
#25192=CARTESIAN_POINT('Ctrl Pts',(-9.29999999999999,66.7631578947368,5.69460761603572E-16));
#25193=CARTESIAN_POINT('Ctrl Pts',(-9.29999999999998,66.9605263157895,-2.49192748960944));
#25194=CARTESIAN_POINT('Ctrl Pts',(-8.05403625519527,67.1578947368421,-4.64999999999999));
#25195=CARTESIAN_POINT('Ctrl Pts',(-6.80807251039054,67.3552631578948,-6.80807251039054));
#25196=CARTESIAN_POINT('Ctrl Pts',(-4.65,67.5526315789474,-8.05403625519526));
#25197=CARTESIAN_POINT('Ctrl Pts',(-2.49192748960944,67.75,-9.29999999999998));
#25198=CARTESIAN_POINT('Ctrl Pts',(-1.13892152320635E-15,67.9473684210527,
-9.29999999999998));
#25199=CARTESIAN_POINT('Ctrl Pts',(2.49192748960943,68.1447368421053,-9.29999999999999));
#25200=CARTESIAN_POINT('Ctrl Pts',(4.64999999999999,68.3421052631579,-8.05403625519526));
#25201=CARTESIAN_POINT('Ctrl Pts',(6.80807251039054,68.5394736842105,-6.80807251039055));
#25202=CARTESIAN_POINT('Ctrl Pts',(8.05403625519526,68.7368421052631,-4.65));
#25203=CARTESIAN_POINT('Ctrl Pts',(9.29999999999998,68.9342105263158,-2.49192748960944));
#25204=CARTESIAN_POINT('Ctrl Pts',(9.29999999999999,69.1315789473684,-1.7083822848104E-15));
#25205=CARTESIAN_POINT('Ctrl Pts',(9.29999999999999,69.3289473684211,2.49192748960943));
#25206=CARTESIAN_POINT('Ctrl Pts',(8.05403625519527,69.5263157894737,4.64999999999999));
#25207=CARTESIAN_POINT('Ctrl Pts',(6.80807251039055,69.7236842105263,6.80807251039054));
#25208=CARTESIAN_POINT('Ctrl Pts',(4.65,69.9210526315789,8.05403625519526));
#25209=CARTESIAN_POINT('Ctrl Pts',(2.49192748960945,70.1184210526316,9.29999999999998));
#25210=CARTESIAN_POINT('Ctrl Pts',(8.22757272242227E-28,70.3157894736842,
9.29999999999999));
#25211=CARTESIAN_POINT('Ctrl Pts',(-2.49192748960944,70.5131578947368,9.29999999999998));
#25212=CARTESIAN_POINT('Ctrl Pts',(-4.64999999999999,70.7105263157894,8.05403625519527));
#25213=CARTESIAN_POINT('Ctrl Pts',(-6.80807251039054,70.9078947368421,6.80807251039054));
#25214=CARTESIAN_POINT('Ctrl Pts',(-8.05403625519527,71.1052631578948,4.64999999999999));
#25215=CARTESIAN_POINT('Ctrl Pts',(-9.29999999999998,71.3026315789474,2.49192748960944));
#25216=CARTESIAN_POINT('Ctrl Pts',(-9.29999999999999,71.5,5.69460761603572E-16));
#25217=CARTESIAN_POINT('Ctrl Pts',(-9.29999999999998,71.6973684210526,-2.49192748960943));
#25218=CARTESIAN_POINT('Ctrl Pts',(-8.05403625519527,71.8947368421052,-4.64999999999999));
#25219=CARTESIAN_POINT('Ctrl Pts',(-6.80807251039054,72.0921052631579,-6.80807251039054));
#25220=CARTESIAN_POINT('Ctrl Pts',(-4.65,72.2894736842105,-8.05403625519526));
#25221=CARTESIAN_POINT('Ctrl Pts',(-2.49192748960944,72.4868421052632,-9.29999999999998));
#25222=CARTESIAN_POINT('Ctrl Pts',(-1.13892152320629E-15,72.6842105263158,
-9.29999999999999));
#25223=CARTESIAN_POINT('Ctrl Pts',(2.49192748960943,72.8815789473684,-9.29999999999999));
#25224=CARTESIAN_POINT('Ctrl Pts',(4.64999999999999,73.078947368421,-8.05403625519527));
#25225=CARTESIAN_POINT('Ctrl Pts',(6.80807251039054,73.2763157894738,-6.80807251039055));
#25226=CARTESIAN_POINT('Ctrl Pts',(8.05403625519526,73.4736842105262,-4.65));
#25227=CARTESIAN_POINT('Ctrl Pts',(9.29999999999998,73.6710526315789,-2.49192748960944));
#25228=CARTESIAN_POINT('Ctrl Pts',(9.29999999999999,73.8684210526316,-1.7083822848104E-15));
#25229=CARTESIAN_POINT('Ctrl Pts',(9.29999999999999,74.0657894736842,2.49192748960943));
#25230=CARTESIAN_POINT('Ctrl Pts',(8.05403625519527,74.2631578947368,4.64999999999998));
#25231=CARTESIAN_POINT('Ctrl Pts',(6.80807251039055,74.4605263157894,6.80807251039054));
#25232=CARTESIAN_POINT('Ctrl Pts',(4.65,74.6578947368421,8.05403625519527));
#25233=CARTESIAN_POINT('Ctrl Pts',(2.49192748960945,74.8552631578947,9.29999999999998));
#25234=CARTESIAN_POINT('Ctrl Pts',(8.7360182277405E-28,75.0526315789473,
9.29999999999999));
#25235=CARTESIAN_POINT('Ctrl Pts',(-2.49192748960944,75.25,9.29999999999998));
#25236=CARTESIAN_POINT('Ctrl Pts',(-4.64999999999999,75.4473684210526,8.05403625519527));
#25237=CARTESIAN_POINT('Ctrl Pts',(-6.80807251039054,75.6447368421052,6.80807251039054));
#25238=CARTESIAN_POINT('Ctrl Pts',(-8.05403625519527,75.8421052631579,4.64999999999999));
#25239=CARTESIAN_POINT('Ctrl Pts',(-9.29999999999998,76.0394736842105,2.49192748960944));
#25240=CARTESIAN_POINT('Ctrl Pts',(-9.29999999999999,76.2368421052631,5.69460761603572E-16));
#25241=CARTESIAN_POINT('Ctrl Pts',(-9.29999999999998,76.4342105263158,-2.49192748960943));
#25242=CARTESIAN_POINT('Ctrl Pts',(-8.05403625519527,76.6315789473684,-4.64999999999999));
#25243=CARTESIAN_POINT('Ctrl Pts',(-6.80807251039054,76.8289473684211,-6.80807251039054));
#25244=CARTESIAN_POINT('Ctrl Pts',(-4.65,77.0263157894737,-8.05403625519526));
#25245=CARTESIAN_POINT('Ctrl Pts',(-2.49192748960944,77.2236842105263,-9.29999999999998));
#25246=CARTESIAN_POINT('Ctrl Pts',(-1.13892152320624E-15,77.4210526315789,
-9.29999999999999));
#25247=CARTESIAN_POINT('Ctrl Pts',(2.49192748960943,77.6184210526316,-9.29999999999999));
#25248=CARTESIAN_POINT('Ctrl Pts',(4.64999999999999,77.8157894736842,-8.05403625519527));
#25249=CARTESIAN_POINT('Ctrl Pts',(6.80807251039054,78.0131578947369,-6.80807251039055));
#25250=CARTESIAN_POINT('Ctrl Pts',(8.05403625519526,78.2105263157894,-4.65));
#25251=CARTESIAN_POINT('Ctrl Pts',(9.29999999999998,78.4078947368421,-2.49192748960944));
#25252=CARTESIAN_POINT('Ctrl Pts',(9.29999999999999,78.6052631578947,-1.70838228481055E-15));
#25253=CARTESIAN_POINT('Ctrl Pts',(9.29999999999999,78.8026315789474,2.49192748960943));
#25254=CARTESIAN_POINT('Ctrl Pts',(8.05403625519527,79.,4.64999999999999));
#25255=CARTESIAN_POINT('Ctrl Pts',(6.80807251039055,79.1973684210526,6.80807251039054));
#25256=CARTESIAN_POINT('Ctrl Pts',(4.65,79.3947368421052,8.05403625519526));
#25257=CARTESIAN_POINT('Ctrl Pts',(2.49192748960945,79.5921052631579,9.29999999999998));
#25258=CARTESIAN_POINT('Ctrl Pts',(9.22135257372608E-28,79.7894736842105,
9.29999999999999));
#25259=CARTESIAN_POINT('Ctrl Pts',(-2.49192748960944,79.9868421052632,9.29999999999998));
#25260=CARTESIAN_POINT('Ctrl Pts',(-4.64999999999999,80.1842105263158,8.05403625519527));
#25261=CARTESIAN_POINT('Ctrl Pts',(-6.80807251039054,80.3815789473684,6.80807251039054));
#25262=CARTESIAN_POINT('Ctrl Pts',(-8.05403625519527,80.5789473684211,4.64999999999999));
#25263=CARTESIAN_POINT('Ctrl Pts',(-9.29999999999998,80.7763157894737,2.49192748960944));
#25264=CARTESIAN_POINT('Ctrl Pts',(-9.29999999999999,80.9736842105263,5.69460761603572E-16));
#25265=CARTESIAN_POINT('Ctrl Pts',(-9.29999999999998,81.1710526315789,-2.49192748960943));
#25266=CARTESIAN_POINT('Ctrl Pts',(-8.05403625519527,81.3684210526315,-4.64999999999999));
#25267=CARTESIAN_POINT('Ctrl Pts',(-6.80807251039054,81.5657894736842,-6.80807251039054));
#25268=CARTESIAN_POINT('Ctrl Pts',(-4.65,81.7631578947368,-8.05403625519526));
#25269=CARTESIAN_POINT('Ctrl Pts',(-2.49192748960944,81.9605263157895,-9.29999999999998));
#25270=CARTESIAN_POINT('Ctrl Pts',(-1.13892152320619E-15,82.1578947368421,
-9.29999999999998));
#25271=CARTESIAN_POINT('Ctrl Pts',(2.49192748960943,82.3552631578947,-9.29999999999999));
#25272=CARTESIAN_POINT('Ctrl Pts',(4.64999999999999,82.5526315789474,-8.05403625519527));
#25273=CARTESIAN_POINT('Ctrl Pts',(6.80807251039054,82.7500000000001,-6.80807251039055));
#25274=CARTESIAN_POINT('Ctrl Pts',(8.05403625519526,82.9473684210525,-4.65));
#25275=CARTESIAN_POINT('Ctrl Pts',(9.29999999999998,83.1447368421052,-2.49192748960944));
#25276=CARTESIAN_POINT('Ctrl Pts',(9.29999999999999,83.3421052631579,-1.70838228481055E-15));
#25277=CARTESIAN_POINT('Ctrl Pts',(9.29999999999999,83.5394736842105,2.49192748960943));
#25278=CARTESIAN_POINT('Ctrl Pts',(8.05403625519527,83.7368421052632,4.64999999999998));
#25279=CARTESIAN_POINT('Ctrl Pts',(6.80807251039055,83.9342105263157,6.80807251039054));
#25280=CARTESIAN_POINT('Ctrl Pts',(4.65,84.1315789473684,8.05403625519526));
#25281=CARTESIAN_POINT('Ctrl Pts',(2.49192748960945,84.328947368421,9.29999999999998));
#25282=CARTESIAN_POINT('Ctrl Pts',(9.8222427163749E-28,84.5263157894737,
9.29999999999999));
#25283=CARTESIAN_POINT('Ctrl Pts',(-2.49192748960944,84.7236842105263,9.29999999999998));
#25284=CARTESIAN_POINT('Ctrl Pts',(-4.64999999999999,84.9210526315789,8.05403625519527));
#25285=CARTESIAN_POINT('Ctrl Pts',(-6.80807251039054,85.1184210526315,6.80807251039054));
#25286=CARTESIAN_POINT('Ctrl Pts',(-8.05403625519527,85.3157894736842,4.64999999999999));
#25287=CARTESIAN_POINT('Ctrl Pts',(-9.29999999999998,85.5131578947368,2.49192748960944));
#25288=CARTESIAN_POINT('Ctrl Pts',(-9.29999999999999,85.7105263157894,5.69460761603425E-16));
#25289=CARTESIAN_POINT('Ctrl Pts',(-9.29999999999998,85.9078947368421,-2.49192748960943));
#25290=CARTESIAN_POINT('Ctrl Pts',(-8.05403625519527,86.1052631578947,-4.64999999999999));
#25291=CARTESIAN_POINT('Ctrl Pts',(-6.80807251039054,86.3026315789474,-6.80807251039054));
#25292=CARTESIAN_POINT('Ctrl Pts',(-4.65,86.5,-8.05403625519526));
#25293=CARTESIAN_POINT('Ctrl Pts',(-2.49192748960944,86.6973684210526,-9.29999999999998));
#25294=CARTESIAN_POINT('Ctrl Pts',(-1.13892152320614E-15,86.8947368421052,
-9.29999999999999));
#25295=CARTESIAN_POINT('Ctrl Pts',(2.49192748960943,87.0921052631579,-9.29999999999999));
#25296=CARTESIAN_POINT('Ctrl Pts',(4.64999999999999,87.2894736842105,-8.05403625519526));
#25297=CARTESIAN_POINT('Ctrl Pts',(6.80807251039054,87.4868421052632,-6.80807251039055));
#25298=CARTESIAN_POINT('Ctrl Pts',(8.05403625519526,87.6842105263158,-4.65));
#25299=CARTESIAN_POINT('Ctrl Pts',(9.29999999999998,87.8815789473684,-2.49192748960945));
#25300=CARTESIAN_POINT('Ctrl Pts',(9.29999999999999,88.078947368421,-1.7083822848107E-15));
#25301=CARTESIAN_POINT('Ctrl Pts',(9.29999999999999,88.2763157894737,2.49192748960943));
#25302=CARTESIAN_POINT('Ctrl Pts',(8.05403625519527,88.4736842105263,4.64999999999998));
#25303=CARTESIAN_POINT('Ctrl Pts',(6.80807251039055,88.6710526315789,6.80807251039054));
#25304=CARTESIAN_POINT('Ctrl Pts',(4.65,88.8684210526316,8.05403625519526));
#25305=CARTESIAN_POINT('Ctrl Pts',(2.49192748960945,89.0657894736842,9.29999999999998));
#25306=CARTESIAN_POINT('Ctrl Pts',(1.02613547436952E-27,89.2631578947368,
9.29999999999999));
#25307=CARTESIAN_POINT('Ctrl Pts',(-2.49192748960944,89.4605263157895,9.29999999999998));
#25308=CARTESIAN_POINT('Ctrl Pts',(-4.64999999999999,89.6578947368421,8.05403625519527));
#25309=CARTESIAN_POINT('Ctrl Pts',(-6.80807251039054,89.8552631578947,6.80807251039054));
#25310=CARTESIAN_POINT('Ctrl Pts',(-8.05403625519527,90.0526315789474,4.64999999999999));
#25311=CARTESIAN_POINT('Ctrl Pts',(-9.29999999999998,90.25,2.49192748960944));
#25312=CARTESIAN_POINT('Ctrl Pts',(-9.29999999999999,90.4473684210526,5.69460761603572E-16));
#25313=CARTESIAN_POINT('Ctrl Pts',(-9.29999999999998,90.6447368421053,-2.49192748960943));
#25314=CARTESIAN_POINT('Ctrl Pts',(-8.05403625519527,90.8421052631578,-4.64999999999999));
#25315=CARTESIAN_POINT('Ctrl Pts',(-6.80807251039054,91.0394736842106,-6.80807251039054));
#25316=CARTESIAN_POINT('Ctrl Pts',(-4.65,91.2368421052632,-8.05403625519526));
#25317=CARTESIAN_POINT('Ctrl Pts',(-2.49192748960944,91.4342105263158,-9.29999999999998));
#25318=CARTESIAN_POINT('Ctrl Pts',(-1.13892152320609E-15,91.6315789473685,
-9.29999999999999));
#25319=CARTESIAN_POINT('Ctrl Pts',(2.49192748960943,91.828947368421,-9.29999999999999));
#25320=CARTESIAN_POINT('Ctrl Pts',(4.64999999999999,92.0263157894737,-8.05403625519527));
#25321=CARTESIAN_POINT('Ctrl Pts',(6.80807251039054,92.2236842105264,-6.80807251039055));
#25322=CARTESIAN_POINT('Ctrl Pts',(8.05403625519526,92.4210526315789,-4.65));
#25323=CARTESIAN_POINT('Ctrl Pts',(9.29999999999998,92.6184210526316,-2.49192748960945));
#25324=CARTESIAN_POINT('Ctrl Pts',(9.29999999999999,92.8157894736842,-1.70838228481055E-15));
#25325=CARTESIAN_POINT('Ctrl Pts',(9.29999999999999,93.0131578947368,2.49192748960943));
#25326=CARTESIAN_POINT('Ctrl Pts',(8.05403625519527,93.2105263157895,4.64999999999999));
#25327=CARTESIAN_POINT('Ctrl Pts',(6.80807251039055,93.4078947368421,6.80807251039054));
#25328=CARTESIAN_POINT('Ctrl Pts',(4.65,93.6052631578947,8.05403625519526));
#25329=CARTESIAN_POINT('Ctrl Pts',(2.49192748960945,93.8026315789474,9.29999999999998));
#25330=CARTESIAN_POINT('Ctrl Pts',(1.08160225676787E-27,94.,9.29999999999999));
#25331=CARTESIAN_POINT('Ctrl Pts',(5.54667823983524E-29,0.,9.29999999999998));
#25332=CARTESIAN_POINT('Ctrl Pts',(-2.49192748960943,0.197368421052581,
9.29999999999998));
#25333=CARTESIAN_POINT('Ctrl Pts',(-4.64999999999999,0.394736842105226,
8.05403625519526));
#25334=CARTESIAN_POINT('Ctrl Pts',(-6.80807251039055,0.592105263157915,
6.80807251039055));
#25335=CARTESIAN_POINT('Ctrl Pts',(-8.05403625519526,0.789473684210562,
4.65));
#25336=CARTESIAN_POINT('Ctrl Pts',(-9.29999999999998,0.986842105263191,
2.49192748960944));
#25337=CARTESIAN_POINT('Ctrl Pts',(-9.29999999999998,1.18421052631579,5.69460761603617E-16));
#25338=CARTESIAN_POINT('Ctrl Pts',(-9.29999999999998,1.38157894736841,-2.49192748960943));
#25339=CARTESIAN_POINT('Ctrl Pts',(-8.05403625519526,1.57894736842101,-4.64999999999998));
#25340=CARTESIAN_POINT('Ctrl Pts',(-6.80807251039055,1.77631578947369,-6.80807251039055));
#25341=CARTESIAN_POINT('Ctrl Pts',(-4.64999999999999,1.97368421052635,-8.05403625519526));
#25342=CARTESIAN_POINT('Ctrl Pts',(-2.49192748960944,2.17105263157896,-9.29999999999998));
#25343=CARTESIAN_POINT('Ctrl Pts',(-1.13892152320706E-15,2.36842105263158,
-9.29999999999998));
#25344=CARTESIAN_POINT('Ctrl Pts',(2.49192748960943,2.56578947368424,-9.29999999999998));
#25345=CARTESIAN_POINT('Ctrl Pts',(4.64999999999999,2.76315789473686,-8.05403625519526));
#25346=CARTESIAN_POINT('Ctrl Pts',(6.80807251039055,2.96052631578946,-6.80807251039056));
#25347=CARTESIAN_POINT('Ctrl Pts',(8.05403625519526,3.15789473684208,-4.64999999999999));
#25348=CARTESIAN_POINT('Ctrl Pts',(9.29999999999998,3.35526315789473,-2.49192748960944));
#25349=CARTESIAN_POINT('Ctrl Pts',(9.29999999999998,3.55263157894736,-1.70838228481046E-15));
#25350=CARTESIAN_POINT('Ctrl Pts',(9.29999999999998,3.75000000000001,2.49192748960943));
#25351=CARTESIAN_POINT('Ctrl Pts',(8.05403625519526,3.94736842105264,4.64999999999998));
#25352=CARTESIAN_POINT('Ctrl Pts',(6.80807251039055,4.14473684210529,6.80807251039055));
#25353=CARTESIAN_POINT('Ctrl Pts',(4.64999999999999,4.34210526315781,8.05403625519526));
#25354=CARTESIAN_POINT('Ctrl Pts',(2.49192748960944,4.53947368421051,9.29999999999998));
#25355=CARTESIAN_POINT('Ctrl Pts',(1.03229845019156E-28,4.73684210526315,
9.29999999999998));
#25356=CARTESIAN_POINT('Ctrl Pts',(-2.49192748960943,4.93421052631578,9.29999999999997));
#25357=CARTESIAN_POINT('Ctrl Pts',(-4.64999999999999,5.13157894736838,8.05403625519527));
#25358=CARTESIAN_POINT('Ctrl Pts',(-6.80807251039055,5.32894736842106,6.80807251039054));
#25359=CARTESIAN_POINT('Ctrl Pts',(-8.05403625519526,5.52631578947371,4.65));
#25360=CARTESIAN_POINT('Ctrl Pts',(-9.29999999999998,5.72368421052634,2.49192748960944));
#25361=CARTESIAN_POINT('Ctrl Pts',(-9.29999999999998,5.92105263157894,5.69460761603617E-16));
#25362=CARTESIAN_POINT('Ctrl Pts',(-9.29999999999998,6.11842105263156,-2.49192748960943));
#25363=CARTESIAN_POINT('Ctrl Pts',(-8.05403625519526,6.31578947368422,-4.64999999999998));
#25364=CARTESIAN_POINT('Ctrl Pts',(-6.80807251039055,6.51315789473683,-6.80807251039055));
#25365=CARTESIAN_POINT('Ctrl Pts',(-4.64999999999999,6.7105263157895,-8.05403625519525));
#25366=CARTESIAN_POINT('Ctrl Pts',(-2.49192748960944,6.90789473684211,-9.29999999999998));
#25367=CARTESIAN_POINT('Ctrl Pts',(-1.138921523207E-15,7.10526315789478,
-9.29999999999997));
#25368=CARTESIAN_POINT('Ctrl Pts',(2.49192748960943,7.30263157894738,-9.29999999999998));
#25369=CARTESIAN_POINT('Ctrl Pts',(4.64999999999999,7.50000000000006,-8.05403625519526));
#25370=CARTESIAN_POINT('Ctrl Pts',(6.80807251039055,7.69736842105261,-6.80807251039056));
#25371=CARTESIAN_POINT('Ctrl Pts',(8.05403625519526,7.89473684210523,-4.64999999999999));
#25372=CARTESIAN_POINT('Ctrl Pts',(9.29999999999998,8.09210526315788,-2.49192748960944));
#25373=CARTESIAN_POINT('Ctrl Pts',(9.29999999999998,8.28947368421051,-1.70838228481065E-15));
#25374=CARTESIAN_POINT('Ctrl Pts',(9.29999999999998,8.48684210526316,2.49192748960943));
#25375=CARTESIAN_POINT('Ctrl Pts',(8.05403625519526,8.68421052631579,4.64999999999998));
#25376=CARTESIAN_POINT('Ctrl Pts',(6.80807251039055,8.88157894736843,6.80807251039054));
#25377=CARTESIAN_POINT('Ctrl Pts',(4.64999999999999,9.07894736842096,8.05403625519526));
#25378=CARTESIAN_POINT('Ctrl Pts',(2.49192748960944,9.27631578947365,9.29999999999998));
#25379=CARTESIAN_POINT('Ctrl Pts',(1.57155883461998E-28,9.4736842105263,
9.29999999999998));
#25380=CARTESIAN_POINT('Ctrl Pts',(-2.49192748960943,9.67105263157893,9.29999999999998));
#25381=CARTESIAN_POINT('Ctrl Pts',(-4.64999999999999,9.86842105263153,8.05403625519526));
#25382=CARTESIAN_POINT('Ctrl Pts',(-6.80807251039055,10.0657894736842,6.80807251039055));
#25383=CARTESIAN_POINT('Ctrl Pts',(-8.05403625519526,10.2631578947369,4.65));
#25384=CARTESIAN_POINT('Ctrl Pts',(-9.29999999999998,10.4605263157895,2.49192748960944));
#25385=CARTESIAN_POINT('Ctrl Pts',(-9.29999999999998,10.6578947368421,5.6946076160342E-16));
#25386=CARTESIAN_POINT('Ctrl Pts',(-9.29999999999998,10.8552631578947,-2.49192748960943));
#25387=CARTESIAN_POINT('Ctrl Pts',(-8.05403625519526,11.0526315789474,-4.64999999999998));
#25388=CARTESIAN_POINT('Ctrl Pts',(-6.80807251039055,11.25,-6.80807251039055));
#25389=CARTESIAN_POINT('Ctrl Pts',(-4.64999999999999,11.4473684210527,-8.05403625519526));
#25390=CARTESIAN_POINT('Ctrl Pts',(-2.49192748960944,11.6447368421053,-9.29999999999999));
#25391=CARTESIAN_POINT('Ctrl Pts',(-1.13892152320696E-15,11.8421052631579,
-9.29999999999998));
#25392=CARTESIAN_POINT('Ctrl Pts',(2.49192748960943,12.0394736842105,-9.29999999999998));
#25393=CARTESIAN_POINT('Ctrl Pts',(4.64999999999999,12.2368421052632,-8.05403625519526));
#25394=CARTESIAN_POINT('Ctrl Pts',(6.80807251039055,12.4342105263158,-6.80807251039055));
#25395=CARTESIAN_POINT('Ctrl Pts',(8.05403625519526,12.6315789473684,-4.64999999999999));
#25396=CARTESIAN_POINT('Ctrl Pts',(9.29999999999998,12.828947368421,-2.49192748960944));
#25397=CARTESIAN_POINT('Ctrl Pts',(9.29999999999998,13.0263157894737,-1.70838228481065E-15));
#25398=CARTESIAN_POINT('Ctrl Pts',(9.29999999999998,13.2236842105263,2.49192748960943));
#25399=CARTESIAN_POINT('Ctrl Pts',(8.05403625519526,13.4210526315789,4.64999999999998));
#25400=CARTESIAN_POINT('Ctrl Pts',(6.80807251039055,13.6184210526316,6.80807251039054));
#25401=CARTESIAN_POINT('Ctrl Pts',(4.64999999999999,13.8157894736841,8.05403625519526));
#25402=CARTESIAN_POINT('Ctrl Pts',(2.49192748960944,14.0131578947368,9.29999999999998));
#25403=CARTESIAN_POINT('Ctrl Pts',(2.04918946082802E-28,14.2105263157895,
9.29999999999998));
#25404=CARTESIAN_POINT('Ctrl Pts',(-2.49192748960943,14.4078947368421,9.29999999999998));
#25405=CARTESIAN_POINT('Ctrl Pts',(-4.64999999999999,14.6052631578947,8.05403625519527));
#25406=CARTESIAN_POINT('Ctrl Pts',(-6.80807251039055,14.8026315789474,6.80807251039055));
#25407=CARTESIAN_POINT('Ctrl Pts',(-8.05403625519526,15.,4.65));
#25408=CARTESIAN_POINT('Ctrl Pts',(-9.29999999999998,15.1973684210526,2.49192748960944));
#25409=CARTESIAN_POINT('Ctrl Pts',(-9.29999999999998,15.3947368421052,5.69460761604603E-16));
#25410=CARTESIAN_POINT('Ctrl Pts',(-9.29999999999998,15.5921052631579,-2.49192748960943));
#25411=CARTESIAN_POINT('Ctrl Pts',(-8.05403625519526,15.7894736842105,-4.64999999999998));
#25412=CARTESIAN_POINT('Ctrl Pts',(-6.80807251039055,15.9868421052631,-6.80807251039055));
#25413=CARTESIAN_POINT('Ctrl Pts',(-4.64999999999999,16.1842105263158,-8.05403625519526));
#25414=CARTESIAN_POINT('Ctrl Pts',(-2.49192748960944,16.3815789473685,-9.29999999999998));
#25415=CARTESIAN_POINT('Ctrl Pts',(-1.13892152320691E-15,16.5789473684211,
-9.29999999999997));
#25416=CARTESIAN_POINT('Ctrl Pts',(2.49192748960943,16.7763157894737,-9.29999999999999));
#25417=CARTESIAN_POINT('Ctrl Pts',(4.64999999999999,16.9736842105264,-8.05403625519526));
#25418=CARTESIAN_POINT('Ctrl Pts',(6.80807251039055,17.1710526315789,-6.80807251039056));
#25419=CARTESIAN_POINT('Ctrl Pts',(8.05403625519526,17.3684210526315,-4.64999999999999));
#25420=CARTESIAN_POINT('Ctrl Pts',(9.29999999999998,17.5657894736842,-2.49192748960944));
#25421=CARTESIAN_POINT('Ctrl Pts',(9.29999999999998,17.7631578947368,-1.70838228481065E-15));
#25422=CARTESIAN_POINT('Ctrl Pts',(9.29999999999998,17.9605263157895,2.49192748960943));
#25423=CARTESIAN_POINT('Ctrl Pts',(8.05403625519526,18.1578947368421,4.64999999999999));
#25424=CARTESIAN_POINT('Ctrl Pts',(6.80807251039055,18.3552631578948,6.80807251039055));
#25425=CARTESIAN_POINT('Ctrl Pts',(4.64999999999999,18.5526315789473,8.05403625519527));
#25426=CARTESIAN_POINT('Ctrl Pts',(2.49192748960944,18.75,9.29999999999998));
#25427=CARTESIAN_POINT('Ctrl Pts',(2.58844984525644E-28,18.9473684210526,
9.29999999999998));
#25428=CARTESIAN_POINT('Ctrl Pts',(-2.49192748960943,19.1447368421052,9.29999999999998));
#25429=CARTESIAN_POINT('Ctrl Pts',(-4.64999999999999,19.3421052631578,8.05403625519526));
#25430=CARTESIAN_POINT('Ctrl Pts',(-6.80807251039055,19.5394736842105,6.80807251039055));
#25431=CARTESIAN_POINT('Ctrl Pts',(-8.05403625519526,19.7368421052632,4.65));
#25432=CARTESIAN_POINT('Ctrl Pts',(-9.29999999999998,19.9342105263158,2.49192748960944));
#25433=CARTESIAN_POINT('Ctrl Pts',(-9.29999999999998,20.1315789473684,5.694607616048E-16));
#25434=CARTESIAN_POINT('Ctrl Pts',(-9.29999999999998,20.328947368421,-2.49192748960943));
#25435=CARTESIAN_POINT('Ctrl Pts',(-8.05403625519526,20.5263157894737,-4.64999999999998));
#25436=CARTESIAN_POINT('Ctrl Pts',(-6.80807251039055,20.7236842105263,-6.80807251039055));
#25437=CARTESIAN_POINT('Ctrl Pts',(-4.64999999999999,20.921052631579,-8.05403625519526));
#25438=CARTESIAN_POINT('Ctrl Pts',(-2.49192748960944,21.1184210526316,-9.29999999999998));
#25439=CARTESIAN_POINT('Ctrl Pts',(-1.13892152320685E-15,21.3157894736842,
-9.29999999999998));
#25440=CARTESIAN_POINT('Ctrl Pts',(2.49192748960943,21.5131578947369,-9.29999999999998));
#25441=CARTESIAN_POINT('Ctrl Pts',(4.64999999999999,21.7105263157895,-8.05403625519526));
#25442=CARTESIAN_POINT('Ctrl Pts',(6.80807251039055,21.9078947368421,-6.80807251039055));
#25443=CARTESIAN_POINT('Ctrl Pts',(8.05403625519526,22.1052631578947,-4.64999999999999));
#25444=CARTESIAN_POINT('Ctrl Pts',(9.29999999999998,22.3026315789474,-2.49192748960944));
#25445=CARTESIAN_POINT('Ctrl Pts',(9.29999999999998,22.5,-1.70838228481046E-15));
#25446=CARTESIAN_POINT('Ctrl Pts',(9.29999999999998,22.6973684210527,2.49192748960943));
#25447=CARTESIAN_POINT('Ctrl Pts',(8.05403625519526,22.8947368421053,4.64999999999999));
#25448=CARTESIAN_POINT('Ctrl Pts',(6.80807251039055,23.0921052631579,6.80807251039054));
#25449=CARTESIAN_POINT('Ctrl Pts',(4.64999999999999,23.2894736842104,8.05403625519526));
#25450=CARTESIAN_POINT('Ctrl Pts',(2.49192748960944,23.4868421052631,9.29999999999996));
#25451=CARTESIAN_POINT('Ctrl Pts',(3.14311766923997E-28,23.6842105263158,
9.29999999999998));
#25452=CARTESIAN_POINT('Ctrl Pts',(-2.49192748960943,23.8815789473684,9.29999999999998));
#25453=CARTESIAN_POINT('Ctrl Pts',(-4.64999999999999,24.078947368421,8.05403625519527));
#25454=CARTESIAN_POINT('Ctrl Pts',(-6.80807251039055,24.2763157894737,6.80807251039055));
#25455=CARTESIAN_POINT('Ctrl Pts',(-8.05403625519526,24.4736842105263,4.65));
#25456=CARTESIAN_POINT('Ctrl Pts',(-9.29999999999998,24.671052631579,2.49192748960944));
#25457=CARTESIAN_POINT('Ctrl Pts',(-9.29999999999998,24.8684210526316,5.69460761603617E-16));
#25458=CARTESIAN_POINT('Ctrl Pts',(-9.29999999999998,25.0657894736842,-2.49192748960943));
#25459=CARTESIAN_POINT('Ctrl Pts',(-8.05403625519526,25.2631578947368,-4.64999999999999));
#25460=CARTESIAN_POINT('Ctrl Pts',(-6.80807251039055,25.4605263157894,-6.80807251039055));
#25461=CARTESIAN_POINT('Ctrl Pts',(-4.64999999999999,25.6578947368421,-8.05403625519526));
#25462=CARTESIAN_POINT('Ctrl Pts',(-2.49192748960944,25.8552631578947,-9.29999999999998));
#25463=CARTESIAN_POINT('Ctrl Pts',(-1.1389215232068E-15,26.0526315789474,
-9.29999999999997));
#25464=CARTESIAN_POINT('Ctrl Pts',(2.49192748960943,26.25,-9.29999999999998));
#25465=CARTESIAN_POINT('Ctrl Pts',(4.64999999999999,26.4473684210527,-8.05403625519526));
#25466=CARTESIAN_POINT('Ctrl Pts',(6.80807251039055,26.6447368421052,-6.80807251039056));
#25467=CARTESIAN_POINT('Ctrl Pts',(8.05403625519526,26.8421052631579,-4.64999999999999));
#25468=CARTESIAN_POINT('Ctrl Pts',(9.29999999999998,27.0394736842105,-2.49192748960945));
#25469=CARTESIAN_POINT('Ctrl Pts',(9.29999999999998,27.2368421052632,-1.70838228481046E-15));
#25470=CARTESIAN_POINT('Ctrl Pts',(9.29999999999998,27.4342105263158,2.49192748960943));
#25471=CARTESIAN_POINT('Ctrl Pts',(8.05403625519526,27.6315789473685,4.64999999999999));
#25472=CARTESIAN_POINT('Ctrl Pts',(6.80807251039055,27.8289473684211,6.80807251039055));
#25473=CARTESIAN_POINT('Ctrl Pts',(4.64999999999999,28.0263157894737,8.05403625519527));
#25474=CARTESIAN_POINT('Ctrl Pts',(2.49192748960944,28.2236842105263,9.29999999999998));
#25475=CARTESIAN_POINT('Ctrl Pts',(3.60534085589291E-28,28.4210526315789,
9.29999999999998));
#25476=CARTESIAN_POINT('Ctrl Pts',(-2.49192748960943,28.6184210526316,9.29999999999997));
#25477=CARTESIAN_POINT('Ctrl Pts',(-4.64999999999999,28.8157894736841,8.05403625519526));
#25478=CARTESIAN_POINT('Ctrl Pts',(-6.80807251039055,29.0131578947368,6.80807251039054));
#25479=CARTESIAN_POINT('Ctrl Pts',(-8.05403625519526,29.2105263157895,4.65));
#25480=CARTESIAN_POINT('Ctrl Pts',(-9.29999999999998,29.4078947368421,2.49192748960944));
#25481=CARTESIAN_POINT('Ctrl Pts',(-9.29999999999998,29.6052631578947,5.69460761603617E-16));
#25482=CARTESIAN_POINT('Ctrl Pts',(-9.29999999999998,29.8026315789473,-2.49192748960943));
#25483=CARTESIAN_POINT('Ctrl Pts',(-8.05403625519526,30.,-4.64999999999999));
#25484=CARTESIAN_POINT('Ctrl Pts',(-6.80807251039055,30.1973684210526,-6.80807251039055));
#25485=CARTESIAN_POINT('Ctrl Pts',(-4.64999999999999,30.3947368421054,-8.05403625519526));
#25486=CARTESIAN_POINT('Ctrl Pts',(-2.49192748960944,30.5921052631579,-9.29999999999998));
#25487=CARTESIAN_POINT('Ctrl Pts',(-1.13892152320674E-15,30.7894736842105,
-9.29999999999998));
#25488=CARTESIAN_POINT('Ctrl Pts',(2.49192748960943,30.9868421052632,-9.29999999999998));
#25489=CARTESIAN_POINT('Ctrl Pts',(4.64999999999999,31.1842105263158,-8.05403625519526));
#25490=CARTESIAN_POINT('Ctrl Pts',(6.80807251039055,31.3815789473684,-6.80807251039055));
#25491=CARTESIAN_POINT('Ctrl Pts',(8.05403625519526,31.578947368421,-4.64999999999999));
#25492=CARTESIAN_POINT('Ctrl Pts',(9.29999999999998,31.7763157894737,-2.49192748960944));
#25493=CARTESIAN_POINT('Ctrl Pts',(9.29999999999998,31.9736842105263,-1.70838228481046E-15));
#25494=CARTESIAN_POINT('Ctrl Pts',(9.29999999999998,32.1710526315789,2.49192748960943));
#25495=CARTESIAN_POINT('Ctrl Pts',(8.05403625519526,32.3684210526316,4.64999999999999));
#25496=CARTESIAN_POINT('Ctrl Pts',(6.80807251039055,32.5657894736842,6.80807251039054));
#25497=CARTESIAN_POINT('Ctrl Pts',(4.64999999999999,32.7631578947368,8.05403625519526));
#25498=CARTESIAN_POINT('Ctrl Pts',(2.49192748960944,32.9605263157894,9.29999999999998));
#25499=CARTESIAN_POINT('Ctrl Pts',(4.14460124032133E-28,33.1578947368421,
9.29999999999998));
#25500=CARTESIAN_POINT('Ctrl Pts',(-2.49192748960943,33.3552631578947,9.29999999999998));
#25501=CARTESIAN_POINT('Ctrl Pts',(-4.64999999999999,33.5526315789473,8.05403625519527));
#25502=CARTESIAN_POINT('Ctrl Pts',(-6.80807251039055,33.75,6.80807251039055));
#25503=CARTESIAN_POINT('Ctrl Pts',(-8.05403625519526,33.9473684210527,4.64999999999999));
#25504=CARTESIAN_POINT('Ctrl Pts',(-9.29999999999998,34.1447368421052,2.49192748960944));
#25505=CARTESIAN_POINT('Ctrl Pts',(-9.29999999999998,34.3421052631579,5.69460761604603E-16));
#25506=CARTESIAN_POINT('Ctrl Pts',(-9.29999999999998,34.5394736842105,-2.49192748960943));
#25507=CARTESIAN_POINT('Ctrl Pts',(-8.05403625519526,34.7368421052631,-4.64999999999999));
#25508=CARTESIAN_POINT('Ctrl Pts',(-6.80807251039055,34.9342105263158,-6.80807251039055));
#25509=CARTESIAN_POINT('Ctrl Pts',(-4.64999999999999,35.1315789473685,-8.05403625519526));
#25510=CARTESIAN_POINT('Ctrl Pts',(-2.49192748960944,35.3289473684211,-9.29999999999999));
#25511=CARTESIAN_POINT('Ctrl Pts',(-1.1389215232067E-15,35.5263157894737,
-9.29999999999998));
#25512=CARTESIAN_POINT('Ctrl Pts',(2.49192748960943,35.7236842105263,-9.29999999999998));
#25513=CARTESIAN_POINT('Ctrl Pts',(4.64999999999999,35.921052631579,-8.05403625519525));
#25514=CARTESIAN_POINT('Ctrl Pts',(6.80807251039055,36.1184210526315,-6.80807251039056));
#25515=CARTESIAN_POINT('Ctrl Pts',(8.05403625519526,36.3157894736842,-4.64999999999999));
#25516=CARTESIAN_POINT('Ctrl Pts',(9.29999999999998,36.5131578947368,-2.49192748960944));
#25517=CARTESIAN_POINT('Ctrl Pts',(9.29999999999998,36.7105263157895,-1.70838228481065E-15));
#25518=CARTESIAN_POINT('Ctrl Pts',(9.29999999999998,36.9078947368421,2.49192748960943));
#25519=CARTESIAN_POINT('Ctrl Pts',(8.05403625519526,37.1052631578948,4.64999999999999));
#25520=CARTESIAN_POINT('Ctrl Pts',(6.80807251039055,37.3026315789473,6.80807251039055));
#25521=CARTESIAN_POINT('Ctrl Pts',(4.64999999999999,37.5,8.05403625519526));
#25522=CARTESIAN_POINT('Ctrl Pts',(2.49192748960944,37.6973684210526,9.29999999999998));
#25523=CARTESIAN_POINT('Ctrl Pts',(4.65304674563956E-28,37.8947368421053,
9.29999999999998));
#25524=CARTESIAN_POINT('Ctrl Pts',(-2.49192748960943,38.0921052631579,9.29999999999998));
#25525=CARTESIAN_POINT('Ctrl Pts',(-4.64999999999999,38.2894736842104,8.05403625519526));
#25526=CARTESIAN_POINT('Ctrl Pts',(-6.80807251039055,38.4868421052632,6.80807251039054));
#25527=CARTESIAN_POINT('Ctrl Pts',(-8.05403625519526,38.6842105263158,4.64999999999999));
#25528=CARTESIAN_POINT('Ctrl Pts',(-9.29999999999998,38.8815789473684,2.49192748960944));
#25529=CARTESIAN_POINT('Ctrl Pts',(-9.29999999999998,39.078947368421,5.69460761604603E-16));
#25530=CARTESIAN_POINT('Ctrl Pts',(-9.29999999999998,39.2763157894737,-2.49192748960943));
#25531=CARTESIAN_POINT('Ctrl Pts',(-8.05403625519526,39.4736842105263,-4.64999999999999));
#25532=CARTESIAN_POINT('Ctrl Pts',(-6.80807251039055,39.6710526315789,-6.80807251039055));
#25533=CARTESIAN_POINT('Ctrl Pts',(-4.64999999999999,39.8684210526317,-8.05403625519526));
#25534=CARTESIAN_POINT('Ctrl Pts',(-2.49192748960944,40.0657894736842,-9.29999999999998));
#25535=CARTESIAN_POINT('Ctrl Pts',(-1.13892152320665E-15,40.2631578947368,
-9.29999999999998));
#25536=CARTESIAN_POINT('Ctrl Pts',(2.49192748960943,40.4605263157895,-9.29999999999999));
#25537=CARTESIAN_POINT('Ctrl Pts',(4.64999999999999,40.6578947368421,-8.05403625519526));
#25538=CARTESIAN_POINT('Ctrl Pts',(6.80807251039055,40.8552631578947,-6.80807251039056));
#25539=CARTESIAN_POINT('Ctrl Pts',(8.05403625519526,41.0526315789473,-4.64999999999999));
#25540=CARTESIAN_POINT('Ctrl Pts',(9.29999999999998,41.25,-2.49192748960944));
#25541=CARTESIAN_POINT('Ctrl Pts',(9.29999999999998,41.4473684210526,-1.70838228481085E-15));
#25542=CARTESIAN_POINT('Ctrl Pts',(9.29999999999998,41.6447368421053,2.49192748960943));
#25543=CARTESIAN_POINT('Ctrl Pts',(8.05403625519526,41.8421052631579,4.64999999999998));
#25544=CARTESIAN_POINT('Ctrl Pts',(6.80807251039055,42.0394736842106,6.80807251039054));
#25545=CARTESIAN_POINT('Ctrl Pts',(4.64999999999999,42.2368421052631,8.05403625519526));
#25546=CARTESIAN_POINT('Ctrl Pts',(2.49192748960944,42.4342105263158,9.29999999999996));
#25547=CARTESIAN_POINT('Ctrl Pts',(5.17689969051289E-28,42.6315789473684,
9.29999999999998));
#25548=CARTESIAN_POINT('Ctrl Pts',(-2.49192748960943,42.828947368421,9.29999999999998));
#25549=CARTESIAN_POINT('Ctrl Pts',(-4.64999999999999,43.0263157894736,8.05403625519526));
#25550=CARTESIAN_POINT('Ctrl Pts',(-6.80807251039055,43.2236842105263,6.80807251039055));
#25551=CARTESIAN_POINT('Ctrl Pts',(-8.05403625519526,43.421052631579,4.64999999999999));
#25552=CARTESIAN_POINT('Ctrl Pts',(-9.29999999999998,43.6184210526316,2.49192748960944));
#25553=CARTESIAN_POINT('Ctrl Pts',(-9.29999999999998,43.8157894736842,5.69460761603617E-16));
#25554=CARTESIAN_POINT('Ctrl Pts',(-9.29999999999998,44.0131578947368,-2.49192748960943));
#25555=CARTESIAN_POINT('Ctrl Pts',(-8.05403625519526,44.2105263157894,-4.64999999999999));
#25556=CARTESIAN_POINT('Ctrl Pts',(-6.80807251039055,44.4078947368421,-6.80807251039055));
#25557=CARTESIAN_POINT('Ctrl Pts',(-4.64999999999999,44.6052631578948,-8.05403625519526));
#25558=CARTESIAN_POINT('Ctrl Pts',(-2.49192748960944,44.8026315789474,-9.29999999999998));
#25559=CARTESIAN_POINT('Ctrl Pts',(-1.1389215232066E-15,45.,-9.29999999999998));
#25560=CARTESIAN_POINT('Ctrl Pts',(2.49192748960943,45.1973684210527,-9.29999999999998));
#25561=CARTESIAN_POINT('Ctrl Pts',(4.64999999999999,45.3947368421053,-8.05403625519525));
#25562=CARTESIAN_POINT('Ctrl Pts',(6.80807251039055,45.5921052631579,-6.80807251039055));
#25563=CARTESIAN_POINT('Ctrl Pts',(8.05403625519526,45.7894736842105,-4.64999999999999));
#25564=CARTESIAN_POINT('Ctrl Pts',(9.29999999999998,45.9868421052631,-2.49192748960944));
#25565=CARTESIAN_POINT('Ctrl Pts',(9.29999999999998,46.1842105263158,-1.70838228481046E-15));
#25566=CARTESIAN_POINT('Ctrl Pts',(9.29999999999998,46.3815789473684,2.49192748960943));
#25567=CARTESIAN_POINT('Ctrl Pts',(8.05403625519526,46.5789473684211,4.64999999999998));
#25568=CARTESIAN_POINT('Ctrl Pts',(6.80807251039055,46.7763157894737,6.80807251039054));
#25569=CARTESIAN_POINT('Ctrl Pts',(4.64999999999999,46.9736842105263,8.05403625519526));
#25570=CARTESIAN_POINT('Ctrl Pts',(2.49192748960944,47.1710526315789,9.29999999999996));
#25571=CARTESIAN_POINT('Ctrl Pts',(5.73156751449641E-28,47.3684210526316,
9.29999999999999));
#25572=CARTESIAN_POINT('Ctrl Pts',(-2.49192748960943,47.5657894736841,9.29999999999998));
#25573=CARTESIAN_POINT('Ctrl Pts',(-4.64999999999999,47.7631578947367,8.05403625519526));
#25574=CARTESIAN_POINT('Ctrl Pts',(-6.80807251039055,47.9605263157895,6.80807251039055));
#25575=CARTESIAN_POINT('Ctrl Pts',(-8.05403625519526,48.1578947368421,4.64999999999999));
#25576=CARTESIAN_POINT('Ctrl Pts',(-9.29999999999998,48.3552631578947,2.49192748960944));
#25577=CARTESIAN_POINT('Ctrl Pts',(-9.29999999999998,48.5526315789474,5.6946076160342E-16));
#25578=CARTESIAN_POINT('Ctrl Pts',(-9.29999999999998,48.75,-2.49192748960943));
#25579=CARTESIAN_POINT('Ctrl Pts',(-8.05403625519526,48.9473684210526,-4.64999999999999));
#25580=CARTESIAN_POINT('Ctrl Pts',(-6.80807251039055,49.1447368421053,-6.80807251039055));
#25581=CARTESIAN_POINT('Ctrl Pts',(-4.64999999999999,49.342105263158,-8.05403625519525));
#25582=CARTESIAN_POINT('Ctrl Pts',(-2.49192748960944,49.5394736842105,-9.29999999999998));
#25583=CARTESIAN_POINT('Ctrl Pts',(-1.13892152320654E-15,49.7368421052632,
-9.29999999999998));
#25584=CARTESIAN_POINT('Ctrl Pts',(2.49192748960943,49.9342105263158,-9.29999999999998));
#25585=CARTESIAN_POINT('Ctrl Pts',(4.64999999999999,50.1315789473684,-8.05403625519526));
#25586=CARTESIAN_POINT('Ctrl Pts',(6.80807251039055,50.328947368421,-6.80807251039056));
#25587=CARTESIAN_POINT('Ctrl Pts',(8.05403625519526,50.5263157894736,-4.64999999999999));
#25588=CARTESIAN_POINT('Ctrl Pts',(9.29999999999998,50.7236842105263,-2.49192748960944));
#25589=CARTESIAN_POINT('Ctrl Pts',(9.29999999999998,50.9210526315789,-1.70838228480937E-15));
#25590=CARTESIAN_POINT('Ctrl Pts',(9.29999999999998,51.1184210526316,2.49192748960943));
#25591=CARTESIAN_POINT('Ctrl Pts',(8.05403625519526,51.3157894736842,4.64999999999998));
#25592=CARTESIAN_POINT('Ctrl Pts',(6.80807251039055,51.5131578947368,6.80807251039055));
#25593=CARTESIAN_POINT('Ctrl Pts',(4.64999999999999,51.7105263157894,8.05403625519526));
#25594=CARTESIAN_POINT('Ctrl Pts',(2.49192748960944,51.9078947368421,9.29999999999998));
#25595=CARTESIAN_POINT('Ctrl Pts',(6.28623533847994E-28,52.1052631578947,
9.29999999999998));
#25596=CARTESIAN_POINT('Ctrl Pts',(-2.49192748960943,52.3026315789474,9.29999999999997));
#25597=CARTESIAN_POINT('Ctrl Pts',(-4.64999999999999,52.5,8.05403625519526));
#25598=CARTESIAN_POINT('Ctrl Pts',(-6.80807251039055,52.6973684210526,6.80807251039054));
#25599=CARTESIAN_POINT('Ctrl Pts',(-8.05403625519526,52.8947368421053,4.64999999999999));
#25600=CARTESIAN_POINT('Ctrl Pts',(-9.29999999999998,53.0921052631579,2.49192748960944));
#25601=CARTESIAN_POINT('Ctrl Pts',(-9.29999999999998,53.2894736842105,5.69460761604603E-16));
#25602=CARTESIAN_POINT('Ctrl Pts',(-9.29999999999998,53.4868421052631,-2.49192748960943));
#25603=CARTESIAN_POINT('Ctrl Pts',(-8.05403625519526,53.6842105263158,-4.64999999999998));
#25604=CARTESIAN_POINT('Ctrl Pts',(-6.80807251039055,53.8815789473684,-6.80807251039055));
#25605=CARTESIAN_POINT('Ctrl Pts',(-4.64999999999999,54.0789473684211,-8.05403625519526));
#25606=CARTESIAN_POINT('Ctrl Pts',(-2.49192748960944,54.2763157894737,-9.29999999999999));
#25607=CARTESIAN_POINT('Ctrl Pts',(-1.13892152320649E-15,54.4736842105263,
-9.29999999999998));
#25608=CARTESIAN_POINT('Ctrl Pts',(2.49192748960943,54.671052631579,-9.29999999999998));
#25609=CARTESIAN_POINT('Ctrl Pts',(4.64999999999999,54.8684210526317,-8.05403625519525));
#25610=CARTESIAN_POINT('Ctrl Pts',(6.80807251039055,55.0657894736842,-6.80807251039055));
#25611=CARTESIAN_POINT('Ctrl Pts',(8.05403625519526,55.2631578947368,-4.64999999999999));
#25612=CARTESIAN_POINT('Ctrl Pts',(9.29999999999998,55.4605263157895,-2.49192748960945));
#25613=CARTESIAN_POINT('Ctrl Pts',(9.29999999999998,55.6578947368421,-1.70838228480947E-15));
#25614=CARTESIAN_POINT('Ctrl Pts',(9.29999999999998,55.8552631578947,2.49192748960943));
#25615=CARTESIAN_POINT('Ctrl Pts',(8.05403625519526,56.0526315789474,4.64999999999998));
#25616=CARTESIAN_POINT('Ctrl Pts',(6.80807251039055,56.25,6.80807251039054));
#25617=CARTESIAN_POINT('Ctrl Pts',(4.64999999999999,56.4473684210526,8.05403625519526));
#25618=CARTESIAN_POINT('Ctrl Pts',(2.49192748960944,56.6447368421052,9.29999999999998));
#25619=CARTESIAN_POINT('Ctrl Pts',(6.74845852513287E-28,56.8421052631579,
9.29999999999999));
#25620=CARTESIAN_POINT('Ctrl Pts',(-2.49192748960943,57.0394736842105,9.29999999999998));
#25621=CARTESIAN_POINT('Ctrl Pts',(-4.64999999999999,57.2368421052632,8.05403625519526));
#25622=CARTESIAN_POINT('Ctrl Pts',(-6.80807251039055,57.4342105263158,6.80807251039055));
#25623=CARTESIAN_POINT('Ctrl Pts',(-8.05403625519526,57.6315789473684,4.64999999999999));
#25624=CARTESIAN_POINT('Ctrl Pts',(-9.29999999999998,57.8289473684211,2.49192748960944));
#25625=CARTESIAN_POINT('Ctrl Pts',(-9.29999999999998,58.0263157894737,5.69460761604603E-16));
#25626=CARTESIAN_POINT('Ctrl Pts',(-9.29999999999998,58.2236842105263,-2.49192748960943));
#25627=CARTESIAN_POINT('Ctrl Pts',(-8.05403625519526,58.4210526315789,-4.64999999999998));
#25628=CARTESIAN_POINT('Ctrl Pts',(-6.80807251039055,58.6184210526316,-6.80807251039055));
#25629=CARTESIAN_POINT('Ctrl Pts',(-4.64999999999999,58.8157894736843,-8.05403625519525));
#25630=CARTESIAN_POINT('Ctrl Pts',(-2.49192748960944,59.0131578947368,-9.29999999999999));
#25631=CARTESIAN_POINT('Ctrl Pts',(-1.13892152320644E-15,59.2105263157895,
-9.29999999999998));
#25632=CARTESIAN_POINT('Ctrl Pts',(2.49192748960943,59.4078947368421,-9.29999999999999));
#25633=CARTESIAN_POINT('Ctrl Pts',(4.64999999999999,59.6052631578948,-8.05403625519526));
#25634=CARTESIAN_POINT('Ctrl Pts',(6.80807251039055,59.8026315789474,-6.80807251039056));
#25635=CARTESIAN_POINT('Ctrl Pts',(8.05403625519526,60.,-4.64999999999999));
#25636=CARTESIAN_POINT('Ctrl Pts',(9.29999999999998,60.1973684210526,-2.49192748960944));
#25637=CARTESIAN_POINT('Ctrl Pts',(9.29999999999998,60.3947368421052,-1.70838228480947E-15));
#25638=CARTESIAN_POINT('Ctrl Pts',(9.29999999999998,60.5921052631579,2.49192748960943));
#25639=CARTESIAN_POINT('Ctrl Pts',(8.05403625519526,60.7894736842106,4.64999999999998));
#25640=CARTESIAN_POINT('Ctrl Pts',(6.80807251039055,60.9868421052632,6.80807251039055));
#25641=CARTESIAN_POINT('Ctrl Pts',(4.64999999999999,61.1842105263157,8.05403625519526));
#25642=CARTESIAN_POINT('Ctrl Pts',(2.49192748960944,61.3815789473684,9.29999999999998));
#25643=CARTESIAN_POINT('Ctrl Pts',(7.21068171178581E-28,61.578947368421,
9.29999999999998));
#25644=CARTESIAN_POINT('Ctrl Pts',(-2.49192748960943,61.7763157894737,9.29999999999998));
#25645=CARTESIAN_POINT('Ctrl Pts',(-4.64999999999999,61.9736842105263,8.05403625519526));
#25646=CARTESIAN_POINT('Ctrl Pts',(-6.80807251039055,62.171052631579,6.80807251039054));
#25647=CARTESIAN_POINT('Ctrl Pts',(-8.05403625519526,62.3684210526316,4.64999999999999));
#25648=CARTESIAN_POINT('Ctrl Pts',(-9.29999999999998,62.5657894736842,2.49192748960944));
#25649=CARTESIAN_POINT('Ctrl Pts',(-9.29999999999998,62.7631578947368,5.69460761604012E-16));
#25650=CARTESIAN_POINT('Ctrl Pts',(-9.29999999999998,62.9605263157895,-2.49192748960943));
#25651=CARTESIAN_POINT('Ctrl Pts',(-8.05403625519526,63.1578947368421,-4.64999999999998));
#25652=CARTESIAN_POINT('Ctrl Pts',(-6.80807251039055,63.3552631578947,-6.80807251039055));
#25653=CARTESIAN_POINT('Ctrl Pts',(-4.64999999999999,63.5526315789474,-8.05403625519526));
#25654=CARTESIAN_POINT('Ctrl Pts',(-2.49192748960944,63.75,-9.29999999999998));
#25655=CARTESIAN_POINT('Ctrl Pts',(-1.13892152320638E-15,63.9473684210526,
-9.29999999999998));
#25656=CARTESIAN_POINT('Ctrl Pts',(2.49192748960943,64.1447368421052,-9.29999999999999));
#25657=CARTESIAN_POINT('Ctrl Pts',(4.64999999999999,64.342105263158,-8.05403625519526));
#25658=CARTESIAN_POINT('Ctrl Pts',(6.80807251039055,64.5394736842105,-6.80807251039056));
#25659=CARTESIAN_POINT('Ctrl Pts',(8.05403625519526,64.7368421052632,-4.64999999999999));
#25660=CARTESIAN_POINT('Ctrl Pts',(9.29999999999998,64.9342105263157,-2.49192748960944));
#25661=CARTESIAN_POINT('Ctrl Pts',(9.29999999999998,65.1315789473684,-1.70838228480937E-15));
#25662=CARTESIAN_POINT('Ctrl Pts',(9.29999999999998,65.3289473684211,2.49192748960943));
#25663=CARTESIAN_POINT('Ctrl Pts',(8.05403625519526,65.5263157894736,4.64999999999998));
#25664=CARTESIAN_POINT('Ctrl Pts',(6.80807251039055,65.7236842105263,6.80807251039054));
#25665=CARTESIAN_POINT('Ctrl Pts',(4.64999999999999,65.9210526315789,8.05403625519526));
#25666=CARTESIAN_POINT('Ctrl Pts',(2.49192748960944,66.1184210526316,9.29999999999996));
#25667=CARTESIAN_POINT('Ctrl Pts',(7.71912721710404E-28,66.3157894736842,
9.29999999999999));
#25668=CARTESIAN_POINT('Ctrl Pts',(-2.49192748960943,66.5131578947368,9.29999999999998));
#25669=CARTESIAN_POINT('Ctrl Pts',(-4.64999999999999,66.7105263157895,8.05403625519526));
#25670=CARTESIAN_POINT('Ctrl Pts',(-6.80807251039055,66.9078947368421,6.80807251039055));
#25671=CARTESIAN_POINT('Ctrl Pts',(-8.05403625519526,67.1052631578947,4.65));
#25672=CARTESIAN_POINT('Ctrl Pts',(-9.29999999999998,67.3026315789474,2.49192748960944));
#25673=CARTESIAN_POINT('Ctrl Pts',(-9.29999999999998,67.5,5.69460761603617E-16));
#25674=CARTESIAN_POINT('Ctrl Pts',(-9.29999999999998,67.6973684210526,-2.49192748960943));
#25675=CARTESIAN_POINT('Ctrl Pts',(-8.05403625519526,67.8947368421053,-4.64999999999998));
#25676=CARTESIAN_POINT('Ctrl Pts',(-6.80807251039055,68.0921052631578,-6.80807251039055));
#25677=CARTESIAN_POINT('Ctrl Pts',(-4.64999999999999,68.2894736842105,-8.05403625519525));
#25678=CARTESIAN_POINT('Ctrl Pts',(-2.49192748960944,68.4868421052632,-9.29999999999998));
#25679=CARTESIAN_POINT('Ctrl Pts',(-1.13892152320634E-15,68.6842105263158,
-9.29999999999998));
#25680=CARTESIAN_POINT('Ctrl Pts',(2.49192748960943,68.8815789473684,-9.29999999999998));
#25681=CARTESIAN_POINT('Ctrl Pts',(4.64999999999999,69.078947368421,-8.05403625519526));
#25682=CARTESIAN_POINT('Ctrl Pts',(6.80807251039055,69.2763157894736,-6.80807251039055));
#25683=CARTESIAN_POINT('Ctrl Pts',(8.05403625519526,69.4736842105263,-4.64999999999999));
#25684=CARTESIAN_POINT('Ctrl Pts',(9.29999999999998,69.6710526315789,-2.49192748960944));
#25685=CARTESIAN_POINT('Ctrl Pts',(9.29999999999998,69.8684210526316,-1.70838228480927E-15));
#25686=CARTESIAN_POINT('Ctrl Pts',(9.29999999999998,70.0657894736842,2.49192748960943));
#25687=CARTESIAN_POINT('Ctrl Pts',(8.05403625519526,70.2631578947368,4.64999999999998));
#25688=CARTESIAN_POINT('Ctrl Pts',(6.80807251039055,70.4605263157895,6.80807251039055));
#25689=CARTESIAN_POINT('Ctrl Pts',(4.64999999999999,70.6578947368421,8.05403625519526));
#25690=CARTESIAN_POINT('Ctrl Pts',(2.49192748960944,70.8552631578948,9.29999999999998));
#25691=CARTESIAN_POINT('Ctrl Pts',(8.28920248064266E-28,71.0526315789473,
9.29999999999998));
#25692=CARTESIAN_POINT('Ctrl Pts',(-2.49192748960943,71.25,9.29999999999998));
#25693=CARTESIAN_POINT('Ctrl Pts',(-4.64999999999999,71.4473684210526,8.05403625519526));
#25694=CARTESIAN_POINT('Ctrl Pts',(-6.80807251039055,71.6447368421052,6.80807251039055));
#25695=CARTESIAN_POINT('Ctrl Pts',(-8.05403625519526,71.8421052631578,4.65));
#25696=CARTESIAN_POINT('Ctrl Pts',(-9.29999999999998,72.0394736842105,2.49192748960944));
#25697=CARTESIAN_POINT('Ctrl Pts',(-9.29999999999998,72.2368421052632,5.69460761604209E-16));
#25698=CARTESIAN_POINT('Ctrl Pts',(-9.29999999999998,72.4342105263157,-2.49192748960943));
#25699=CARTESIAN_POINT('Ctrl Pts',(-8.05403625519526,72.6315789473684,-4.64999999999998));
#25700=CARTESIAN_POINT('Ctrl Pts',(-6.80807251039055,72.828947368421,-6.80807251039055));
#25701=CARTESIAN_POINT('Ctrl Pts',(-4.64999999999999,73.0263157894737,-8.05403625519526));
#25702=CARTESIAN_POINT('Ctrl Pts',(-2.49192748960944,73.2236842105263,-9.29999999999998));
#25703=CARTESIAN_POINT('Ctrl Pts',(-1.13892152320628E-15,73.4210526315789,
-9.29999999999998));
#25704=CARTESIAN_POINT('Ctrl Pts',(2.49192748960943,73.6184210526315,-9.29999999999998));
#25705=CARTESIAN_POINT('Ctrl Pts',(4.64999999999999,73.8157894736842,-8.05403625519526));
#25706=CARTESIAN_POINT('Ctrl Pts',(6.80807251039055,74.0131578947368,-6.80807251039056));
#25707=CARTESIAN_POINT('Ctrl Pts',(8.05403625519526,74.2105263157895,-4.64999999999999));
#25708=CARTESIAN_POINT('Ctrl Pts',(9.29999999999998,74.4078947368421,-2.49192748960944));
#25709=CARTESIAN_POINT('Ctrl Pts',(9.29999999999998,74.6052631578947,-1.70838228480937E-15));
#25710=CARTESIAN_POINT('Ctrl Pts',(9.29999999999998,74.8026315789473,2.49192748960943));
#25711=CARTESIAN_POINT('Ctrl Pts',(8.05403625519526,75.,4.64999999999998));
#25712=CARTESIAN_POINT('Ctrl Pts',(6.80807251039055,75.1973684210526,6.80807251039055));
#25713=CARTESIAN_POINT('Ctrl Pts',(4.64999999999999,75.3947368421053,8.05403625519526));
#25714=CARTESIAN_POINT('Ctrl Pts',(2.49192748960944,75.5921052631579,9.29999999999998));
#25715=CARTESIAN_POINT('Ctrl Pts',(8.87468518373638E-28,75.7894736842105,
9.29999999999998));
#25716=CARTESIAN_POINT('Ctrl Pts',(-2.49192748960943,75.9868421052632,9.29999999999997));
#25717=CARTESIAN_POINT('Ctrl Pts',(-4.64999999999999,76.1842105263158,8.05403625519527));
#25718=CARTESIAN_POINT('Ctrl Pts',(-6.80807251039055,76.3815789473684,6.80807251039055));
#25719=CARTESIAN_POINT('Ctrl Pts',(-8.05403625519526,76.578947368421,4.65));
#25720=CARTESIAN_POINT('Ctrl Pts',(-9.29999999999998,76.7763157894737,2.49192748960944));
#25721=CARTESIAN_POINT('Ctrl Pts',(-9.29999999999998,76.9736842105263,5.69460761603519E-16));
#25722=CARTESIAN_POINT('Ctrl Pts',(-9.29999999999998,77.1710526315789,-2.49192748960943));
#25723=CARTESIAN_POINT('Ctrl Pts',(-8.05403625519526,77.3684210526316,-4.64999999999998));
#25724=CARTESIAN_POINT('Ctrl Pts',(-6.80807251039055,77.5657894736842,-6.80807251039055));
#25725=CARTESIAN_POINT('Ctrl Pts',(-4.64999999999999,77.7631578947368,-8.05403625519525));
#25726=CARTESIAN_POINT('Ctrl Pts',(-2.49192748960944,77.9605263157894,-9.29999999999999));
#25727=CARTESIAN_POINT('Ctrl Pts',(-1.13892152320623E-15,78.1578947368421,
-9.29999999999997));
#25728=CARTESIAN_POINT('Ctrl Pts',(2.49192748960943,78.3552631578947,-9.29999999999998));
#25729=CARTESIAN_POINT('Ctrl Pts',(4.64999999999999,78.5526315789473,-8.05403625519526));
#25730=CARTESIAN_POINT('Ctrl Pts',(6.80807251039055,78.75,-6.80807251039055));
#25731=CARTESIAN_POINT('Ctrl Pts',(8.05403625519526,78.9473684210526,-4.64999999999999));
#25732=CARTESIAN_POINT('Ctrl Pts',(9.29999999999998,79.1447368421052,-2.49192748960944));
#25733=CARTESIAN_POINT('Ctrl Pts',(9.29999999999998,79.3421052631579,-1.70838228480937E-15));
#25734=CARTESIAN_POINT('Ctrl Pts',(9.29999999999998,79.5394736842105,2.49192748960943));
#25735=CARTESIAN_POINT('Ctrl Pts',(8.05403625519526,79.7368421052631,4.64999999999998));
#25736=CARTESIAN_POINT('Ctrl Pts',(6.80807251039055,79.9342105263157,6.80807251039054));
#25737=CARTESIAN_POINT('Ctrl Pts',(4.64999999999999,80.1315789473684,8.05403625519526));
#25738=CARTESIAN_POINT('Ctrl Pts',(2.49192748960944,80.328947368421,9.29999999999998));
#25739=CARTESIAN_POINT('Ctrl Pts',(9.33690837038932E-28,80.5263157894737,
9.29999999999998));
#25740=CARTESIAN_POINT('Ctrl Pts',(-2.49192748960943,80.7236842105263,9.29999999999998));
#25741=CARTESIAN_POINT('Ctrl Pts',(-4.64999999999999,80.9210526315789,8.05403625519526));
#25742=CARTESIAN_POINT('Ctrl Pts',(-6.80807251039055,81.1184210526315,6.80807251039055));
#25743=CARTESIAN_POINT('Ctrl Pts',(-8.05403625519526,81.3157894736842,4.65));
#25744=CARTESIAN_POINT('Ctrl Pts',(-9.29999999999998,81.5131578947368,2.49192748960944));
#25745=CARTESIAN_POINT('Ctrl Pts',(-9.29999999999998,81.7105263157895,5.69460761604603E-16));
#25746=CARTESIAN_POINT('Ctrl Pts',(-9.29999999999998,81.9078947368421,-2.49192748960943));
#25747=CARTESIAN_POINT('Ctrl Pts',(-8.05403625519526,82.1052631578948,-4.64999999999998));
#25748=CARTESIAN_POINT('Ctrl Pts',(-6.80807251039055,82.3026315789473,-6.80807251039055));
#25749=CARTESIAN_POINT('Ctrl Pts',(-4.64999999999999,82.5,-8.05403625519526));
#25750=CARTESIAN_POINT('Ctrl Pts',(-2.49192748960944,82.6973684210527,-9.29999999999998));
#25751=CARTESIAN_POINT('Ctrl Pts',(-1.13892152320618E-15,82.8947368421053,
-9.29999999999998));
#25752=CARTESIAN_POINT('Ctrl Pts',(2.49192748960943,83.0921052631579,-9.29999999999999));
#25753=CARTESIAN_POINT('Ctrl Pts',(4.64999999999999,83.2894736842105,-8.05403625519526));
#25754=CARTESIAN_POINT('Ctrl Pts',(6.80807251039055,83.4868421052631,-6.80807251039056));
#25755=CARTESIAN_POINT('Ctrl Pts',(8.05403625519526,83.6842105263158,-4.64999999999999));
#25756=CARTESIAN_POINT('Ctrl Pts',(9.29999999999998,83.8815789473684,-2.49192748960945));
#25757=CARTESIAN_POINT('Ctrl Pts',(9.29999999999998,84.078947368421,-1.70838228480937E-15));
#25758=CARTESIAN_POINT('Ctrl Pts',(9.29999999999998,84.2763157894737,2.49192748960943));
#25759=CARTESIAN_POINT('Ctrl Pts',(8.05403625519526,84.4736842105263,4.64999999999998));
#25760=CARTESIAN_POINT('Ctrl Pts',(6.80807251039055,84.6710526315789,6.80807251039055));
#25761=CARTESIAN_POINT('Ctrl Pts',(4.64999999999999,84.8684210526316,8.05403625519526));
#25762=CARTESIAN_POINT('Ctrl Pts',(2.49192748960944,85.0657894736842,9.29999999999998));
#25763=CARTESIAN_POINT('Ctrl Pts',(9.87616875481775E-28,85.2631578947368,
9.29999999999998));
#25764=CARTESIAN_POINT('Ctrl Pts',(-2.49192748960943,85.4605263157894,9.29999999999998));
#25765=CARTESIAN_POINT('Ctrl Pts',(-4.64999999999999,85.6578947368421,8.05403625519527));
#25766=CARTESIAN_POINT('Ctrl Pts',(-6.80807251039055,85.8552631578947,6.80807251039054));
#25767=CARTESIAN_POINT('Ctrl Pts',(-8.05403625519526,86.0526315789474,4.65));
#25768=CARTESIAN_POINT('Ctrl Pts',(-9.29999999999998,86.25,2.49192748960944));
#25769=CARTESIAN_POINT('Ctrl Pts',(-9.29999999999998,86.4473684210526,5.6946076160411E-16));
#25770=CARTESIAN_POINT('Ctrl Pts',(-9.29999999999998,86.6447368421052,-2.49192748960943));
#25771=CARTESIAN_POINT('Ctrl Pts',(-8.05403625519526,86.8421052631579,-4.64999999999998));
#25772=CARTESIAN_POINT('Ctrl Pts',(-6.80807251039055,87.0394736842105,-6.80807251039055));
#25773=CARTESIAN_POINT('Ctrl Pts',(-4.64999999999999,87.2368421052631,-8.05403625519526));
#25774=CARTESIAN_POINT('Ctrl Pts',(-2.49192748960944,87.4342105263158,-9.29999999999998));
#25775=CARTESIAN_POINT('Ctrl Pts',(-1.13892152320613E-15,87.6315789473684,
-9.29999999999997));
#25776=CARTESIAN_POINT('Ctrl Pts',(2.49192748960943,87.828947368421,-9.29999999999998));
#25777=CARTESIAN_POINT('Ctrl Pts',(4.64999999999999,88.0263157894737,-8.05403625519526));
#25778=CARTESIAN_POINT('Ctrl Pts',(6.80807251039055,88.2236842105263,-6.80807251039055));
#25779=CARTESIAN_POINT('Ctrl Pts',(8.05403625519526,88.4210526315789,-4.64999999999999));
#25780=CARTESIAN_POINT('Ctrl Pts',(9.29999999999998,88.6184210526315,-2.49192748960944));
#25781=CARTESIAN_POINT('Ctrl Pts',(9.29999999999998,88.8157894736842,-1.70838228480927E-15));
#25782=CARTESIAN_POINT('Ctrl Pts',(9.29999999999998,89.0131578947368,2.49192748960943));
#25783=CARTESIAN_POINT('Ctrl Pts',(8.05403625519526,89.2105263157894,4.64999999999999));
#25784=CARTESIAN_POINT('Ctrl Pts',(6.80807251039055,89.4078947368421,6.80807251039054));
#25785=CARTESIAN_POINT('Ctrl Pts',(4.64999999999999,89.6052631578947,8.05403625519527));
#25786=CARTESIAN_POINT('Ctrl Pts',(2.49192748960944,89.8026315789473,9.29999999999996));
#25787=CARTESIAN_POINT('Ctrl Pts',(1.03537993810258E-27,90.,9.29999999999998));
#25788=CARTESIAN_POINT('Ctrl Pts',(6.93334779979405E-30,-4.00000000000002,
9.29999999999999));
#25789=CARTESIAN_POINT('Ctrl Pts',(-2.49192748960944,-3.80263157894737,
9.29999999999998));
#25790=CARTESIAN_POINT('Ctrl Pts',(-4.64999999999999,-3.60526315789474,
8.05403625519527));
#25791=CARTESIAN_POINT('Ctrl Pts',(-6.80807251039054,-3.40789473684211,
6.80807251039054));
#25792=CARTESIAN_POINT('Ctrl Pts',(-8.05403625519527,-3.21052631578946,
4.64999999999999));
#25793=CARTESIAN_POINT('Ctrl Pts',(-9.29999999999998,-3.01315789473685,
2.49192748960944));
#25794=CARTESIAN_POINT('Ctrl Pts',(-9.29999999999999,-2.81578947368422,
5.69460761603572E-16));
#25795=CARTESIAN_POINT('Ctrl Pts',(-9.29999999999998,-2.61842105263159,
-2.49192748960943));
#25796=CARTESIAN_POINT('Ctrl Pts',(-8.05403625519527,-2.42105263157898,
-4.64999999999999));
#25797=CARTESIAN_POINT('Ctrl Pts',(-6.80807251039054,-2.22368421052628,
-6.80807251039054));
#25798=CARTESIAN_POINT('Ctrl Pts',(-4.65,-2.02631578947365,-8.05403625519526));
#25799=CARTESIAN_POINT('Ctrl Pts',(-2.49192748960944,-1.82894736842106,
-9.29999999999998));
#25800=CARTESIAN_POINT('Ctrl Pts',(-1.13892152320711E-15,-1.63157894736841,
-9.29999999999999));
#25801=CARTESIAN_POINT('Ctrl Pts',(2.49192748960943,-1.43421052631576,-9.29999999999999));
#25802=CARTESIAN_POINT('Ctrl Pts',(4.64999999999999,-1.23684210526313,-8.05403625519527));
#25803=CARTESIAN_POINT('Ctrl Pts',(6.80807251039054,-1.0394736842105,-6.80807251039055));
#25804=CARTESIAN_POINT('Ctrl Pts',(8.05403625519526,-0.842105263157894,
-4.65));
#25805=CARTESIAN_POINT('Ctrl Pts',(9.29999999999998,-0.644736842105277,
-2.49192748960945));
#25806=CARTESIAN_POINT('Ctrl Pts',(9.29999999999999,-0.447368421052613,
-1.70838228481055E-15));
#25807=CARTESIAN_POINT('Ctrl Pts',(9.29999999999999,-0.249999999999972,
2.49192748960943));
#25808=CARTESIAN_POINT('Ctrl Pts',(8.05403625519527,-0.0526315789473736,
4.64999999999998));
#25809=CARTESIAN_POINT('Ctrl Pts',(6.80807251039055,0.144736842105247,6.80807251039054));
#25810=CARTESIAN_POINT('Ctrl Pts',(4.65,0.342105263157866,8.05403625519526));
#25811=CARTESIAN_POINT('Ctrl Pts',(2.49192748960945,0.539473684210509,9.29999999999998));
#25812=CARTESIAN_POINT('Ctrl Pts',(6.24001301981464E-29,0.736842105263147,
9.29999999999999));
#25813=CARTESIAN_POINT('Ctrl Pts',(-2.49192748960944,0.934210526315771,
9.29999999999998));
#25814=CARTESIAN_POINT('Ctrl Pts',(-4.64999999999999,1.13157894736839,8.05403625519527));
#25815=CARTESIAN_POINT('Ctrl Pts',(-6.80807251039054,1.32894736842103,6.80807251039054));
#25816=CARTESIAN_POINT('Ctrl Pts',(-8.05403625519527,1.52631578947371,4.64999999999999));
#25817=CARTESIAN_POINT('Ctrl Pts',(-9.29999999999998,1.72368421052634,2.49192748960944));
#25818=CARTESIAN_POINT('Ctrl Pts',(-9.29999999999999,1.92105263157895,5.69460761603572E-16));
#25819=CARTESIAN_POINT('Ctrl Pts',(-9.29999999999998,2.11842105263156,-2.49192748960944));
#25820=CARTESIAN_POINT('Ctrl Pts',(-8.05403625519527,2.31578947368419,-4.64999999999999));
#25821=CARTESIAN_POINT('Ctrl Pts',(-6.80807251039054,2.51315789473686,-6.80807251039054));
#25822=CARTESIAN_POINT('Ctrl Pts',(-4.65,2.71052631578947,-8.05403625519526));
#25823=CARTESIAN_POINT('Ctrl Pts',(-2.49192748960944,2.90789473684212,-9.29999999999998));
#25824=CARTESIAN_POINT('Ctrl Pts',(-1.13892152320705E-15,3.10526315789475,
-9.29999999999998));
#25825=CARTESIAN_POINT('Ctrl Pts',(2.49192748960943,3.30263157894739,-9.29999999999999));
#25826=CARTESIAN_POINT('Ctrl Pts',(4.64999999999999,3.50000000000003,-8.05403625519526));
#25827=CARTESIAN_POINT('Ctrl Pts',(6.80807251039054,3.69736842105265,-6.80807251039055));
#25828=CARTESIAN_POINT('Ctrl Pts',(8.05403625519526,3.89473684210523,-4.65));
#25829=CARTESIAN_POINT('Ctrl Pts',(9.29999999999998,4.09210526315787,-2.49192748960944));
#25830=CARTESIAN_POINT('Ctrl Pts',(9.29999999999999,4.28947368421051,-1.7083822848107E-15));
#25831=CARTESIAN_POINT('Ctrl Pts',(9.29999999999999,4.48684210526317,2.49192748960943));
#25832=CARTESIAN_POINT('Ctrl Pts',(8.05403625519527,4.68421052631579,4.64999999999999));
#25833=CARTESIAN_POINT('Ctrl Pts',(6.80807251039055,4.88157894736839,6.80807251039054));
#25834=CARTESIAN_POINT('Ctrl Pts',(4.65,5.07894736842103,8.05403625519526));
#25835=CARTESIAN_POINT('Ctrl Pts',(2.49192748960945,5.27631578947365,9.29999999999998));
#25836=CARTESIAN_POINT('Ctrl Pts',(1.10933564796705E-28,5.47368421052631,
9.29999999999999));
#25837=CARTESIAN_POINT('Ctrl Pts',(-2.49192748960944,5.67105263157892,9.29999999999998));
#25838=CARTESIAN_POINT('Ctrl Pts',(-4.64999999999999,5.86842105263155,8.05403625519527));
#25839=CARTESIAN_POINT('Ctrl Pts',(-6.80807251039054,6.06578947368418,6.80807251039054));
#25840=CARTESIAN_POINT('Ctrl Pts',(-8.05403625519527,6.26315789473687,4.64999999999999));
#25841=CARTESIAN_POINT('Ctrl Pts',(-9.29999999999998,6.46052631578948,2.49192748960944));
#25842=CARTESIAN_POINT('Ctrl Pts',(-9.29999999999999,6.65789473684211,5.69460761603572E-16));
#25843=CARTESIAN_POINT('Ctrl Pts',(-9.29999999999998,6.85526315789475,-2.49192748960944));
#25844=CARTESIAN_POINT('Ctrl Pts',(-8.05403625519527,7.05263157894735,-4.64999999999999));
#25845=CARTESIAN_POINT('Ctrl Pts',(-6.80807251039054,7.25000000000001,-6.80807251039054));
#25846=CARTESIAN_POINT('Ctrl Pts',(-4.65,7.44736842105263,-8.05403625519526));
#25847=CARTESIAN_POINT('Ctrl Pts',(-2.49192748960944,7.64473684210527,-9.29999999999998));
#25848=CARTESIAN_POINT('Ctrl Pts',(-1.138921523207E-15,7.84210526315791,
-9.29999999999999));
#25849=CARTESIAN_POINT('Ctrl Pts',(2.49192748960943,8.03947368421053,-9.29999999999999));
#25850=CARTESIAN_POINT('Ctrl Pts',(4.64999999999999,8.23684210526315,-8.05403625519527));
#25851=CARTESIAN_POINT('Ctrl Pts',(6.80807251039054,8.43421052631579,-6.80807251039055));
#25852=CARTESIAN_POINT('Ctrl Pts',(8.05403625519526,8.63157894736839,-4.65));
#25853=CARTESIAN_POINT('Ctrl Pts',(9.29999999999998,8.82894736842105,-2.49192748960944));
#25854=CARTESIAN_POINT('Ctrl Pts',(9.29999999999999,9.02631578947367,-1.7083822848107E-15));
#25855=CARTESIAN_POINT('Ctrl Pts',(9.29999999999999,9.22368421052632,2.49192748960943));
#25856=CARTESIAN_POINT('Ctrl Pts',(8.05403625519527,9.42105263157895,4.64999999999998));
#25857=CARTESIAN_POINT('Ctrl Pts',(6.80807251039055,9.61842105263154,6.80807251039054));
#25858=CARTESIAN_POINT('Ctrl Pts',(4.65,9.81578947368419,8.05403625519527));
#25859=CARTESIAN_POINT('Ctrl Pts',(2.49192748960945,10.0131578947368,9.29999999999998));
#25860=CARTESIAN_POINT('Ctrl Pts',(1.60622557361895E-28,10.2105263157895,
9.29999999999999));
#25861=CARTESIAN_POINT('Ctrl Pts',(-2.49192748960944,10.4078947368421,9.29999999999998));
#25862=CARTESIAN_POINT('Ctrl Pts',(-4.64999999999999,10.6052631578947,8.05403625519527));
#25863=CARTESIAN_POINT('Ctrl Pts',(-6.80807251039054,10.8026315789474,6.80807251039054));
#25864=CARTESIAN_POINT('Ctrl Pts',(-8.05403625519527,11.,4.64999999999999));
#25865=CARTESIAN_POINT('Ctrl Pts',(-9.29999999999998,11.1973684210526,2.49192748960944));
#25866=CARTESIAN_POINT('Ctrl Pts',(-9.29999999999999,11.3947368421053,5.69460761603572E-16));
#25867=CARTESIAN_POINT('Ctrl Pts',(-9.29999999999998,11.5921052631579,-2.49192748960944));
#25868=CARTESIAN_POINT('Ctrl Pts',(-8.05403625519527,11.7894736842105,-4.64999999999999));
#25869=CARTESIAN_POINT('Ctrl Pts',(-6.80807251039054,11.9868421052632,-6.80807251039054));
#25870=CARTESIAN_POINT('Ctrl Pts',(-4.65,12.1842105263158,-8.05403625519526));
#25871=CARTESIAN_POINT('Ctrl Pts',(-2.49192748960944,12.3815789473684,-9.29999999999998));
#25872=CARTESIAN_POINT('Ctrl Pts',(-1.13892152320695E-15,12.5789473684211,
-9.29999999999999));
#25873=CARTESIAN_POINT('Ctrl Pts',(2.49192748960943,12.7763157894737,-9.29999999999999));
#25874=CARTESIAN_POINT('Ctrl Pts',(4.64999999999999,12.9736842105263,-8.05403625519527));
#25875=CARTESIAN_POINT('Ctrl Pts',(6.80807251039054,13.171052631579,-6.80807251039055));
#25876=CARTESIAN_POINT('Ctrl Pts',(8.05403625519526,13.3684210526316,-4.65));
#25877=CARTESIAN_POINT('Ctrl Pts',(9.29999999999998,13.5657894736842,-2.49192748960944));
#25878=CARTESIAN_POINT('Ctrl Pts',(9.29999999999999,13.7631578947368,-1.7083822848107E-15));
#25879=CARTESIAN_POINT('Ctrl Pts',(9.29999999999999,13.9605263157895,2.49192748960943));
#25880=CARTESIAN_POINT('Ctrl Pts',(8.05403625519527,14.1578947368421,4.64999999999999));
#25881=CARTESIAN_POINT('Ctrl Pts',(6.80807251039055,14.3552631578947,6.80807251039054));
#25882=CARTESIAN_POINT('Ctrl Pts',(4.65,14.5526315789474,8.05403625519526));
#25883=CARTESIAN_POINT('Ctrl Pts',(2.49192748960945,14.75,9.29999999999998));
#25884=CARTESIAN_POINT('Ctrl Pts',(2.14933781793615E-28,14.9473684210526,
9.29999999999999));
#25885=CARTESIAN_POINT('Ctrl Pts',(-2.49192748960944,15.1447368421053,9.29999999999998));
#25886=CARTESIAN_POINT('Ctrl Pts',(-4.64999999999999,15.3421052631579,8.05403625519527));
#25887=CARTESIAN_POINT('Ctrl Pts',(-6.80807251039054,15.5394736842105,6.80807251039054));
#25888=CARTESIAN_POINT('Ctrl Pts',(-8.05403625519527,15.7368421052632,4.64999999999999));
#25889=CARTESIAN_POINT('Ctrl Pts',(-9.29999999999998,15.9342105263158,2.49192748960944));
#25890=CARTESIAN_POINT('Ctrl Pts',(-9.29999999999999,16.1315789473684,5.69460761603425E-16));
#25891=CARTESIAN_POINT('Ctrl Pts',(-9.29999999999998,16.328947368421,-2.49192748960944));
#25892=CARTESIAN_POINT('Ctrl Pts',(-8.05403625519527,16.5263157894737,-4.64999999999999));
#25893=CARTESIAN_POINT('Ctrl Pts',(-6.80807251039054,16.7236842105263,-6.80807251039054));
#25894=CARTESIAN_POINT('Ctrl Pts',(-4.65,16.921052631579,-8.05403625519526));
#25895=CARTESIAN_POINT('Ctrl Pts',(-2.49192748960944,17.1184210526316,-9.29999999999998));
#25896=CARTESIAN_POINT('Ctrl Pts',(-1.1389215232069E-15,17.3157894736842,
-9.29999999999998));
#25897=CARTESIAN_POINT('Ctrl Pts',(2.49192748960943,17.5131578947369,-9.29999999999999));
#25898=CARTESIAN_POINT('Ctrl Pts',(4.64999999999999,17.7105263157895,-8.05403625519527));
#25899=CARTESIAN_POINT('Ctrl Pts',(6.80807251039054,17.9078947368421,-6.80807251039055));
#25900=CARTESIAN_POINT('Ctrl Pts',(8.05403625519526,18.1052631578947,-4.65));
#25901=CARTESIAN_POINT('Ctrl Pts',(9.29999999999998,18.3026315789473,-2.49192748960944));
#25902=CARTESIAN_POINT('Ctrl Pts',(9.29999999999999,18.5,-1.70838228481055E-15));
#25903=CARTESIAN_POINT('Ctrl Pts',(9.29999999999999,18.6973684210526,2.49192748960943));
#25904=CARTESIAN_POINT('Ctrl Pts',(8.05403625519527,18.8947368421053,4.64999999999998));
#25905=CARTESIAN_POINT('Ctrl Pts',(6.80807251039055,19.0921052631579,6.80807251039054));
#25906=CARTESIAN_POINT('Ctrl Pts',(4.65,19.2894736842105,8.05403625519526));
#25907=CARTESIAN_POINT('Ctrl Pts',(2.49192748960945,19.4868421052631,9.29999999999998));
#25908=CARTESIAN_POINT('Ctrl Pts',(2.70400564191968E-28,19.6842105263158,
9.29999999999999));
#25909=CARTESIAN_POINT('Ctrl Pts',(-2.49192748960944,19.8815789473684,9.29999999999998));
#25910=CARTESIAN_POINT('Ctrl Pts',(-4.64999999999999,20.078947368421,8.05403625519527));
#25911=CARTESIAN_POINT('Ctrl Pts',(-6.80807251039054,20.2763157894737,6.80807251039055));
#25912=CARTESIAN_POINT('Ctrl Pts',(-8.05403625519527,20.4736842105263,4.64999999999999));
#25913=CARTESIAN_POINT('Ctrl Pts',(-9.29999999999998,20.671052631579,2.49192748960944));
#25914=CARTESIAN_POINT('Ctrl Pts',(-9.29999999999999,20.8684210526316,5.69460761603572E-16));
#25915=CARTESIAN_POINT('Ctrl Pts',(-9.29999999999998,21.0657894736842,-2.49192748960943));
#25916=CARTESIAN_POINT('Ctrl Pts',(-8.05403625519527,21.2631578947368,-4.64999999999999));
#25917=CARTESIAN_POINT('Ctrl Pts',(-6.80807251039054,21.4605263157895,-6.80807251039054));
#25918=CARTESIAN_POINT('Ctrl Pts',(-4.65,21.6578947368421,-8.05403625519526));
#25919=CARTESIAN_POINT('Ctrl Pts',(-2.49192748960944,21.8552631578947,-9.29999999999998));
#25920=CARTESIAN_POINT('Ctrl Pts',(-1.13892152320684E-15,22.0526315789474,
-9.29999999999999));
#25921=CARTESIAN_POINT('Ctrl Pts',(2.49192748960943,22.25,-9.29999999999999));
#25922=CARTESIAN_POINT('Ctrl Pts',(4.64999999999999,22.4473684210526,-8.05403625519526));
#25923=CARTESIAN_POINT('Ctrl Pts',(6.80807251039054,22.6447368421053,-6.80807251039055));
#25924=CARTESIAN_POINT('Ctrl Pts',(8.05403625519526,22.8421052631579,-4.65));
#25925=CARTESIAN_POINT('Ctrl Pts',(9.29999999999998,23.0394736842105,-2.49192748960944));
#25926=CARTESIAN_POINT('Ctrl Pts',(9.29999999999999,23.2368421052632,-1.70838228481055E-15));
#25927=CARTESIAN_POINT('Ctrl Pts',(9.29999999999999,23.4342105263158,2.49192748960943));
#25928=CARTESIAN_POINT('Ctrl Pts',(8.05403625519527,23.6315789473684,4.64999999999998));
#25929=CARTESIAN_POINT('Ctrl Pts',(6.80807251039055,23.828947368421,6.80807251039054));
#25930=CARTESIAN_POINT('Ctrl Pts',(4.65,24.0263157894736,8.05403625519526));
#25931=CARTESIAN_POINT('Ctrl Pts',(2.49192748960945,24.2236842105263,9.29999999999998));
#25932=CARTESIAN_POINT('Ctrl Pts',(3.16622882857262E-28,24.4210526315789,
9.29999999999999));
#25933=CARTESIAN_POINT('Ctrl Pts',(-2.49192748960944,24.6184210526316,9.29999999999998));
#25934=CARTESIAN_POINT('Ctrl Pts',(-4.64999999999999,24.8157894736842,8.05403625519527));
#25935=CARTESIAN_POINT('Ctrl Pts',(-6.80807251039054,25.0131578947368,6.80807251039054));
#25936=CARTESIAN_POINT('Ctrl Pts',(-8.05403625519527,25.2105263157895,4.64999999999999));
#25937=CARTESIAN_POINT('Ctrl Pts',(-9.29999999999998,25.4078947368421,2.49192748960944));
#25938=CARTESIAN_POINT('Ctrl Pts',(-9.29999999999999,25.6052631578947,5.69460761603572E-16));
#25939=CARTESIAN_POINT('Ctrl Pts',(-9.29999999999998,25.8026315789474,-2.49192748960943));
#25940=CARTESIAN_POINT('Ctrl Pts',(-8.05403625519527,26.,-4.64999999999999));
#25941=CARTESIAN_POINT('Ctrl Pts',(-6.80807251039054,26.1973684210526,-6.80807251039054));
#25942=CARTESIAN_POINT('Ctrl Pts',(-4.65,26.3947368421053,-8.05403625519526));
#25943=CARTESIAN_POINT('Ctrl Pts',(-2.49192748960944,26.5921052631579,-9.29999999999998));
#25944=CARTESIAN_POINT('Ctrl Pts',(-1.13892152320679E-15,26.7894736842105,
-9.29999999999999));
#25945=CARTESIAN_POINT('Ctrl Pts',(2.49192748960943,26.9868421052632,-9.29999999999999));
#25946=CARTESIAN_POINT('Ctrl Pts',(4.64999999999999,27.1842105263158,-8.05403625519527));
#25947=CARTESIAN_POINT('Ctrl Pts',(6.80807251039054,27.3815789473685,-6.80807251039055));
#25948=CARTESIAN_POINT('Ctrl Pts',(8.05403625519526,27.578947368421,-4.65));
#25949=CARTESIAN_POINT('Ctrl Pts',(9.29999999999998,27.7763157894737,-2.49192748960944));
#25950=CARTESIAN_POINT('Ctrl Pts',(9.29999999999999,27.9736842105263,-1.70838228481055E-15));
#25951=CARTESIAN_POINT('Ctrl Pts',(9.29999999999999,28.1710526315789,2.49192748960943));
#25952=CARTESIAN_POINT('Ctrl Pts',(8.05403625519527,28.3684210526316,4.64999999999999));
#25953=CARTESIAN_POINT('Ctrl Pts',(6.80807251039055,28.5657894736842,6.80807251039054));
#25954=CARTESIAN_POINT('Ctrl Pts',(4.65,28.7631578947368,8.05403625519526));
#25955=CARTESIAN_POINT('Ctrl Pts',(2.49192748960945,28.9605263157895,9.29999999999998));
#25956=CARTESIAN_POINT('Ctrl Pts',(3.67467433389085E-28,29.1578947368421,
9.29999999999999));
#25957=CARTESIAN_POINT('Ctrl Pts',(-2.49192748960944,29.3552631578947,9.29999999999998));
#25958=CARTESIAN_POINT('Ctrl Pts',(-4.64999999999999,29.5526315789473,8.05403625519527));
#25959=CARTESIAN_POINT('Ctrl Pts',(-6.80807251039054,29.7499999999999,6.80807251039054));
#25960=CARTESIAN_POINT('Ctrl Pts',(-8.05403625519527,29.9473684210527,4.64999999999999));
#25961=CARTESIAN_POINT('Ctrl Pts',(-9.29999999999998,30.1447368421053,2.49192748960944));
#25962=CARTESIAN_POINT('Ctrl Pts',(-9.29999999999999,30.3421052631579,5.69460761603572E-16));
#25963=CARTESIAN_POINT('Ctrl Pts',(-9.29999999999998,30.5394736842105,-2.49192748960943));
#25964=CARTESIAN_POINT('Ctrl Pts',(-8.05403625519527,30.7368421052631,-4.64999999999999));
#25965=CARTESIAN_POINT('Ctrl Pts',(-6.80807251039054,30.9342105263159,-6.80807251039054));
#25966=CARTESIAN_POINT('Ctrl Pts',(-4.65,31.1315789473685,-8.05403625519526));
#25967=CARTESIAN_POINT('Ctrl Pts',(-2.49192748960944,31.3289473684211,-9.29999999999998));
#25968=CARTESIAN_POINT('Ctrl Pts',(-1.13892152320674E-15,31.5263157894737,
-9.29999999999999));
#25969=CARTESIAN_POINT('Ctrl Pts',(2.49192748960943,31.7236842105263,-9.29999999999999));
#25970=CARTESIAN_POINT('Ctrl Pts',(4.64999999999999,31.921052631579,-8.05403625519527));
#25971=CARTESIAN_POINT('Ctrl Pts',(6.80807251039054,32.1184210526316,-6.80807251039055));
#25972=CARTESIAN_POINT('Ctrl Pts',(8.05403625519526,32.3157894736842,-4.65));
#25973=CARTESIAN_POINT('Ctrl Pts',(9.29999999999998,32.5131578947368,-2.49192748960945));
#25974=CARTESIAN_POINT('Ctrl Pts',(9.29999999999999,32.7105263157895,-1.7083822848107E-15));
#25975=CARTESIAN_POINT('Ctrl Pts',(9.29999999999999,32.9078947368421,2.49192748960943));
#25976=CARTESIAN_POINT('Ctrl Pts',(8.05403625519527,33.1052631578947,4.64999999999998));
#25977=CARTESIAN_POINT('Ctrl Pts',(6.80807251039055,33.3026315789473,6.80807251039054));
#25978=CARTESIAN_POINT('Ctrl Pts',(4.65,33.5,8.05403625519526));
#25979=CARTESIAN_POINT('Ctrl Pts',(2.49192748960945,33.6973684210526,9.29999999999998));
#25980=CARTESIAN_POINT('Ctrl Pts',(4.22934215787437E-28,33.8947368421052,
9.29999999999999));
#25981=CARTESIAN_POINT('Ctrl Pts',(-2.49192748960944,34.0921052631579,9.29999999999998));
#25982=CARTESIAN_POINT('Ctrl Pts',(-4.64999999999999,34.2894736842105,8.05403625519527));
#25983=CARTESIAN_POINT('Ctrl Pts',(-6.80807251039054,34.4868421052631,6.80807251039054));
#25984=CARTESIAN_POINT('Ctrl Pts',(-8.05403625519527,34.6842105263158,4.64999999999999));
#25985=CARTESIAN_POINT('Ctrl Pts',(-9.29999999999998,34.8815789473684,2.49192748960944));
#25986=CARTESIAN_POINT('Ctrl Pts',(-9.29999999999999,35.078947368421,5.69460761603572E-16));
#25987=CARTESIAN_POINT('Ctrl Pts',(-9.29999999999998,35.2763157894737,-2.49192748960943));
#25988=CARTESIAN_POINT('Ctrl Pts',(-8.05403625519527,35.4736842105263,-4.64999999999999));
#25989=CARTESIAN_POINT('Ctrl Pts',(-6.80807251039054,35.671052631579,-6.80807251039054));
#25990=CARTESIAN_POINT('Ctrl Pts',(-4.65,35.8684210526316,-8.05403625519526));
#25991=CARTESIAN_POINT('Ctrl Pts',(-2.49192748960944,36.0657894736842,-9.29999999999998));
#25992=CARTESIAN_POINT('Ctrl Pts',(-1.13892152320669E-15,36.2631578947368,
-9.29999999999998));
#25993=CARTESIAN_POINT('Ctrl Pts',(2.49192748960943,36.4605263157895,-9.29999999999999));
#25994=CARTESIAN_POINT('Ctrl Pts',(4.64999999999999,36.6578947368421,-8.05403625519526));
#25995=CARTESIAN_POINT('Ctrl Pts',(6.80807251039054,36.8552631578947,-6.80807251039055));
#25996=CARTESIAN_POINT('Ctrl Pts',(8.05403625519526,37.0526315789473,-4.65));
#25997=CARTESIAN_POINT('Ctrl Pts',(9.29999999999998,37.25,-2.49192748960945));
#25998=CARTESIAN_POINT('Ctrl Pts',(9.29999999999999,37.4473684210526,-1.70838228481055E-15));
#25999=CARTESIAN_POINT('Ctrl Pts',(9.29999999999999,37.6447368421053,2.49192748960943));
#26000=CARTESIAN_POINT('Ctrl Pts',(8.05403625519527,37.8421052631579,4.64999999999999));
#26001=CARTESIAN_POINT('Ctrl Pts',(6.80807251039055,38.0394736842105,6.80807251039054));
#26002=CARTESIAN_POINT('Ctrl Pts',(4.65,38.2368421052631,8.05403625519526));
#26003=CARTESIAN_POINT('Ctrl Pts',(2.49192748960945,38.4342105263158,9.29999999999998));
#26004=CARTESIAN_POINT('Ctrl Pts',(4.78400998185789E-28,38.6315789473684,
9.29999999999999));
#26005=CARTESIAN_POINT('Ctrl Pts',(-2.49192748960944,38.828947368421,9.29999999999998));
#26006=CARTESIAN_POINT('Ctrl Pts',(-4.64999999999999,39.0263157894736,8.05403625519527));
#26007=CARTESIAN_POINT('Ctrl Pts',(-6.80807251039054,39.2236842105262,6.80807251039054));
#26008=CARTESIAN_POINT('Ctrl Pts',(-8.05403625519527,39.421052631579,4.64999999999999));
#26009=CARTESIAN_POINT('Ctrl Pts',(-9.29999999999998,39.6184210526316,2.49192748960944));
#26010=CARTESIAN_POINT('Ctrl Pts',(-9.29999999999999,39.8157894736842,5.69460761603572E-16));
#26011=CARTESIAN_POINT('Ctrl Pts',(-9.29999999999998,40.0131578947368,-2.49192748960943));
#26012=CARTESIAN_POINT('Ctrl Pts',(-8.05403625519527,40.2105263157895,-4.64999999999999));
#26013=CARTESIAN_POINT('Ctrl Pts',(-6.80807251039054,40.4078947368421,-6.80807251039054));
#26014=CARTESIAN_POINT('Ctrl Pts',(-4.65,40.6052631578947,-8.05403625519526));
#26015=CARTESIAN_POINT('Ctrl Pts',(-2.49192748960944,40.8026315789474,-9.29999999999998));
#26016=CARTESIAN_POINT('Ctrl Pts',(-1.13892152320664E-15,41.,-9.29999999999999));
#26017=CARTESIAN_POINT('Ctrl Pts',(2.49192748960943,41.1973684210526,-9.29999999999999));
#26018=CARTESIAN_POINT('Ctrl Pts',(4.64999999999999,41.3947368421053,-8.05403625519527));
#26019=CARTESIAN_POINT('Ctrl Pts',(6.80807251039054,41.5921052631579,-6.80807251039055));
#26020=CARTESIAN_POINT('Ctrl Pts',(8.05403625519526,41.7894736842105,-4.65));
#26021=CARTESIAN_POINT('Ctrl Pts',(9.29999999999998,41.9868421052632,-2.49192748960945));
#26022=CARTESIAN_POINT('Ctrl Pts',(9.29999999999999,42.1842105263158,-1.70838228481055E-15));
#26023=CARTESIAN_POINT('Ctrl Pts',(9.29999999999999,42.3815789473684,2.49192748960943));
#26024=CARTESIAN_POINT('Ctrl Pts',(8.05403625519527,42.5789473684211,4.64999999999998));
#26025=CARTESIAN_POINT('Ctrl Pts',(6.80807251039055,42.7763157894736,6.80807251039054));
#26026=CARTESIAN_POINT('Ctrl Pts',(4.65,42.9736842105263,8.05403625519527));
#26027=CARTESIAN_POINT('Ctrl Pts',(2.49192748960945,43.1710526315789,9.29999999999998));
#26028=CARTESIAN_POINT('Ctrl Pts',(5.26934432784348E-28,43.3684210526316,
9.29999999999999));
#26029=CARTESIAN_POINT('Ctrl Pts',(-2.49192748960944,43.5657894736842,9.29999999999998));
#26030=CARTESIAN_POINT('Ctrl Pts',(-4.64999999999999,43.7631578947368,8.05403625519527));
#26031=CARTESIAN_POINT('Ctrl Pts',(-6.80807251039054,43.9605263157895,6.80807251039054));
#26032=CARTESIAN_POINT('Ctrl Pts',(-8.05403625519527,44.1578947368421,4.64999999999999));
#26033=CARTESIAN_POINT('Ctrl Pts',(-9.29999999999998,44.3552631578947,2.49192748960944));
#26034=CARTESIAN_POINT('Ctrl Pts',(-9.29999999999999,44.5526315789474,5.6946076160372E-16));
#26035=CARTESIAN_POINT('Ctrl Pts',(-9.29999999999998,44.75,-2.49192748960944));
#26036=CARTESIAN_POINT('Ctrl Pts',(-8.05403625519527,44.9473684210526,-4.64999999999999));
#26037=CARTESIAN_POINT('Ctrl Pts',(-6.80807251039054,45.1447368421053,-6.80807251039054));
#26038=CARTESIAN_POINT('Ctrl Pts',(-4.65,45.3421052631579,-8.05403625519526));
#26039=CARTESIAN_POINT('Ctrl Pts',(-2.49192748960944,45.5394736842105,-9.29999999999998));
#26040=CARTESIAN_POINT('Ctrl Pts',(-1.13892152320659E-15,45.7368421052632,
-9.29999999999999));
#26041=CARTESIAN_POINT('Ctrl Pts',(2.49192748960943,45.9342105263158,-9.29999999999999));
#26042=CARTESIAN_POINT('Ctrl Pts',(4.64999999999999,46.1315789473684,-8.05403625519527));
#26043=CARTESIAN_POINT('Ctrl Pts',(6.80807251039054,46.328947368421,-6.80807251039055));
#26044=CARTESIAN_POINT('Ctrl Pts',(8.05403625519526,46.5263157894737,-4.65));
#26045=CARTESIAN_POINT('Ctrl Pts',(9.29999999999998,46.7236842105263,-2.49192748960944));
#26046=CARTESIAN_POINT('Ctrl Pts',(9.29999999999999,46.9210526315789,-1.70838228481055E-15));
#26047=CARTESIAN_POINT('Ctrl Pts',(9.29999999999999,47.1184210526316,2.49192748960943));
#26048=CARTESIAN_POINT('Ctrl Pts',(8.05403625519527,47.3157894736843,4.64999999999999));
#26049=CARTESIAN_POINT('Ctrl Pts',(6.80807251039055,47.5131578947368,6.80807251039054));
#26050=CARTESIAN_POINT('Ctrl Pts',(4.65,47.7105263157895,8.05403625519526));
#26051=CARTESIAN_POINT('Ctrl Pts',(2.49192748960945,47.9078947368421,9.29999999999998));
#26052=CARTESIAN_POINT('Ctrl Pts',(5.75467867382906E-28,48.1052631578947,
9.29999999999999));
#26053=CARTESIAN_POINT('Ctrl Pts',(-2.49192748960944,48.3026315789473,9.29999999999998));
#26054=CARTESIAN_POINT('Ctrl Pts',(-4.64999999999999,48.5,8.05403625519527));
#26055=CARTESIAN_POINT('Ctrl Pts',(-6.80807251039054,48.6973684210526,6.80807251039054));
#26056=CARTESIAN_POINT('Ctrl Pts',(-8.05403625519527,48.8947368421053,4.64999999999999));
#26057=CARTESIAN_POINT('Ctrl Pts',(-9.29999999999998,49.0921052631579,2.49192748960944));
#26058=CARTESIAN_POINT('Ctrl Pts',(-9.29999999999999,49.2894736842105,5.69460761603572E-16));
#26059=CARTESIAN_POINT('Ctrl Pts',(-9.29999999999998,49.4868421052631,-2.49192748960944));
#26060=CARTESIAN_POINT('Ctrl Pts',(-8.05403625519527,49.6842105263157,-4.64999999999999));
#26061=CARTESIAN_POINT('Ctrl Pts',(-6.80807251039054,49.8815789473684,-6.80807251039054));
#26062=CARTESIAN_POINT('Ctrl Pts',(-4.65,50.0789473684211,-8.05403625519526));
#26063=CARTESIAN_POINT('Ctrl Pts',(-2.49192748960944,50.2763157894737,-9.29999999999998));
#26064=CARTESIAN_POINT('Ctrl Pts',(-1.13892152320653E-15,50.4736842105263,
-9.29999999999998));
#26065=CARTESIAN_POINT('Ctrl Pts',(2.49192748960943,50.671052631579,-9.29999999999999));
#26066=CARTESIAN_POINT('Ctrl Pts',(4.64999999999999,50.8684210526316,-8.05403625519527));
#26067=CARTESIAN_POINT('Ctrl Pts',(6.80807251039054,51.0657894736843,-6.80807251039055));
#26068=CARTESIAN_POINT('Ctrl Pts',(8.05403625519526,51.2631578947368,-4.65));
#26069=CARTESIAN_POINT('Ctrl Pts',(9.29999999999998,51.4605263157895,-2.49192748960944));
#26070=CARTESIAN_POINT('Ctrl Pts',(9.29999999999999,51.6578947368421,-1.70838228481055E-15));
#26071=CARTESIAN_POINT('Ctrl Pts',(9.29999999999999,51.8552631578948,2.49192748960943));
#26072=CARTESIAN_POINT('Ctrl Pts',(8.05403625519527,52.0526315789474,4.64999999999998));
#26073=CARTESIAN_POINT('Ctrl Pts',(6.80807251039055,52.2499999999999,6.80807251039053));
#26074=CARTESIAN_POINT('Ctrl Pts',(4.65,52.4473684210526,8.05403625519526));
#26075=CARTESIAN_POINT('Ctrl Pts',(2.49192748960945,52.6447368421052,9.29999999999998));
#26076=CARTESIAN_POINT('Ctrl Pts',(6.30934649781258E-28,52.8421052631579,
9.29999999999999));
#26077=CARTESIAN_POINT('Ctrl Pts',(-2.49192748960944,53.0394736842105,9.29999999999999));
#26078=CARTESIAN_POINT('Ctrl Pts',(-4.64999999999999,53.2368421052632,8.05403625519527));
#26079=CARTESIAN_POINT('Ctrl Pts',(-6.80807251039054,53.4342105263158,6.80807251039055));
#26080=CARTESIAN_POINT('Ctrl Pts',(-8.05403625519527,53.6315789473684,4.64999999999999));
#26081=CARTESIAN_POINT('Ctrl Pts',(-9.29999999999998,53.8289473684211,2.49192748960944));
#26082=CARTESIAN_POINT('Ctrl Pts',(-9.29999999999999,54.0263157894737,5.69460761603572E-16));
#26083=CARTESIAN_POINT('Ctrl Pts',(-9.29999999999998,54.2236842105263,-2.49192748960944));
#26084=CARTESIAN_POINT('Ctrl Pts',(-8.05403625519527,54.4210526315789,-4.64999999999999));
#26085=CARTESIAN_POINT('Ctrl Pts',(-6.80807251039054,54.6184210526316,-6.80807251039054));
#26086=CARTESIAN_POINT('Ctrl Pts',(-4.65,54.8157894736842,-8.05403625519526));
#26087=CARTESIAN_POINT('Ctrl Pts',(-2.49192748960944,55.0131578947369,-9.29999999999998));
#26088=CARTESIAN_POINT('Ctrl Pts',(-1.13892152320648E-15,55.2105263157895,
-9.29999999999999));
#26089=CARTESIAN_POINT('Ctrl Pts',(2.49192748960943,55.4078947368421,-9.29999999999999));
#26090=CARTESIAN_POINT('Ctrl Pts',(4.64999999999999,55.6052631578947,-8.05403625519527));
#26091=CARTESIAN_POINT('Ctrl Pts',(6.80807251039054,55.8026315789474,-6.80807251039055));
#26092=CARTESIAN_POINT('Ctrl Pts',(8.05403625519526,55.9999999999999,-4.65));
#26093=CARTESIAN_POINT('Ctrl Pts',(9.29999999999998,56.1973684210526,-2.49192748960944));
#26094=CARTESIAN_POINT('Ctrl Pts',(9.29999999999999,56.3947368421052,-1.7083822848107E-15));
#26095=CARTESIAN_POINT('Ctrl Pts',(9.29999999999999,56.5921052631579,2.49192748960943));
#26096=CARTESIAN_POINT('Ctrl Pts',(8.05403625519527,56.7894736842106,4.64999999999998));
#26097=CARTESIAN_POINT('Ctrl Pts',(6.80807251039055,56.9868421052631,6.80807251039054));
#26098=CARTESIAN_POINT('Ctrl Pts',(4.65,57.1842105263158,8.05403625519526));
#26099=CARTESIAN_POINT('Ctrl Pts',(2.49192748960945,57.3815789473684,9.29999999999998));
#26100=CARTESIAN_POINT('Ctrl Pts',(6.73690294546655E-28,57.578947368421,
9.29999999999999));
#26101=CARTESIAN_POINT('Ctrl Pts',(-2.49192748960944,57.7763157894737,9.29999999999998));
#26102=CARTESIAN_POINT('Ctrl Pts',(-4.64999999999999,57.9736842105263,8.05403625519527));
#26103=CARTESIAN_POINT('Ctrl Pts',(-6.80807251039054,58.1710526315789,6.80807251039054));
#26104=CARTESIAN_POINT('Ctrl Pts',(-8.05403625519527,58.3684210526316,4.64999999999999));
#26105=CARTESIAN_POINT('Ctrl Pts',(-9.29999999999998,58.5657894736842,2.49192748960944));
#26106=CARTESIAN_POINT('Ctrl Pts',(-9.29999999999999,58.7631578947368,5.69460761603572E-16));
#26107=CARTESIAN_POINT('Ctrl Pts',(-9.29999999999998,58.9605263157895,-2.49192748960944));
#26108=CARTESIAN_POINT('Ctrl Pts',(-8.05403625519527,59.157894736842,-4.64999999999999));
#26109=CARTESIAN_POINT('Ctrl Pts',(-6.80807251039054,59.3552631578947,-6.80807251039054));
#26110=CARTESIAN_POINT('Ctrl Pts',(-4.65,59.5526315789473,-8.05403625519526));
#26111=CARTESIAN_POINT('Ctrl Pts',(-2.49192748960944,59.75,-9.29999999999998));
#26112=CARTESIAN_POINT('Ctrl Pts',(-1.13892152320643E-15,59.9473684210526,
-9.29999999999999));
#26113=CARTESIAN_POINT('Ctrl Pts',(2.49192748960943,60.1447368421053,-9.29999999999999));
#26114=CARTESIAN_POINT('Ctrl Pts',(4.64999999999999,60.3421052631579,-8.05403625519527));
#26115=CARTESIAN_POINT('Ctrl Pts',(6.80807251039054,60.5394736842106,-6.80807251039055));
#26116=CARTESIAN_POINT('Ctrl Pts',(8.05403625519526,60.7368421052631,-4.65));
#26117=CARTESIAN_POINT('Ctrl Pts',(9.29999999999998,60.9342105263158,-2.49192748960944));
#26118=CARTESIAN_POINT('Ctrl Pts',(9.29999999999999,61.1315789473684,-1.70838228481055E-15));
#26119=CARTESIAN_POINT('Ctrl Pts',(9.29999999999999,61.328947368421,2.49192748960943));
#26120=CARTESIAN_POINT('Ctrl Pts',(8.05403625519527,61.5263157894737,4.64999999999999));
#26121=CARTESIAN_POINT('Ctrl Pts',(6.80807251039055,61.7236842105263,6.80807251039054));
#26122=CARTESIAN_POINT('Ctrl Pts',(4.65,61.9210526315789,8.05403625519526));
#26123=CARTESIAN_POINT('Ctrl Pts',(2.49192748960945,62.1184210526316,9.29999999999998));
#26124=CARTESIAN_POINT('Ctrl Pts',(7.34934866778169E-28,62.3157894736842,
9.29999999999999));
#26125=CARTESIAN_POINT('Ctrl Pts',(-2.49192748960944,62.5131578947368,9.29999999999998));
#26126=CARTESIAN_POINT('Ctrl Pts',(-4.64999999999999,62.7105263157894,8.05403625519527));
#26127=CARTESIAN_POINT('Ctrl Pts',(-6.80807251039054,62.9078947368421,6.80807251039054));
#26128=CARTESIAN_POINT('Ctrl Pts',(-8.05403625519527,63.1052631578947,4.64999999999999));
#26129=CARTESIAN_POINT('Ctrl Pts',(-9.29999999999998,63.3026315789474,2.49192748960944));
#26130=CARTESIAN_POINT('Ctrl Pts',(-9.29999999999999,63.5,5.69460761603572E-16));
#26131=CARTESIAN_POINT('Ctrl Pts',(-9.29999999999998,63.6973684210526,-2.49192748960943));
#26132=CARTESIAN_POINT('Ctrl Pts',(-8.05403625519527,63.8947368421052,-4.64999999999999));
#26133=CARTESIAN_POINT('Ctrl Pts',(-6.80807251039054,64.092105263158,-6.80807251039054));
#26134=CARTESIAN_POINT('Ctrl Pts',(-4.65,64.2894736842105,-8.05403625519526));
#26135=CARTESIAN_POINT('Ctrl Pts',(-2.49192748960944,64.4868421052632,-9.29999999999998));
#26136=CARTESIAN_POINT('Ctrl Pts',(-1.13892152320638E-15,64.6842105263158,
-9.29999999999999));
#26137=CARTESIAN_POINT('Ctrl Pts',(2.49192748960943,64.8815789473684,-9.29999999999999));
#26138=CARTESIAN_POINT('Ctrl Pts',(4.64999999999999,65.078947368421,-8.05403625519527));
#26139=CARTESIAN_POINT('Ctrl Pts',(6.80807251039054,65.2763157894737,-6.80807251039055));
#26140=CARTESIAN_POINT('Ctrl Pts',(8.05403625519526,65.4736842105263,-4.65));
#26141=CARTESIAN_POINT('Ctrl Pts',(9.29999999999998,65.6710526315789,-2.49192748960944));
#26142=CARTESIAN_POINT('Ctrl Pts',(9.29999999999999,65.8684210526316,-1.70838228481055E-15));
#26143=CARTESIAN_POINT('Ctrl Pts',(9.29999999999999,66.0657894736842,2.49192748960943));
#26144=CARTESIAN_POINT('Ctrl Pts',(8.05403625519527,66.2631578947368,4.64999999999998));
#26145=CARTESIAN_POINT('Ctrl Pts',(6.80807251039055,66.4605263157895,6.80807251039054));
#26146=CARTESIAN_POINT('Ctrl Pts',(4.65,66.6578947368421,8.05403625519526));
#26147=CARTESIAN_POINT('Ctrl Pts',(2.49192748960945,66.8552631578947,9.29999999999998));
#26148=CARTESIAN_POINT('Ctrl Pts',(7.90401649176522E-28,67.0526315789473,
9.29999999999999));
#26149=CARTESIAN_POINT('Ctrl Pts',(-2.49192748960944,67.25,9.29999999999998));
#26150=CARTESIAN_POINT('Ctrl Pts',(-4.64999999999999,67.4473684210526,8.05403625519527));
#26151=CARTESIAN_POINT('Ctrl Pts',(-6.80807251039054,67.6447368421052,6.80807251039054));
#26152=CARTESIAN_POINT('Ctrl Pts',(-8.05403625519527,67.8421052631579,4.64999999999999));
#26153=CARTESIAN_POINT('Ctrl Pts',(-9.29999999999998,68.0394736842105,2.49192748960944));
#26154=CARTESIAN_POINT('Ctrl Pts',(-9.29999999999999,68.2368421052632,5.69460761603868E-16));
#26155=CARTESIAN_POINT('Ctrl Pts',(-9.29999999999998,68.4342105263158,-2.49192748960943));
#26156=CARTESIAN_POINT('Ctrl Pts',(-8.05403625519527,68.6315789473684,-4.64999999999999));
#26157=CARTESIAN_POINT('Ctrl Pts',(-6.80807251039054,68.8289473684211,-6.80807251039054));
#26158=CARTESIAN_POINT('Ctrl Pts',(-4.65,69.0263157894737,-8.05403625519526));
#26159=CARTESIAN_POINT('Ctrl Pts',(-2.49192748960944,69.2236842105263,-9.29999999999998));
#26160=CARTESIAN_POINT('Ctrl Pts',(-1.13892152320633E-15,69.421052631579,
-9.29999999999998));
#26161=CARTESIAN_POINT('Ctrl Pts',(2.49192748960943,69.6184210526316,-9.29999999999999));
#26162=CARTESIAN_POINT('Ctrl Pts',(4.64999999999999,69.8157894736842,-8.05403625519526));
#26163=CARTESIAN_POINT('Ctrl Pts',(6.80807251039054,70.0131578947368,-6.80807251039055));
#26164=CARTESIAN_POINT('Ctrl Pts',(8.05403625519526,70.2105263157894,-4.65));
#26165=CARTESIAN_POINT('Ctrl Pts',(9.29999999999998,70.4078947368421,-2.49192748960944));
#26166=CARTESIAN_POINT('Ctrl Pts',(9.29999999999999,70.6052631578947,-1.70838228481055E-15));
#26167=CARTESIAN_POINT('Ctrl Pts',(9.29999999999999,70.8026315789474,2.49192748960943));
#26168=CARTESIAN_POINT('Ctrl Pts',(8.05403625519527,71.,4.64999999999999));
#26169=CARTESIAN_POINT('Ctrl Pts',(6.80807251039055,71.1973684210526,6.80807251039054));
#26170=CARTESIAN_POINT('Ctrl Pts',(4.65,71.3947368421052,8.05403625519526));
#26171=CARTESIAN_POINT('Ctrl Pts',(2.49192748960945,71.5921052631579,9.29999999999998));
#26172=CARTESIAN_POINT('Ctrl Pts',(8.37779525808447E-28,71.7894736842105,
9.29999999999999));
#26173=CARTESIAN_POINT('Ctrl Pts',(-2.49192748960944,71.9868421052631,9.29999999999998));
#26174=CARTESIAN_POINT('Ctrl Pts',(-4.64999999999999,72.1842105263157,8.05403625519527));
#26175=CARTESIAN_POINT('Ctrl Pts',(-6.80807251039054,72.3815789473683,6.80807251039054));
#26176=CARTESIAN_POINT('Ctrl Pts',(-8.05403625519527,72.5789473684211,4.64999999999999));
#26177=CARTESIAN_POINT('Ctrl Pts',(-9.29999999999998,72.7763157894737,2.49192748960944));
#26178=CARTESIAN_POINT('Ctrl Pts',(-9.29999999999999,72.9736842105263,5.6946076160372E-16));
#26179=CARTESIAN_POINT('Ctrl Pts',(-9.29999999999998,73.1710526315789,-2.49192748960943));
#26180=CARTESIAN_POINT('Ctrl Pts',(-8.05403625519527,73.3684210526315,-4.64999999999999));
#26181=CARTESIAN_POINT('Ctrl Pts',(-6.80807251039054,73.5657894736842,-6.80807251039054));
#26182=CARTESIAN_POINT('Ctrl Pts',(-4.65,73.7631578947368,-8.05403625519526));
#26183=CARTESIAN_POINT('Ctrl Pts',(-2.49192748960944,73.9605263157895,-9.29999999999998));
#26184=CARTESIAN_POINT('Ctrl Pts',(-1.13892152320627E-15,74.1578947368421,
-9.29999999999999));
#26185=CARTESIAN_POINT('Ctrl Pts',(2.49192748960943,74.3552631578947,-9.29999999999999));
#26186=CARTESIAN_POINT('Ctrl Pts',(4.64999999999999,74.5526315789473,-8.05403625519527));
#26187=CARTESIAN_POINT('Ctrl Pts',(6.80807251039054,74.75,-6.80807251039055));
#26188=CARTESIAN_POINT('Ctrl Pts',(8.05403625519526,74.9473684210526,-4.65));
#26189=CARTESIAN_POINT('Ctrl Pts',(9.29999999999998,75.1447368421053,-2.49192748960945));
#26190=CARTESIAN_POINT('Ctrl Pts',(9.29999999999999,75.3421052631579,-1.70838228481055E-15));
#26191=CARTESIAN_POINT('Ctrl Pts',(9.29999999999999,75.5394736842105,2.49192748960943));
#26192=CARTESIAN_POINT('Ctrl Pts',(8.05403625519527,75.7368421052631,4.64999999999998));
#26193=CARTESIAN_POINT('Ctrl Pts',(6.80807251039055,75.9342105263157,6.80807251039054));
#26194=CARTESIAN_POINT('Ctrl Pts',(4.65,76.1315789473684,8.05403625519527));
#26195=CARTESIAN_POINT('Ctrl Pts',(2.49192748960945,76.3289473684211,9.29999999999998));
#26196=CARTESIAN_POINT('Ctrl Pts',(8.87468518373638E-28,76.5263157894736,
9.29999999999999));
#26197=CARTESIAN_POINT('Ctrl Pts',(-2.49192748960944,76.7236842105263,9.29999999999998));
#26198=CARTESIAN_POINT('Ctrl Pts',(-4.64999999999999,76.9210526315789,8.05403625519527));
#26199=CARTESIAN_POINT('Ctrl Pts',(-6.80807251039054,77.1184210526315,6.80807251039054));
#26200=CARTESIAN_POINT('Ctrl Pts',(-8.05403625519527,77.3157894736842,4.64999999999999));
#26201=CARTESIAN_POINT('Ctrl Pts',(-9.29999999999998,77.5131578947368,2.49192748960944));
#26202=CARTESIAN_POINT('Ctrl Pts',(-9.29999999999999,77.7105263157894,5.6946076160372E-16));
#26203=CARTESIAN_POINT('Ctrl Pts',(-9.29999999999998,77.9078947368421,-2.49192748960943));
#26204=CARTESIAN_POINT('Ctrl Pts',(-8.05403625519527,78.1052631578947,-4.64999999999999));
#26205=CARTESIAN_POINT('Ctrl Pts',(-6.80807251039054,78.3026315789474,-6.80807251039054));
#26206=CARTESIAN_POINT('Ctrl Pts',(-4.65,78.5,-8.05403625519526));
#26207=CARTESIAN_POINT('Ctrl Pts',(-2.49192748960944,78.6973684210526,-9.29999999999998));
#26208=CARTESIAN_POINT('Ctrl Pts',(-1.13892152320622E-15,78.8947368421053,
-9.29999999999999));
#26209=CARTESIAN_POINT('Ctrl Pts',(2.49192748960943,79.0921052631579,-9.29999999999999));
#26210=CARTESIAN_POINT('Ctrl Pts',(4.64999999999999,79.2894736842105,-8.05403625519527));
#26211=CARTESIAN_POINT('Ctrl Pts',(6.80807251039054,79.4868421052632,-6.80807251039055));
#26212=CARTESIAN_POINT('Ctrl Pts',(8.05403625519526,79.6842105263157,-4.65));
#26213=CARTESIAN_POINT('Ctrl Pts',(9.29999999999998,79.8815789473684,-2.49192748960945));
#26214=CARTESIAN_POINT('Ctrl Pts',(9.29999999999999,80.0789473684211,-1.70838228481055E-15));
#26215=CARTESIAN_POINT('Ctrl Pts',(9.29999999999999,80.2763157894737,2.49192748960943));
#26216=CARTESIAN_POINT('Ctrl Pts',(8.05403625519527,80.4736842105264,4.64999999999998));
#26217=CARTESIAN_POINT('Ctrl Pts',(6.80807251039055,80.6710526315789,6.80807251039054));
#26218=CARTESIAN_POINT('Ctrl Pts',(4.65,80.8684210526316,8.05403625519526));
#26219=CARTESIAN_POINT('Ctrl Pts',(2.49192748960945,81.0657894736842,9.29999999999998));
#26220=CARTESIAN_POINT('Ctrl Pts',(9.36001952972196E-28,81.2631578947368,
9.29999999999999));
#26221=CARTESIAN_POINT('Ctrl Pts',(-2.49192748960944,81.4605263157895,9.29999999999998));
#26222=CARTESIAN_POINT('Ctrl Pts',(-4.64999999999999,81.6578947368421,8.05403625519527));
#26223=CARTESIAN_POINT('Ctrl Pts',(-6.80807251039054,81.8552631578947,6.80807251039054));
#26224=CARTESIAN_POINT('Ctrl Pts',(-8.05403625519527,82.0526315789474,4.64999999999999));
#26225=CARTESIAN_POINT('Ctrl Pts',(-9.29999999999998,82.25,2.49192748960944));
#26226=CARTESIAN_POINT('Ctrl Pts',(-9.29999999999999,82.4473684210526,5.6946076160372E-16));
#26227=CARTESIAN_POINT('Ctrl Pts',(-9.29999999999998,82.6447368421053,-2.49192748960944));
#26228=CARTESIAN_POINT('Ctrl Pts',(-8.05403625519527,82.8421052631579,-4.64999999999999));
#26229=CARTESIAN_POINT('Ctrl Pts',(-6.80807251039054,83.0394736842105,-6.80807251039054));
#26230=CARTESIAN_POINT('Ctrl Pts',(-4.65,83.2368421052631,-8.05403625519526));
#26231=CARTESIAN_POINT('Ctrl Pts',(-2.49192748960944,83.4342105263158,-9.29999999999998));
#26232=CARTESIAN_POINT('Ctrl Pts',(-1.13892152320617E-15,83.6315789473684,
-9.29999999999998));
#26233=CARTESIAN_POINT('Ctrl Pts',(2.49192748960943,83.8289473684211,-9.29999999999999));
#26234=CARTESIAN_POINT('Ctrl Pts',(4.64999999999999,84.0263157894737,-8.05403625519527));
#26235=CARTESIAN_POINT('Ctrl Pts',(6.80807251039054,84.2236842105264,-6.80807251039055));
#26236=CARTESIAN_POINT('Ctrl Pts',(8.05403625519526,84.4210526315789,-4.65));
#26237=CARTESIAN_POINT('Ctrl Pts',(9.29999999999998,84.6184210526316,-2.49192748960945));
#26238=CARTESIAN_POINT('Ctrl Pts',(9.29999999999999,84.8157894736842,-1.7083822848104E-15));
#26239=CARTESIAN_POINT('Ctrl Pts',(9.29999999999999,85.0131578947368,2.49192748960943));
#26240=CARTESIAN_POINT('Ctrl Pts',(8.05403625519527,85.2105263157895,4.64999999999998));
#26241=CARTESIAN_POINT('Ctrl Pts',(6.80807251039055,85.407894736842,6.80807251039054));
#26242=CARTESIAN_POINT('Ctrl Pts',(4.65,85.6052631578947,8.05403625519526));
#26243=CARTESIAN_POINT('Ctrl Pts',(2.49192748960945,85.8026315789473,9.29999999999998));
#26244=CARTESIAN_POINT('Ctrl Pts',(9.98402083170343E-28,86.,9.29999999999999));
#26245=CARTESIAN_POINT('Ctrl Pts',(-1.38666955995881E-29,-3.99999999999997,
5.29999999999999));
#26246=CARTESIAN_POINT('Ctrl Pts',(-1.42013071988495,-3.80263157894733,
5.29999999999999));
#26247=CARTESIAN_POINT('Ctrl Pts',(-2.65,-3.60526315789474,4.58993464005751));
#26248=CARTESIAN_POINT('Ctrl Pts',(-3.87986928011504,-3.40789473684211,
3.87986928011504));
#26249=CARTESIAN_POINT('Ctrl Pts',(-4.58993464005752,-3.21052631578946,
2.65));
#26250=CARTESIAN_POINT('Ctrl Pts',(-5.29999999999999,-3.01315789473685,
1.42013071988495));
#26251=CARTESIAN_POINT('Ctrl Pts',(-5.29999999999999,-2.81578947368422,
3.24531401773979E-16));
#26252=CARTESIAN_POINT('Ctrl Pts',(-5.29999999999999,-2.61842105263159,
-1.42013071988495));
#26253=CARTESIAN_POINT('Ctrl Pts',(-4.58993464005752,-2.42105263157898,
-2.65));
#26254=CARTESIAN_POINT('Ctrl Pts',(-3.87986928011504,-2.22368421052633,
-3.87986928011504));
#26255=CARTESIAN_POINT('Ctrl Pts',(-2.65,-2.02631578947369,-4.58993464005752));
#26256=CARTESIAN_POINT('Ctrl Pts',(-1.42013071988495,-1.82894736842106,
-5.29999999999999));
#26257=CARTESIAN_POINT('Ctrl Pts',(-6.4906280354814E-16,-1.63157894736846,
-5.29999999999999));
#26258=CARTESIAN_POINT('Ctrl Pts',(1.42013071988495,-1.4342105263158,-5.29999999999999));
#26259=CARTESIAN_POINT('Ctrl Pts',(2.65,-1.23684210526317,-4.58993464005752));
#26260=CARTESIAN_POINT('Ctrl Pts',(3.87986928011504,-1.03947368421054,-3.87986928011504));
#26261=CARTESIAN_POINT('Ctrl Pts',(4.58993464005752,-0.842105263157894,
-2.65));
#26262=CARTESIAN_POINT('Ctrl Pts',(5.29999999999999,-0.644736842105277,
-1.42013071988495));
#26263=CARTESIAN_POINT('Ctrl Pts',(5.29999999999999,-0.447368421052613,
-9.73594205322067E-16));
#26264=CARTESIAN_POINT('Ctrl Pts',(5.29999999999999,-0.250000000000015,
1.42013071988495));
#26265=CARTESIAN_POINT('Ctrl Pts',(4.58993464005752,-0.0526315789473736,
2.64999999999999));
#26266=CARTESIAN_POINT('Ctrl Pts',(3.87986928011504,0.14473684210529,3.87986928011504));
#26267=CARTESIAN_POINT('Ctrl Pts',(2.65,0.342105263157907,4.58993464005751));
#26268=CARTESIAN_POINT('Ctrl Pts',(1.42013071988495,0.539473684210552,5.29999999999999));
#26269=CARTESIAN_POINT('Ctrl Pts',(4.16000867987643E-29,0.736842105263188,
5.29999999999999));
#26270=CARTESIAN_POINT('Ctrl Pts',(-1.42013071988495,0.934210526315814,
5.29999999999999));
#26271=CARTESIAN_POINT('Ctrl Pts',(-2.65,1.13157894736843,4.58993464005752));
#26272=CARTESIAN_POINT('Ctrl Pts',(-3.87986928011504,1.32894736842108,3.87986928011504));
#26273=CARTESIAN_POINT('Ctrl Pts',(-4.58993464005752,1.52631578947371,2.65));
#26274=CARTESIAN_POINT('Ctrl Pts',(-5.29999999999999,1.72368421052634,1.42013071988495));
#26275=CARTESIAN_POINT('Ctrl Pts',(-5.29999999999999,1.92105263157895,3.24531401773979E-16));
#26276=CARTESIAN_POINT('Ctrl Pts',(-5.29999999999999,2.11842105263156,-1.42013071988495));
#26277=CARTESIAN_POINT('Ctrl Pts',(-4.58993464005752,2.31578947368419,-2.65));
#26278=CARTESIAN_POINT('Ctrl Pts',(-3.87986928011504,2.51315789473682,-3.87986928011504));
#26279=CARTESIAN_POINT('Ctrl Pts',(-2.65,2.71052631578947,-4.58993464005752));
#26280=CARTESIAN_POINT('Ctrl Pts',(-1.42013071988495,2.90789473684208,-5.29999999999999));
#26281=CARTESIAN_POINT('Ctrl Pts',(-6.49062803548097E-16,3.10526315789471,
-5.3));
#26282=CARTESIAN_POINT('Ctrl Pts',(1.42013071988495,3.30263157894734,-5.29999999999999));
#26283=CARTESIAN_POINT('Ctrl Pts',(2.65,3.49999999999999,-4.58993464005752));
#26284=CARTESIAN_POINT('Ctrl Pts',(3.87986928011504,3.69736842105261,-3.87986928011504));
#26285=CARTESIAN_POINT('Ctrl Pts',(4.58993464005752,3.89473684210527,-2.65));
#26286=CARTESIAN_POINT('Ctrl Pts',(5.29999999999999,4.09210526315787,-1.42013071988495));
#26287=CARTESIAN_POINT('Ctrl Pts',(5.29999999999999,4.28947368421051,-9.73594205322215E-16));
#26288=CARTESIAN_POINT('Ctrl Pts',(5.29999999999999,4.48684210526317,1.42013071988495));
#26289=CARTESIAN_POINT('Ctrl Pts',(4.58993464005752,4.68421052631579,2.64999999999999));
#26290=CARTESIAN_POINT('Ctrl Pts',(3.87986928011504,4.88157894736844,3.87986928011504));
#26291=CARTESIAN_POINT('Ctrl Pts',(2.65,5.07894736842107,4.58993464005752));
#26292=CARTESIAN_POINT('Ctrl Pts',(1.42013071988495,5.2763157894737,5.29999999999999));
#26293=CARTESIAN_POINT('Ctrl Pts',(8.66668474974256E-29,5.47368421052635,
5.29999999999999));
#26294=CARTESIAN_POINT('Ctrl Pts',(-1.42013071988495,5.67105263157896,5.29999999999999));
#26295=CARTESIAN_POINT('Ctrl Pts',(-2.65,5.86842105263159,4.58993464005752));
#26296=CARTESIAN_POINT('Ctrl Pts',(-3.87986928011504,6.06578947368422,3.87986928011504));
#26297=CARTESIAN_POINT('Ctrl Pts',(-4.58993464005752,6.26315789473683,2.65));
#26298=CARTESIAN_POINT('Ctrl Pts',(-5.29999999999999,6.46052631578948,1.42013071988495));
#26299=CARTESIAN_POINT('Ctrl Pts',(-5.29999999999999,6.65789473684211,3.24531401773979E-16));
#26300=CARTESIAN_POINT('Ctrl Pts',(-5.29999999999999,6.85526315789475,-1.42013071988495));
#26301=CARTESIAN_POINT('Ctrl Pts',(-4.58993464005752,7.05263157894735,-2.65));
#26302=CARTESIAN_POINT('Ctrl Pts',(-3.87986928011504,7.24999999999997,-3.87986928011504));
#26303=CARTESIAN_POINT('Ctrl Pts',(-2.65,7.44736842105263,-4.58993464005752));
#26304=CARTESIAN_POINT('Ctrl Pts',(-1.42013071988495,7.64473684210523,-5.29999999999999));
#26305=CARTESIAN_POINT('Ctrl Pts',(-6.49062803548034E-16,7.84210526315787,
-5.29999999999999));
#26306=CARTESIAN_POINT('Ctrl Pts',(1.42013071988495,8.03947368421049,-5.29999999999999));
#26307=CARTESIAN_POINT('Ctrl Pts',(2.65,8.23684210526315,-4.58993464005752));
#26308=CARTESIAN_POINT('Ctrl Pts',(3.87986928011504,8.43421052631579,-3.87986928011504));
#26309=CARTESIAN_POINT('Ctrl Pts',(4.58993464005752,8.63157894736839,-2.65));
#26310=CARTESIAN_POINT('Ctrl Pts',(5.29999999999999,8.82894736842105,-1.42013071988495));
#26311=CARTESIAN_POINT('Ctrl Pts',(5.29999999999999,9.02631578947367,-9.73594205322215E-16));
#26312=CARTESIAN_POINT('Ctrl Pts',(5.29999999999999,9.22368421052632,1.42013071988494));
#26313=CARTESIAN_POINT('Ctrl Pts',(4.58993464005752,9.42105263157895,2.64999999999999));
#26314=CARTESIAN_POINT('Ctrl Pts',(3.87986928011504,9.61842105263158,3.87986928011504));
#26315=CARTESIAN_POINT('Ctrl Pts',(2.65,9.81578947368424,4.58993464005751));
#26316=CARTESIAN_POINT('Ctrl Pts',(1.42013071988495,10.0131578947368,5.29999999999999));
#26317=CARTESIAN_POINT('Ctrl Pts',(1.45600303795675E-28,10.2105263157895,
5.29999999999999));
#26318=CARTESIAN_POINT('Ctrl Pts',(-1.42013071988495,10.4078947368421,5.29999999999999));
#26319=CARTESIAN_POINT('Ctrl Pts',(-2.65,10.6052631578948,4.58993464005751));
#26320=CARTESIAN_POINT('Ctrl Pts',(-3.87986928011504,10.8026315789474,3.87986928011504));
#26321=CARTESIAN_POINT('Ctrl Pts',(-4.58993464005752,11.,2.65));
#26322=CARTESIAN_POINT('Ctrl Pts',(-5.29999999999999,11.1973684210526,1.42013071988495));
#26323=CARTESIAN_POINT('Ctrl Pts',(-5.29999999999999,11.3947368421053,3.24531401773979E-16));
#26324=CARTESIAN_POINT('Ctrl Pts',(-5.29999999999999,11.5921052631579,-1.42013071988495));
#26325=CARTESIAN_POINT('Ctrl Pts',(-4.58993464005752,11.7894736842105,-2.64999999999999));
#26326=CARTESIAN_POINT('Ctrl Pts',(-3.87986928011504,11.9868421052632,-3.87986928011504));
#26327=CARTESIAN_POINT('Ctrl Pts',(-2.65,12.1842105263158,-4.58993464005752));
#26328=CARTESIAN_POINT('Ctrl Pts',(-1.42013071988495,12.3815789473684,-5.29999999999999));
#26329=CARTESIAN_POINT('Ctrl Pts',(-6.4906280354798E-16,12.578947368421,
-5.3));
#26330=CARTESIAN_POINT('Ctrl Pts',(1.42013071988495,12.7763157894737,-5.29999999999999));
#26331=CARTESIAN_POINT('Ctrl Pts',(2.65,12.9736842105263,-4.58993464005752));
#26332=CARTESIAN_POINT('Ctrl Pts',(3.87986928011504,13.1710526315789,-3.87986928011504));
#26333=CARTESIAN_POINT('Ctrl Pts',(4.58993464005752,13.3684210526316,-2.65));
#26334=CARTESIAN_POINT('Ctrl Pts',(5.29999999999999,13.5657894736842,-1.42013071988495));
#26335=CARTESIAN_POINT('Ctrl Pts',(5.29999999999999,13.7631578947368,-9.73594205322067E-16));
#26336=CARTESIAN_POINT('Ctrl Pts',(5.29999999999999,13.9605263157895,1.42013071988495));
#26337=CARTESIAN_POINT('Ctrl Pts',(4.58993464005752,14.1578947368421,2.64999999999999));
#26338=CARTESIAN_POINT('Ctrl Pts',(3.87986928011504,14.3552631578948,3.87986928011504));
#26339=CARTESIAN_POINT('Ctrl Pts',(2.65,14.5526315789474,4.58993464005752));
#26340=CARTESIAN_POINT('Ctrl Pts',(1.42013071988495,14.75,5.3));
#26341=CARTESIAN_POINT('Ctrl Pts',(1.94133738394233E-28,14.9473684210526,
5.29999999999999));
#26342=CARTESIAN_POINT('Ctrl Pts',(-1.42013071988495,15.1447368421053,5.3));
#26343=CARTESIAN_POINT('Ctrl Pts',(-2.65,15.3421052631579,4.58993464005752));
#26344=CARTESIAN_POINT('Ctrl Pts',(-3.87986928011504,15.5394736842106,3.87986928011505));
#26345=CARTESIAN_POINT('Ctrl Pts',(-4.58993464005752,15.7368421052632,2.65));
#26346=CARTESIAN_POINT('Ctrl Pts',(-5.29999999999999,15.9342105263158,1.42013071988495));
#26347=CARTESIAN_POINT('Ctrl Pts',(-5.29999999999999,16.1315789473684,3.24531401773979E-16));
#26348=CARTESIAN_POINT('Ctrl Pts',(-5.29999999999999,16.328947368421,-1.42013071988495));
#26349=CARTESIAN_POINT('Ctrl Pts',(-4.58993464005752,16.5263157894737,-2.64999999999999));
#26350=CARTESIAN_POINT('Ctrl Pts',(-3.87986928011504,16.7236842105263,-3.87986928011504));
#26351=CARTESIAN_POINT('Ctrl Pts',(-2.65,16.9210526315789,-4.58993464005752));
#26352=CARTESIAN_POINT('Ctrl Pts',(-1.42013071988495,17.1184210526316,-5.29999999999999));
#26353=CARTESIAN_POINT('Ctrl Pts',(-6.49062803547937E-16,17.3157894736842,
-5.3));
#26354=CARTESIAN_POINT('Ctrl Pts',(1.42013071988495,17.5131578947368,-5.29999999999999));
#26355=CARTESIAN_POINT('Ctrl Pts',(2.65,17.7105263157894,-4.58993464005752));
#26356=CARTESIAN_POINT('Ctrl Pts',(3.87986928011504,17.9078947368421,-3.87986928011504));
#26357=CARTESIAN_POINT('Ctrl Pts',(4.58993464005752,18.1052631578947,-2.65));
#26358=CARTESIAN_POINT('Ctrl Pts',(5.29999999999999,18.3026315789473,-1.42013071988495));
#26359=CARTESIAN_POINT('Ctrl Pts',(5.29999999999999,18.5,-9.73594205322067E-16));
#26360=CARTESIAN_POINT('Ctrl Pts',(5.29999999999999,18.6973684210526,1.42013071988495));
#26361=CARTESIAN_POINT('Ctrl Pts',(4.58993464005752,18.8947368421053,2.64999999999999));
#26362=CARTESIAN_POINT('Ctrl Pts',(3.87986928011504,19.0921052631579,3.87986928011504));
#26363=CARTESIAN_POINT('Ctrl Pts',(2.65,19.2894736842105,4.58993464005751));
#26364=CARTESIAN_POINT('Ctrl Pts',(1.42013071988495,19.4868421052632,5.29999999999999));
#26365=CARTESIAN_POINT('Ctrl Pts',(2.42667172992792E-28,19.6842105263158,
5.29999999999999));
#26366=CARTESIAN_POINT('Ctrl Pts',(-1.42013071988495,19.8815789473684,5.29999999999999));
#26367=CARTESIAN_POINT('Ctrl Pts',(-2.65,20.0789473684211,4.58993464005751));
#26368=CARTESIAN_POINT('Ctrl Pts',(-3.87986928011504,20.2763157894737,3.87986928011504));
#26369=CARTESIAN_POINT('Ctrl Pts',(-4.58993464005752,20.4736842105263,2.65));
#26370=CARTESIAN_POINT('Ctrl Pts',(-5.29999999999999,20.671052631579,1.42013071988495));
#26371=CARTESIAN_POINT('Ctrl Pts',(-5.29999999999999,20.8684210526316,3.24531401773979E-16));
#26372=CARTESIAN_POINT('Ctrl Pts',(-5.29999999999999,21.0657894736842,-1.42013071988495));
#26373=CARTESIAN_POINT('Ctrl Pts',(-4.58993464005752,21.2631578947368,-2.65));
#26374=CARTESIAN_POINT('Ctrl Pts',(-3.87986928011504,21.4605263157894,-3.87986928011504));
#26375=CARTESIAN_POINT('Ctrl Pts',(-2.65,21.6578947368421,-4.58993464005752));
#26376=CARTESIAN_POINT('Ctrl Pts',(-1.42013071988495,21.8552631578947,-5.29999999999999));
#26377=CARTESIAN_POINT('Ctrl Pts',(-6.49062803547882E-16,22.0526315789474,
-5.29999999999999));
#26378=CARTESIAN_POINT('Ctrl Pts',(1.42013071988495,22.25,-5.29999999999999));
#26379=CARTESIAN_POINT('Ctrl Pts',(2.65,22.4473684210526,-4.58993464005752));
#26380=CARTESIAN_POINT('Ctrl Pts',(3.87986928011504,22.6447368421052,-3.87986928011504));
#26381=CARTESIAN_POINT('Ctrl Pts',(4.58993464005752,22.8421052631579,-2.65));
#26382=CARTESIAN_POINT('Ctrl Pts',(5.29999999999999,23.0394736842105,-1.42013071988495));
#26383=CARTESIAN_POINT('Ctrl Pts',(5.29999999999999,23.2368421052632,-9.73594205322067E-16));
#26384=CARTESIAN_POINT('Ctrl Pts',(5.29999999999999,23.4342105263158,1.42013071988495));
#26385=CARTESIAN_POINT('Ctrl Pts',(4.58993464005752,23.6315789473684,2.64999999999999));
#26386=CARTESIAN_POINT('Ctrl Pts',(3.87986928011504,23.8289473684211,3.87986928011504));
#26387=CARTESIAN_POINT('Ctrl Pts',(2.65,24.0263157894737,4.58993464005752));
#26388=CARTESIAN_POINT('Ctrl Pts',(1.42013071988495,24.2236842105263,5.29999999999999));
#26389=CARTESIAN_POINT('Ctrl Pts',(2.9120060759135E-28,24.421052631579,
5.29999999999999));
#26390=CARTESIAN_POINT('Ctrl Pts',(-1.42013071988495,24.6184210526316,5.29999999999999));
#26391=CARTESIAN_POINT('Ctrl Pts',(-2.65,24.8157894736842,4.58993464005752));
#26392=CARTESIAN_POINT('Ctrl Pts',(-3.87986928011504,25.0131578947368,3.87986928011504));
#26393=CARTESIAN_POINT('Ctrl Pts',(-4.58993464005752,25.2105263157895,2.65));
#26394=CARTESIAN_POINT('Ctrl Pts',(-5.29999999999999,25.4078947368421,1.42013071988495));
#26395=CARTESIAN_POINT('Ctrl Pts',(-5.29999999999999,25.6052631578947,3.24531401773979E-16));
#26396=CARTESIAN_POINT('Ctrl Pts',(-5.29999999999999,25.8026315789474,-1.42013071988495));
#26397=CARTESIAN_POINT('Ctrl Pts',(-4.58993464005752,26.,-2.65));
#26398=CARTESIAN_POINT('Ctrl Pts',(-3.87986928011504,26.1973684210526,-3.87986928011504));
#26399=CARTESIAN_POINT('Ctrl Pts',(-2.65,26.3947368421052,-4.58993464005752));
#26400=CARTESIAN_POINT('Ctrl Pts',(-1.42013071988495,26.5921052631579,-5.29999999999999));
#26401=CARTESIAN_POINT('Ctrl Pts',(-6.49062803547835E-16,26.7894736842105,
-5.3));
#26402=CARTESIAN_POINT('Ctrl Pts',(1.42013071988495,26.9868421052632,-5.29999999999999));
#26403=CARTESIAN_POINT('Ctrl Pts',(2.65,27.1842105263158,-4.58993464005752));
#26404=CARTESIAN_POINT('Ctrl Pts',(3.87986928011504,27.3815789473684,-3.87986928011504));
#26405=CARTESIAN_POINT('Ctrl Pts',(4.58993464005752,27.578947368421,-2.65));
#26406=CARTESIAN_POINT('Ctrl Pts',(5.29999999999999,27.7763157894737,-1.42013071988495));
#26407=CARTESIAN_POINT('Ctrl Pts',(5.29999999999999,27.9736842105263,-9.73594205322067E-16));
#26408=CARTESIAN_POINT('Ctrl Pts',(5.29999999999999,28.1710526315789,1.42013071988494));
#26409=CARTESIAN_POINT('Ctrl Pts',(4.58993464005752,28.3684210526316,2.64999999999999));
#26410=CARTESIAN_POINT('Ctrl Pts',(3.87986928011504,28.5657894736842,3.87986928011504));
#26411=CARTESIAN_POINT('Ctrl Pts',(2.65,28.7631578947368,4.58993464005752));
#26412=CARTESIAN_POINT('Ctrl Pts',(1.42013071988495,28.9605263157895,5.29999999999999));
#26413=CARTESIAN_POINT('Ctrl Pts',(3.48978505922967E-28,29.1578947368422,
5.29999999999999));
#26414=CARTESIAN_POINT('Ctrl Pts',(-1.42013071988495,29.3552631578947,5.29999999999999));
#26415=CARTESIAN_POINT('Ctrl Pts',(-2.65,29.5526315789474,4.58993464005751));
#26416=CARTESIAN_POINT('Ctrl Pts',(-3.87986928011504,29.75,3.87986928011504));
#26417=CARTESIAN_POINT('Ctrl Pts',(-4.58993464005752,29.9473684210527,2.65));
#26418=CARTESIAN_POINT('Ctrl Pts',(-5.29999999999999,30.1447368421053,1.42013071988495));
#26419=CARTESIAN_POINT('Ctrl Pts',(-5.29999999999999,30.3421052631579,3.24531401773979E-16));
#26420=CARTESIAN_POINT('Ctrl Pts',(-5.29999999999999,30.5394736842105,-1.42013071988495));
#26421=CARTESIAN_POINT('Ctrl Pts',(-4.58993464005752,30.7368421052631,-2.65));
#26422=CARTESIAN_POINT('Ctrl Pts',(-3.87986928011504,30.9342105263158,-3.87986928011504));
#26423=CARTESIAN_POINT('Ctrl Pts',(-2.65,31.1315789473684,-4.58993464005752));
#26424=CARTESIAN_POINT('Ctrl Pts',(-1.42013071988495,31.328947368421,-5.29999999999999));
#26425=CARTESIAN_POINT('Ctrl Pts',(-6.49062803547778E-16,31.5263157894736,
-5.29999999999999));
#26426=CARTESIAN_POINT('Ctrl Pts',(1.42013071988495,31.7236842105263,-5.29999999999999));
#26427=CARTESIAN_POINT('Ctrl Pts',(2.65,31.9210526315789,-4.58993464005752));
#26428=CARTESIAN_POINT('Ctrl Pts',(3.87986928011504,32.1184210526316,-3.87986928011504));
#26429=CARTESIAN_POINT('Ctrl Pts',(4.58993464005752,32.3157894736842,-2.65));
#26430=CARTESIAN_POINT('Ctrl Pts',(5.29999999999999,32.5131578947368,-1.42013071988495));
#26431=CARTESIAN_POINT('Ctrl Pts',(5.29999999999999,32.7105263157895,-9.73594205322215E-16));
#26432=CARTESIAN_POINT('Ctrl Pts',(5.29999999999999,32.9078947368421,1.42013071988495));
#26433=CARTESIAN_POINT('Ctrl Pts',(4.58993464005752,33.1052631578947,2.64999999999999));
#26434=CARTESIAN_POINT('Ctrl Pts',(3.87986928011504,33.3026315789474,3.87986928011504));
#26435=CARTESIAN_POINT('Ctrl Pts',(2.65,33.5,4.58993464005751));
#26436=CARTESIAN_POINT('Ctrl Pts',(1.42013071988495,33.6973684210527,5.29999999999999));
#26437=CARTESIAN_POINT('Ctrl Pts',(4.06756404254584E-28,33.8947368421053,
5.29999999999999));
#26438=CARTESIAN_POINT('Ctrl Pts',(-1.42013071988495,34.0921052631579,5.29999999999999));
#26439=CARTESIAN_POINT('Ctrl Pts',(-2.65,34.2894736842105,4.58993464005752));
#26440=CARTESIAN_POINT('Ctrl Pts',(-3.87986928011504,34.4868421052632,3.87986928011504));
#26441=CARTESIAN_POINT('Ctrl Pts',(-4.58993464005752,34.6842105263158,2.65));
#26442=CARTESIAN_POINT('Ctrl Pts',(-5.29999999999999,34.8815789473684,1.42013071988495));
#26443=CARTESIAN_POINT('Ctrl Pts',(-5.29999999999999,35.078947368421,3.24531401773979E-16));
#26444=CARTESIAN_POINT('Ctrl Pts',(-5.29999999999999,35.2763157894737,-1.42013071988495));
#26445=CARTESIAN_POINT('Ctrl Pts',(-4.58993464005752,35.4736842105263,-2.65));
#26446=CARTESIAN_POINT('Ctrl Pts',(-3.87986928011504,35.6710526315789,-3.87986928011504));
#26447=CARTESIAN_POINT('Ctrl Pts',(-2.65,35.8684210526316,-4.58993464005752));
#26448=CARTESIAN_POINT('Ctrl Pts',(-1.42013071988495,36.0657894736842,-5.29999999999999));
#26449=CARTESIAN_POINT('Ctrl Pts',(-6.4906280354773E-16,36.2631578947368,
-5.3));
#26450=CARTESIAN_POINT('Ctrl Pts',(1.42013071988495,36.4605263157895,-5.29999999999999));
#26451=CARTESIAN_POINT('Ctrl Pts',(2.65,36.6578947368421,-4.58993464005752));
#26452=CARTESIAN_POINT('Ctrl Pts',(3.87986928011504,36.8552631578947,-3.87986928011504));
#26453=CARTESIAN_POINT('Ctrl Pts',(4.58993464005752,37.0526315789474,-2.65));
#26454=CARTESIAN_POINT('Ctrl Pts',(5.29999999999999,37.25,-1.42013071988495));
#26455=CARTESIAN_POINT('Ctrl Pts',(5.29999999999999,37.4473684210526,-9.73594205322067E-16));
#26456=CARTESIAN_POINT('Ctrl Pts',(5.29999999999999,37.6447368421053,1.42013071988495));
#26457=CARTESIAN_POINT('Ctrl Pts',(4.58993464005752,37.8421052631579,2.64999999999999));
#26458=CARTESIAN_POINT('Ctrl Pts',(3.87986928011504,38.0394736842105,3.87986928011504));
#26459=CARTESIAN_POINT('Ctrl Pts',(2.65,38.2368421052632,4.58993464005752));
#26460=CARTESIAN_POINT('Ctrl Pts',(1.42013071988495,38.4342105263158,5.29999999999999));
#26461=CARTESIAN_POINT('Ctrl Pts',(4.50667606986613E-28,38.6315789473685,
5.29999999999999));
#26462=CARTESIAN_POINT('Ctrl Pts',(-1.42013071988495,38.8289473684211,5.29999999999999));
#26463=CARTESIAN_POINT('Ctrl Pts',(-2.65,39.0263157894737,4.58993464005752));
#26464=CARTESIAN_POINT('Ctrl Pts',(-3.87986928011504,39.2236842105263,3.87986928011504));
#26465=CARTESIAN_POINT('Ctrl Pts',(-4.58993464005752,39.4210526315789,2.65));
#26466=CARTESIAN_POINT('Ctrl Pts',(-5.29999999999999,39.6184210526316,1.42013071988495));
#26467=CARTESIAN_POINT('Ctrl Pts',(-5.29999999999999,39.8157894736842,3.24531401773979E-16));
#26468=CARTESIAN_POINT('Ctrl Pts',(-5.29999999999999,40.0131578947369,-1.42013071988495));
#26469=CARTESIAN_POINT('Ctrl Pts',(-4.58993464005752,40.2105263157895,-2.64999999999999));
#26470=CARTESIAN_POINT('Ctrl Pts',(-3.87986928011504,40.4078947368421,-3.87986928011504));
#26471=CARTESIAN_POINT('Ctrl Pts',(-2.65,40.6052631578947,-4.58993464005752));
#26472=CARTESIAN_POINT('Ctrl Pts',(-1.42013071988495,40.8026315789473,-5.29999999999999));
#26473=CARTESIAN_POINT('Ctrl Pts',(-6.49062803547674E-16,40.9999999999999,
-5.29999999999999));
#26474=CARTESIAN_POINT('Ctrl Pts',(1.42013071988495,41.1973684210526,-5.29999999999999));
#26475=CARTESIAN_POINT('Ctrl Pts',(2.65,41.3947368421053,-4.58993464005752));
#26476=CARTESIAN_POINT('Ctrl Pts',(3.87986928011504,41.5921052631579,-3.87986928011504));
#26477=CARTESIAN_POINT('Ctrl Pts',(4.58993464005752,41.7894736842105,-2.65));
#26478=CARTESIAN_POINT('Ctrl Pts',(5.29999999999999,41.9868421052632,-1.42013071988495));
#26479=CARTESIAN_POINT('Ctrl Pts',(5.29999999999999,42.1842105263158,-9.73594205322067E-16));
#26480=CARTESIAN_POINT('Ctrl Pts',(5.29999999999999,42.3815789473684,1.42013071988495));
#26481=CARTESIAN_POINT('Ctrl Pts',(4.58993464005752,42.5789473684211,2.64999999999999));
#26482=CARTESIAN_POINT('Ctrl Pts',(3.87986928011504,42.7763157894737,3.87986928011504));
#26483=CARTESIAN_POINT('Ctrl Pts',(2.65,42.9736842105263,4.58993464005751));
#26484=CARTESIAN_POINT('Ctrl Pts',(1.42013071988495,43.1710526315789,5.29999999999999));
#26485=CARTESIAN_POINT('Ctrl Pts',(5.06134389384965E-28,43.3684210526316,
5.29999999999999));
#26486=CARTESIAN_POINT('Ctrl Pts',(-1.42013071988495,43.5657894736842,5.29999999999999));
#26487=CARTESIAN_POINT('Ctrl Pts',(-2.65,43.7631578947369,4.58993464005751));
#26488=CARTESIAN_POINT('Ctrl Pts',(-3.87986928011504,43.9605263157895,3.87986928011504));
#26489=CARTESIAN_POINT('Ctrl Pts',(-4.58993464005752,44.1578947368421,2.65));
#26490=CARTESIAN_POINT('Ctrl Pts',(-5.29999999999999,44.3552631578947,1.42013071988495));
#26491=CARTESIAN_POINT('Ctrl Pts',(-5.29999999999999,44.5526315789474,3.24531401774127E-16));
#26492=CARTESIAN_POINT('Ctrl Pts',(-5.29999999999999,44.75,-1.42013071988495));
#26493=CARTESIAN_POINT('Ctrl Pts',(-4.58993464005752,44.9473684210526,-2.64999999999999));
#26494=CARTESIAN_POINT('Ctrl Pts',(-3.87986928011504,45.1447368421053,-3.87986928011504));
#26495=CARTESIAN_POINT('Ctrl Pts',(-2.65,45.3421052631579,-4.58993464005752));
#26496=CARTESIAN_POINT('Ctrl Pts',(-1.42013071988495,45.5394736842105,-5.29999999999999));
#26497=CARTESIAN_POINT('Ctrl Pts',(-6.4906280354762E-16,45.7368421052632,
-5.29999999999999));
#26498=CARTESIAN_POINT('Ctrl Pts',(1.42013071988495,45.9342105263158,-5.29999999999999));
#26499=CARTESIAN_POINT('Ctrl Pts',(2.65,46.1315789473684,-4.58993464005752));
#26500=CARTESIAN_POINT('Ctrl Pts',(3.87986928011504,46.328947368421,-3.87986928011504));
#26501=CARTESIAN_POINT('Ctrl Pts',(4.58993464005752,46.5263157894737,-2.65));
#26502=CARTESIAN_POINT('Ctrl Pts',(5.29999999999999,46.7236842105263,-1.42013071988495));
#26503=CARTESIAN_POINT('Ctrl Pts',(5.29999999999999,46.9210526315789,-9.73594205322067E-16));
#26504=CARTESIAN_POINT('Ctrl Pts',(5.29999999999999,47.1184210526316,1.42013071988494));
#26505=CARTESIAN_POINT('Ctrl Pts',(4.58993464005752,47.3157894736842,2.64999999999999));
#26506=CARTESIAN_POINT('Ctrl Pts',(3.87986928011504,47.5131578947369,3.87986928011504));
#26507=CARTESIAN_POINT('Ctrl Pts',(2.65,47.7105263157895,4.58993464005752));
#26508=CARTESIAN_POINT('Ctrl Pts',(1.42013071988495,47.9078947368421,5.29999999999999));
#26509=CARTESIAN_POINT('Ctrl Pts',(5.54667823983524E-28,48.1052631578947,
5.29999999999999));
#26510=CARTESIAN_POINT('Ctrl Pts',(-1.42013071988495,48.3026315789474,5.29999999999999));
#26511=CARTESIAN_POINT('Ctrl Pts',(-2.65,48.5,4.58993464005752));
#26512=CARTESIAN_POINT('Ctrl Pts',(-3.87986928011504,48.6973684210527,3.87986928011505));
#26513=CARTESIAN_POINT('Ctrl Pts',(-4.58993464005752,48.8947368421053,2.65));
#26514=CARTESIAN_POINT('Ctrl Pts',(-5.29999999999999,49.0921052631579,1.42013071988495));
#26515=CARTESIAN_POINT('Ctrl Pts',(-5.29999999999999,49.2894736842105,3.24531401773979E-16));
#26516=CARTESIAN_POINT('Ctrl Pts',(-5.29999999999999,49.4868421052632,-1.42013071988495));
#26517=CARTESIAN_POINT('Ctrl Pts',(-4.58993464005752,49.6842105263158,-2.65));
#26518=CARTESIAN_POINT('Ctrl Pts',(-3.87986928011504,49.8815789473684,-3.87986928011504));
#26519=CARTESIAN_POINT('Ctrl Pts',(-2.65,50.078947368421,-4.58993464005752));
#26520=CARTESIAN_POINT('Ctrl Pts',(-1.42013071988495,50.2763157894736,-5.29999999999999));
#26521=CARTESIAN_POINT('Ctrl Pts',(-6.49062803547577E-16,50.4736842105263,
-5.3));
#26522=CARTESIAN_POINT('Ctrl Pts',(1.42013071988495,50.6710526315789,-5.29999999999999));
#26523=CARTESIAN_POINT('Ctrl Pts',(2.65,50.8684210526316,-4.58993464005752));
#26524=CARTESIAN_POINT('Ctrl Pts',(3.87986928011504,51.0657894736842,-3.87986928011504));
#26525=CARTESIAN_POINT('Ctrl Pts',(4.58993464005752,51.2631578947368,-2.65));
#26526=CARTESIAN_POINT('Ctrl Pts',(5.29999999999999,51.4605263157895,-1.42013071988495));
#26527=CARTESIAN_POINT('Ctrl Pts',(5.29999999999999,51.6578947368421,-9.73594205321919E-16));
#26528=CARTESIAN_POINT('Ctrl Pts',(5.29999999999999,51.8552631578948,1.42013071988495));
#26529=CARTESIAN_POINT('Ctrl Pts',(4.58993464005752,52.0526315789474,2.64999999999999));
#26530=CARTESIAN_POINT('Ctrl Pts',(3.87986928011504,52.25,3.87986928011504));
#26531=CARTESIAN_POINT('Ctrl Pts',(2.65,52.4473684210527,4.58993464005751));
#26532=CARTESIAN_POINT('Ctrl Pts',(1.42013071988495,52.6447368421053,5.29999999999999));
#26533=CARTESIAN_POINT('Ctrl Pts',(6.07823490448612E-28,52.842105263158,
5.29999999999999));
#26534=CARTESIAN_POINT('Ctrl Pts',(-1.42013071988495,53.0394736842106,5.29999999999999));
#26535=CARTESIAN_POINT('Ctrl Pts',(-2.65,53.2368421052632,4.58993464005751));
#26536=CARTESIAN_POINT('Ctrl Pts',(-3.87986928011504,53.4342105263158,3.87986928011504));
#26537=CARTESIAN_POINT('Ctrl Pts',(-4.58993464005752,53.6315789473684,2.65));
#26538=CARTESIAN_POINT('Ctrl Pts',(-5.29999999999999,53.8289473684211,1.42013071988495));
#26539=CARTESIAN_POINT('Ctrl Pts',(-5.29999999999999,54.0263157894737,3.24531401773979E-16));
#26540=CARTESIAN_POINT('Ctrl Pts',(-5.29999999999999,54.2236842105263,-1.42013071988495));
#26541=CARTESIAN_POINT('Ctrl Pts',(-4.58993464005752,54.4210526315789,-2.65));
#26542=CARTESIAN_POINT('Ctrl Pts',(-3.87986928011504,54.6184210526315,-3.87986928011504));
#26543=CARTESIAN_POINT('Ctrl Pts',(-2.65,54.8157894736842,-4.58993464005752));
#26544=CARTESIAN_POINT('Ctrl Pts',(-1.42013071988495,55.0131578947368,-5.29999999999999));
#26545=CARTESIAN_POINT('Ctrl Pts',(-6.49062803547515E-16,55.2105263157894,
-5.29999999999999));
#26546=CARTESIAN_POINT('Ctrl Pts',(1.42013071988495,55.4078947368421,-5.29999999999999));
#26547=CARTESIAN_POINT('Ctrl Pts',(2.65,55.6052631578947,-4.58993464005752));
#26548=CARTESIAN_POINT('Ctrl Pts',(3.87986928011504,55.8026315789474,-3.87986928011504));
#26549=CARTESIAN_POINT('Ctrl Pts',(4.58993464005752,56.,-2.65));
#26550=CARTESIAN_POINT('Ctrl Pts',(5.29999999999999,56.1973684210526,-1.42013071988495));
#26551=CARTESIAN_POINT('Ctrl Pts',(5.29999999999999,56.3947368421052,-9.73594205322067E-16));
#26552=CARTESIAN_POINT('Ctrl Pts',(5.29999999999999,56.5921052631579,1.42013071988495));
#26553=CARTESIAN_POINT('Ctrl Pts',(4.58993464005752,56.7894736842105,2.64999999999999));
#26554=CARTESIAN_POINT('Ctrl Pts',(3.87986928011504,56.9868421052632,3.87986928011504));
#26555=CARTESIAN_POINT('Ctrl Pts',(2.65,57.1842105263158,4.58993464005751));
#26556=CARTESIAN_POINT('Ctrl Pts',(1.42013071988495,57.3815789473684,5.29999999999999));
#26557=CARTESIAN_POINT('Ctrl Pts',(6.58668040980435E-28,57.5789473684211,
5.29999999999999));
#26558=CARTESIAN_POINT('Ctrl Pts',(-1.42013071988495,57.7763157894737,5.29999999999999));
#26559=CARTESIAN_POINT('Ctrl Pts',(-2.65,57.9736842105264,4.58993464005752));
#26560=CARTESIAN_POINT('Ctrl Pts',(-3.87986928011504,58.171052631579,3.87986928011505));
#26561=CARTESIAN_POINT('Ctrl Pts',(-4.58993464005752,58.3684210526316,2.65));
#26562=CARTESIAN_POINT('Ctrl Pts',(-5.29999999999999,58.5657894736842,1.42013071988495));
#26563=CARTESIAN_POINT('Ctrl Pts',(-5.29999999999999,58.7631578947368,3.24531401774127E-16));
#26564=CARTESIAN_POINT('Ctrl Pts',(-5.29999999999999,58.9605263157895,-1.42013071988495));
#26565=CARTESIAN_POINT('Ctrl Pts',(-4.58993464005752,59.1578947368421,-2.65));
#26566=CARTESIAN_POINT('Ctrl Pts',(-3.87986928011504,59.3552631578947,-3.87986928011504));
#26567=CARTESIAN_POINT('Ctrl Pts',(-2.65,59.5526315789473,-4.58993464005752));
#26568=CARTESIAN_POINT('Ctrl Pts',(-1.42013071988495,59.7499999999999,-5.29999999999999));
#26569=CARTESIAN_POINT('Ctrl Pts',(-6.49062803547467E-16,59.9473684210526,
-5.3));
#26570=CARTESIAN_POINT('Ctrl Pts',(1.42013071988495,60.1447368421052,-5.29999999999999));
#26571=CARTESIAN_POINT('Ctrl Pts',(2.65,60.3421052631579,-4.58993464005752));
#26572=CARTESIAN_POINT('Ctrl Pts',(3.87986928011504,60.5394736842105,-3.87986928011504));
#26573=CARTESIAN_POINT('Ctrl Pts',(4.58993464005752,60.7368421052632,-2.65));
#26574=CARTESIAN_POINT('Ctrl Pts',(5.29999999999999,60.9342105263158,-1.42013071988495));
#26575=CARTESIAN_POINT('Ctrl Pts',(5.29999999999999,61.1315789473684,-9.73594205321919E-16));
#26576=CARTESIAN_POINT('Ctrl Pts',(5.29999999999999,61.328947368421,1.42013071988495));
#26577=CARTESIAN_POINT('Ctrl Pts',(4.58993464005752,61.5263157894737,2.64999999999999));
#26578=CARTESIAN_POINT('Ctrl Pts',(3.87986928011504,61.7236842105263,3.87986928011504));
#26579=CARTESIAN_POINT('Ctrl Pts',(2.65,61.921052631579,4.58993464005752));
#26580=CARTESIAN_POINT('Ctrl Pts',(1.42013071988495,62.1184210526316,5.29999999999999));
#26581=CARTESIAN_POINT('Ctrl Pts',(7.14134823378787E-28,62.3157894736843,
5.29999999999999));
#26582=CARTESIAN_POINT('Ctrl Pts',(-1.42013071988495,62.5131578947369,5.29999999999999));
#26583=CARTESIAN_POINT('Ctrl Pts',(-2.65,62.7105263157895,4.58993464005751));
#26584=CARTESIAN_POINT('Ctrl Pts',(-3.87986928011504,62.9078947368421,3.87986928011504));
#26585=CARTESIAN_POINT('Ctrl Pts',(-4.58993464005752,63.1052631578947,2.65));
#26586=CARTESIAN_POINT('Ctrl Pts',(-5.29999999999999,63.3026315789474,1.42013071988495));
#26587=CARTESIAN_POINT('Ctrl Pts',(-5.29999999999999,63.5,3.24531401774127E-16));
#26588=CARTESIAN_POINT('Ctrl Pts',(-5.29999999999999,63.6973684210526,-1.42013071988495));
#26589=CARTESIAN_POINT('Ctrl Pts',(-4.58993464005752,63.8947368421052,-2.65));
#26590=CARTESIAN_POINT('Ctrl Pts',(-3.87986928011504,64.0921052631579,-3.87986928011504));
#26591=CARTESIAN_POINT('Ctrl Pts',(-2.65,64.2894736842104,-4.58993464005752));
#26592=CARTESIAN_POINT('Ctrl Pts',(-1.42013071988495,64.4868421052631,-5.29999999999999));
#26593=CARTESIAN_POINT('Ctrl Pts',(-6.49062803547417E-16,64.6842105263157,
-5.29999999999999));
#26594=CARTESIAN_POINT('Ctrl Pts',(1.42013071988495,64.8815789473684,-5.29999999999999));
#26595=CARTESIAN_POINT('Ctrl Pts',(2.65,65.078947368421,-4.58993464005752));
#26596=CARTESIAN_POINT('Ctrl Pts',(3.87986928011504,65.2763157894737,-3.87986928011504));
#26597=CARTESIAN_POINT('Ctrl Pts',(4.58993464005752,65.4736842105263,-2.65));
#26598=CARTESIAN_POINT('Ctrl Pts',(5.29999999999999,65.6710526315789,-1.42013071988495));
#26599=CARTESIAN_POINT('Ctrl Pts',(5.29999999999999,65.8684210526316,-9.73594205322067E-16));
#26600=CARTESIAN_POINT('Ctrl Pts',(5.29999999999999,66.0657894736842,1.42013071988495));
#26601=CARTESIAN_POINT('Ctrl Pts',(4.58993464005752,66.2631578947368,2.64999999999999));
#26602=CARTESIAN_POINT('Ctrl Pts',(3.87986928011504,66.4605263157895,3.87986928011504));
#26603=CARTESIAN_POINT('Ctrl Pts',(2.65,66.6578947368421,4.58993464005751));
#26604=CARTESIAN_POINT('Ctrl Pts',(1.42013071988495,66.8552631578948,5.29999999999999));
#26605=CARTESIAN_POINT('Ctrl Pts',(7.62668257977345E-28,67.0526315789474,
5.29999999999999));
#26606=CARTESIAN_POINT('Ctrl Pts',(-1.42013071988495,67.25,5.29999999999999));
#26607=CARTESIAN_POINT('Ctrl Pts',(-2.65,67.4473684210527,4.58993464005752));
#26608=CARTESIAN_POINT('Ctrl Pts',(-3.87986928011504,67.6447368421053,3.87986928011504));
#26609=CARTESIAN_POINT('Ctrl Pts',(-4.58993464005752,67.8421052631579,2.65));
#26610=CARTESIAN_POINT('Ctrl Pts',(-5.29999999999999,68.0394736842105,1.42013071988495));
#26611=CARTESIAN_POINT('Ctrl Pts',(-5.29999999999999,68.2368421052632,3.24531401774127E-16));
#26612=CARTESIAN_POINT('Ctrl Pts',(-5.29999999999999,68.4342105263158,-1.42013071988495));
#26613=CARTESIAN_POINT('Ctrl Pts',(-4.58993464005752,68.6315789473684,-2.65));
#26614=CARTESIAN_POINT('Ctrl Pts',(-3.87986928011504,68.828947368421,-3.87986928011504));
#26615=CARTESIAN_POINT('Ctrl Pts',(-2.65,69.0263157894736,-4.58993464005752));
#26616=CARTESIAN_POINT('Ctrl Pts',(-1.42013071988495,69.2236842105263,-5.29999999999999));
#26617=CARTESIAN_POINT('Ctrl Pts',(-6.49062803547369E-16,69.4210526315789,
-5.3));
#26618=CARTESIAN_POINT('Ctrl Pts',(1.42013071988495,69.6184210526315,-5.29999999999999));
#26619=CARTESIAN_POINT('Ctrl Pts',(2.65,69.8157894736841,-4.58993464005752));
#26620=CARTESIAN_POINT('Ctrl Pts',(3.87986928011504,70.0131578947368,-3.87986928011504));
#26621=CARTESIAN_POINT('Ctrl Pts',(4.58993464005752,70.2105263157894,-2.65));
#26622=CARTESIAN_POINT('Ctrl Pts',(5.29999999999999,70.4078947368421,-1.42013071988495));
#26623=CARTESIAN_POINT('Ctrl Pts',(5.29999999999999,70.6052631578947,-9.73594205322067E-16));
#26624=CARTESIAN_POINT('Ctrl Pts',(5.29999999999999,70.8026315789473,1.42013071988494));
#26625=CARTESIAN_POINT('Ctrl Pts',(4.58993464005752,71.,2.64999999999999));
#26626=CARTESIAN_POINT('Ctrl Pts',(3.87986928011504,71.1973684210527,3.87986928011504));
#26627=CARTESIAN_POINT('Ctrl Pts',(2.65,71.3947368421053,4.58993464005752));
#26628=CARTESIAN_POINT('Ctrl Pts',(1.42013071988495,71.5921052631579,5.29999999999999));
#26629=CARTESIAN_POINT('Ctrl Pts',(8.11201692575904E-28,71.7894736842105,
5.29999999999999));
#26630=CARTESIAN_POINT('Ctrl Pts',(-1.42013071988495,71.9868421052632,5.29999999999999));
#26631=CARTESIAN_POINT('Ctrl Pts',(-2.65,72.1842105263158,4.58993464005752));
#26632=CARTESIAN_POINT('Ctrl Pts',(-3.87986928011504,72.3815789473684,3.87986928011504));
#26633=CARTESIAN_POINT('Ctrl Pts',(-4.58993464005752,72.578947368421,2.65));
#26634=CARTESIAN_POINT('Ctrl Pts',(-5.29999999999999,72.7763157894737,1.42013071988495));
#26635=CARTESIAN_POINT('Ctrl Pts',(-5.29999999999999,72.9736842105263,3.24531401773979E-16));
#26636=CARTESIAN_POINT('Ctrl Pts',(-5.29999999999999,73.171052631579,-1.42013071988495));
#26637=CARTESIAN_POINT('Ctrl Pts',(-4.58993464005752,73.3684210526315,-2.64999999999999));
#26638=CARTESIAN_POINT('Ctrl Pts',(-3.87986928011504,73.5657894736842,-3.87986928011504));
#26639=CARTESIAN_POINT('Ctrl Pts',(-2.65,73.7631578947367,-4.58993464005752));
#26640=CARTESIAN_POINT('Ctrl Pts',(-1.42013071988495,73.9605263157894,-5.29999999999999));
#26641=CARTESIAN_POINT('Ctrl Pts',(-6.49062803547313E-16,74.157894736842,
-5.29999999999999));
#26642=CARTESIAN_POINT('Ctrl Pts',(1.42013071988495,74.3552631578946,-5.29999999999999));
#26643=CARTESIAN_POINT('Ctrl Pts',(2.65,74.5526315789473,-4.58993464005752));
#26644=CARTESIAN_POINT('Ctrl Pts',(3.87986928011504,74.75,-3.87986928011504));
#26645=CARTESIAN_POINT('Ctrl Pts',(4.58993464005752,74.9473684210526,-2.65));
#26646=CARTESIAN_POINT('Ctrl Pts',(5.29999999999999,75.1447368421053,-1.42013071988495));
#26647=CARTESIAN_POINT('Ctrl Pts',(5.29999999999999,75.3421052631579,-9.73594205322067E-16));
#26648=CARTESIAN_POINT('Ctrl Pts',(5.29999999999999,75.5394736842105,1.42013071988495));
#26649=CARTESIAN_POINT('Ctrl Pts',(4.58993464005752,75.7368421052631,2.64999999999999));
#26650=CARTESIAN_POINT('Ctrl Pts',(3.87986928011504,75.9342105263158,3.87986928011504));
#26651=CARTESIAN_POINT('Ctrl Pts',(2.65,76.1315789473684,4.58993464005751));
#26652=CARTESIAN_POINT('Ctrl Pts',(1.42013071988495,76.3289473684211,5.29999999999999));
#26653=CARTESIAN_POINT('Ctrl Pts',(8.70135148874153E-28,76.5263157894737,
5.29999999999999));
#26654=CARTESIAN_POINT('Ctrl Pts',(-1.42013071988495,76.7236842105263,5.29999999999999));
#26655=CARTESIAN_POINT('Ctrl Pts',(-2.65,76.921052631579,4.58993464005751));
#26656=CARTESIAN_POINT('Ctrl Pts',(-3.87986928011504,77.1184210526316,3.87986928011504));
#26657=CARTESIAN_POINT('Ctrl Pts',(-4.58993464005752,77.3157894736842,2.65));
#26658=CARTESIAN_POINT('Ctrl Pts',(-5.29999999999999,77.5131578947368,1.42013071988495));
#26659=CARTESIAN_POINT('Ctrl Pts',(-5.29999999999999,77.7105263157894,3.24531401773979E-16));
#26660=CARTESIAN_POINT('Ctrl Pts',(-5.29999999999999,77.9078947368421,-1.42013071988495));
#26661=CARTESIAN_POINT('Ctrl Pts',(-4.58993464005752,78.1052631578947,-2.64999999999999));
#26662=CARTESIAN_POINT('Ctrl Pts',(-3.87986928011504,78.3026315789474,-3.87986928011504));
#26663=CARTESIAN_POINT('Ctrl Pts',(-2.65,78.5,-4.58993464005752));
#26664=CARTESIAN_POINT('Ctrl Pts',(-1.42013071988495,78.6973684210526,-5.29999999999999));
#26665=CARTESIAN_POINT('Ctrl Pts',(-6.49062803547253E-16,78.8947368421053,
-5.29999999999999));
#26666=CARTESIAN_POINT('Ctrl Pts',(1.42013071988495,79.0921052631579,-5.29999999999999));
#26667=CARTESIAN_POINT('Ctrl Pts',(2.65,79.2894736842105,-4.58993464005752));
#26668=CARTESIAN_POINT('Ctrl Pts',(3.87986928011504,79.4868421052631,-3.87986928011504));
#26669=CARTESIAN_POINT('Ctrl Pts',(4.58993464005752,79.6842105263158,-2.65));
#26670=CARTESIAN_POINT('Ctrl Pts',(5.29999999999999,79.8815789473684,-1.42013071988495));
#26671=CARTESIAN_POINT('Ctrl Pts',(5.29999999999999,80.0789473684211,-9.73594205322067E-16));
#26672=CARTESIAN_POINT('Ctrl Pts',(5.29999999999999,80.2763157894737,1.42013071988495));
#26673=CARTESIAN_POINT('Ctrl Pts',(4.58993464005752,80.4736842105263,2.64999999999999));
#26674=CARTESIAN_POINT('Ctrl Pts',(3.87986928011504,80.671052631579,3.87986928011504));
#26675=CARTESIAN_POINT('Ctrl Pts',(2.65,80.8684210526316,4.58993464005752));
#26676=CARTESIAN_POINT('Ctrl Pts',(1.42013071988495,81.0657894736842,5.29999999999999));
#26677=CARTESIAN_POINT('Ctrl Pts',(9.22135257372608E-28,81.2631578947368,
5.29999999999999));
#26678=CARTESIAN_POINT('Ctrl Pts',(-1.42013071988495,81.4605263157895,5.29999999999999));
#26679=CARTESIAN_POINT('Ctrl Pts',(-2.65,81.6578947368421,4.58993464005752));
#26680=CARTESIAN_POINT('Ctrl Pts',(-3.87986928011504,81.8552631578948,3.87986928011504));
#26681=CARTESIAN_POINT('Ctrl Pts',(-4.58993464005752,82.0526315789474,2.65));
#26682=CARTESIAN_POINT('Ctrl Pts',(-5.29999999999999,82.25,1.42013071988495));
#26683=CARTESIAN_POINT('Ctrl Pts',(-5.29999999999999,82.4473684210526,3.24531401773979E-16));
#26684=CARTESIAN_POINT('Ctrl Pts',(-5.29999999999999,82.6447368421053,-1.42013071988495));
#26685=CARTESIAN_POINT('Ctrl Pts',(-4.58993464005752,82.8421052631579,-2.65));
#26686=CARTESIAN_POINT('Ctrl Pts',(-3.87986928011504,83.0394736842105,-3.87986928011504));
#26687=CARTESIAN_POINT('Ctrl Pts',(-2.65,83.2368421052631,-4.58993464005752));
#26688=CARTESIAN_POINT('Ctrl Pts',(-1.42013071988495,83.4342105263157,-5.29999999999999));
#26689=CARTESIAN_POINT('Ctrl Pts',(-6.49062803547209E-16,83.6315789473684,
-5.3));
#26690=CARTESIAN_POINT('Ctrl Pts',(1.42013071988495,83.828947368421,-5.29999999999999));
#26691=CARTESIAN_POINT('Ctrl Pts',(2.65,84.0263157894736,-4.58993464005752));
#26692=CARTESIAN_POINT('Ctrl Pts',(3.87986928011504,84.2236842105263,-3.87986928011504));
#26693=CARTESIAN_POINT('Ctrl Pts',(4.58993464005752,84.4210526315789,-2.65));
#26694=CARTESIAN_POINT('Ctrl Pts',(5.29999999999999,84.6184210526316,-1.42013071988495));
#26695=CARTESIAN_POINT('Ctrl Pts',(5.29999999999999,84.8157894736842,-9.73594205321179E-16));
#26696=CARTESIAN_POINT('Ctrl Pts',(5.29999999999999,85.0131578947368,1.42013071988495));
#26697=CARTESIAN_POINT('Ctrl Pts',(4.58993464005752,85.2105263157895,2.64999999999999));
#26698=CARTESIAN_POINT('Ctrl Pts',(3.87986928011504,85.4078947368421,3.87986928011504));
#26699=CARTESIAN_POINT('Ctrl Pts',(2.65,85.6052631578948,4.58993464005751));
#26700=CARTESIAN_POINT('Ctrl Pts',(1.42013071988495,85.8026315789474,5.29999999999999));
#26701=CARTESIAN_POINT('Ctrl Pts',(9.70668691971167E-28,86.0000000000001,
5.29999999999999));
#26702=CARTESIAN_POINT('Ctrl Pts',(2.77333911991762E-29,0.,5.29999999999999));
#26703=CARTESIAN_POINT('Ctrl Pts',(-1.42013071988495,0.197368421052638,
5.29999999999998));
#26704=CARTESIAN_POINT('Ctrl Pts',(-2.65,0.394736842105281,4.58993464005751));
#26705=CARTESIAN_POINT('Ctrl Pts',(-3.87986928011504,0.592105263157915,
3.87986928011505));
#26706=CARTESIAN_POINT('Ctrl Pts',(-4.58993464005751,0.789473684210562,
2.65));
#26707=CARTESIAN_POINT('Ctrl Pts',(-5.29999999999999,0.986842105263191,
1.42013071988495));
#26708=CARTESIAN_POINT('Ctrl Pts',(-5.29999999999999,1.18421052631579,3.24531401774024E-16));
#26709=CARTESIAN_POINT('Ctrl Pts',(-5.29999999999999,1.38157894736841,-1.42013071988495));
#26710=CARTESIAN_POINT('Ctrl Pts',(-4.58993464005751,1.57894736842107,-2.64999999999999));
#26711=CARTESIAN_POINT('Ctrl Pts',(-3.87986928011504,1.77631578947369,-3.87986928011504));
#26712=CARTESIAN_POINT('Ctrl Pts',(-2.65,1.97368421052629,-4.58993464005751));
#26713=CARTESIAN_POINT('Ctrl Pts',(-1.42013071988495,2.17105263157891,-5.29999999999999));
#26714=CARTESIAN_POINT('Ctrl Pts',(-6.49062803548097E-16,2.36842105263158,
-5.29999999999999));
#26715=CARTESIAN_POINT('Ctrl Pts',(1.42013071988495,2.56578947368418,-5.29999999999999));
#26716=CARTESIAN_POINT('Ctrl Pts',(2.64999999999999,2.7631578947368,-4.58993464005751));
#26717=CARTESIAN_POINT('Ctrl Pts',(3.87986928011504,2.96052631578946,-3.87986928011505));
#26718=CARTESIAN_POINT('Ctrl Pts',(4.58993464005751,3.15789473684208,-2.65));
#26719=CARTESIAN_POINT('Ctrl Pts',(5.29999999999999,3.35526315789473,-1.42013071988495));
#26720=CARTESIAN_POINT('Ctrl Pts',(5.29999999999999,3.55263157894736,-9.73594205321085E-16));
#26721=CARTESIAN_POINT('Ctrl Pts',(5.29999999999999,3.75000000000001,1.42013071988494));
#26722=CARTESIAN_POINT('Ctrl Pts',(4.58993464005752,3.94736842105264,2.64999999999999));
#26723=CARTESIAN_POINT('Ctrl Pts',(3.87986928011505,4.14473684210529,3.87986928011504));
#26724=CARTESIAN_POINT('Ctrl Pts',(2.65,4.34210526315792,4.58993464005751));
#26725=CARTESIAN_POINT('Ctrl Pts',(1.42013071988495,4.53947368421056,5.29999999999998));
#26726=CARTESIAN_POINT('Ctrl Pts',(8.32001735975286E-29,4.73684210526315,
5.29999999999999));
#26727=CARTESIAN_POINT('Ctrl Pts',(-1.42013071988495,4.93421052631578,5.29999999999999));
#26728=CARTESIAN_POINT('Ctrl Pts',(-2.65,5.13157894736843,4.58993464005751));
#26729=CARTESIAN_POINT('Ctrl Pts',(-3.87986928011504,5.32894736842106,3.87986928011505));
#26730=CARTESIAN_POINT('Ctrl Pts',(-4.58993464005751,5.52631578947371,2.65));
#26731=CARTESIAN_POINT('Ctrl Pts',(-5.29999999999999,5.72368421052634,1.42013071988495));
#26732=CARTESIAN_POINT('Ctrl Pts',(-5.29999999999999,5.92105263157894,3.24531401774024E-16));
#26733=CARTESIAN_POINT('Ctrl Pts',(-5.29999999999999,6.11842105263156,-1.42013071988495));
#26734=CARTESIAN_POINT('Ctrl Pts',(-4.58993464005751,6.31578947368422,-2.64999999999999));
#26735=CARTESIAN_POINT('Ctrl Pts',(-3.87986928011504,6.51315789473683,-3.87986928011504));
#26736=CARTESIAN_POINT('Ctrl Pts',(-2.65,6.71052631578944,-4.58993464005751));
#26737=CARTESIAN_POINT('Ctrl Pts',(-1.42013071988495,6.90789473684211,-5.29999999999999));
#26738=CARTESIAN_POINT('Ctrl Pts',(-6.49062803548043E-16,7.10526315789473,
-5.29999999999999));
#26739=CARTESIAN_POINT('Ctrl Pts',(1.42013071988495,7.30263157894733,-5.29999999999999));
#26740=CARTESIAN_POINT('Ctrl Pts',(2.64999999999999,7.50000000000001,-4.58993464005751));
#26741=CARTESIAN_POINT('Ctrl Pts',(3.87986928011504,7.69736842105261,-3.87986928011505));
#26742=CARTESIAN_POINT('Ctrl Pts',(4.58993464005751,7.89473684210523,-2.65));
#26743=CARTESIAN_POINT('Ctrl Pts',(5.29999999999999,8.09210526315788,-1.42013071988495));
#26744=CARTESIAN_POINT('Ctrl Pts',(5.29999999999999,8.28947368421051,-9.73594205321085E-16));
#26745=CARTESIAN_POINT('Ctrl Pts',(5.29999999999999,8.48684210526316,1.42013071988495));
#26746=CARTESIAN_POINT('Ctrl Pts',(4.58993464005752,8.68421052631579,2.64999999999999));
#26747=CARTESIAN_POINT('Ctrl Pts',(3.87986928011505,8.88157894736843,3.87986928011504));
#26748=CARTESIAN_POINT('Ctrl Pts',(2.65,9.07894736842108,4.58993464005751));
#26749=CARTESIAN_POINT('Ctrl Pts',(1.42013071988495,9.27631578947371,5.29999999999999));
#26750=CARTESIAN_POINT('Ctrl Pts',(1.35585468084861E-28,9.47368421052636,
5.3));
#26751=CARTESIAN_POINT('Ctrl Pts',(-1.42013071988495,9.67105263157899,5.29999999999998));
#26752=CARTESIAN_POINT('Ctrl Pts',(-2.65,9.86842105263158,4.58993464005751));
#26753=CARTESIAN_POINT('Ctrl Pts',(-3.87986928011504,10.0657894736842,3.87986928011504));
#26754=CARTESIAN_POINT('Ctrl Pts',(-4.58993464005751,10.2631578947369,2.65));
#26755=CARTESIAN_POINT('Ctrl Pts',(-5.29999999999999,10.4605263157895,1.42013071988495));
#26756=CARTESIAN_POINT('Ctrl Pts',(-5.29999999999999,10.6578947368421,3.24531401772841E-16));
#26757=CARTESIAN_POINT('Ctrl Pts',(-5.29999999999999,10.8552631578948,-1.42013071988495));
#26758=CARTESIAN_POINT('Ctrl Pts',(-4.58993464005751,11.0526315789474,-2.64999999999999));
#26759=CARTESIAN_POINT('Ctrl Pts',(-3.87986928011504,11.25,-3.87986928011504));
#26760=CARTESIAN_POINT('Ctrl Pts',(-2.65,11.4473684210526,-4.58993464005751));
#26761=CARTESIAN_POINT('Ctrl Pts',(-1.42013071988495,11.6447368421052,-5.29999999999999));
#26762=CARTESIAN_POINT('Ctrl Pts',(-6.49062803547995E-16,11.8421052631579,
-5.29999999999999));
#26763=CARTESIAN_POINT('Ctrl Pts',(1.42013071988495,12.0394736842105,-5.29999999999999));
#26764=CARTESIAN_POINT('Ctrl Pts',(2.64999999999999,12.2368421052632,-4.58993464005751));
#26765=CARTESIAN_POINT('Ctrl Pts',(3.87986928011504,12.4342105263158,-3.87986928011505));
#26766=CARTESIAN_POINT('Ctrl Pts',(4.58993464005751,12.6315789473684,-2.65));
#26767=CARTESIAN_POINT('Ctrl Pts',(5.29999999999999,12.828947368421,-1.42013071988495));
#26768=CARTESIAN_POINT('Ctrl Pts',(5.29999999999999,13.0263157894737,-9.73594205322072E-16));
#26769=CARTESIAN_POINT('Ctrl Pts',(5.29999999999999,13.2236842105263,1.42013071988495));
#26770=CARTESIAN_POINT('Ctrl Pts',(4.58993464005752,13.4210526315789,2.64999999999999));
#26771=CARTESIAN_POINT('Ctrl Pts',(3.87986928011505,13.6184210526316,3.87986928011504));
#26772=CARTESIAN_POINT('Ctrl Pts',(2.65,13.8157894736842,4.58993464005751));
#26773=CARTESIAN_POINT('Ctrl Pts',(1.42013071988495,14.0131578947369,5.29999999999998));
#26774=CARTESIAN_POINT('Ctrl Pts',(1.84889274661175E-28,14.2105263157895,
5.3));
#26775=CARTESIAN_POINT('Ctrl Pts',(-1.42013071988495,14.4078947368421,5.29999999999999));
#26776=CARTESIAN_POINT('Ctrl Pts',(-2.65,14.6052631578947,4.58993464005751));
#26777=CARTESIAN_POINT('Ctrl Pts',(-3.87986928011504,14.8026315789474,3.87986928011504));
#26778=CARTESIAN_POINT('Ctrl Pts',(-4.58993464005751,15.,2.65));
#26779=CARTESIAN_POINT('Ctrl Pts',(-5.29999999999999,15.1973684210526,1.42013071988495));
#26780=CARTESIAN_POINT('Ctrl Pts',(-5.29999999999999,15.3947368421052,3.24531401774024E-16));
#26781=CARTESIAN_POINT('Ctrl Pts',(-5.29999999999999,15.5921052631579,-1.42013071988495));
#26782=CARTESIAN_POINT('Ctrl Pts',(-4.58993464005751,15.7894736842105,-2.64999999999999));
#26783=CARTESIAN_POINT('Ctrl Pts',(-3.87986928011504,15.9868421052631,-3.87986928011504));
#26784=CARTESIAN_POINT('Ctrl Pts',(-2.65,16.1842105263157,-4.58993464005751));
#26785=CARTESIAN_POINT('Ctrl Pts',(-1.42013071988495,16.3815789473684,-5.29999999999999));
#26786=CARTESIAN_POINT('Ctrl Pts',(-6.49062803547949E-16,16.578947368421,
-5.29999999999999));
#26787=CARTESIAN_POINT('Ctrl Pts',(1.42013071988495,16.7763157894737,-5.29999999999999));
#26788=CARTESIAN_POINT('Ctrl Pts',(2.64999999999999,16.9736842105263,-4.58993464005751));
#26789=CARTESIAN_POINT('Ctrl Pts',(3.87986928011504,17.171052631579,-3.87986928011505));
#26790=CARTESIAN_POINT('Ctrl Pts',(4.58993464005751,17.3684210526316,-2.65));
#26791=CARTESIAN_POINT('Ctrl Pts',(5.29999999999999,17.5657894736842,-1.42013071988495));
#26792=CARTESIAN_POINT('Ctrl Pts',(5.29999999999999,17.7631578947368,-9.73594205322269E-16));
#26793=CARTESIAN_POINT('Ctrl Pts',(5.29999999999999,17.9605263157895,1.42013071988494));
#26794=CARTESIAN_POINT('Ctrl Pts',(4.58993464005752,18.1578947368421,2.64999999999999));
#26795=CARTESIAN_POINT('Ctrl Pts',(3.87986928011505,18.3552631578947,3.87986928011504));
#26796=CARTESIAN_POINT('Ctrl Pts',(2.65,18.5526315789474,4.58993464005751));
#26797=CARTESIAN_POINT('Ctrl Pts',(1.42013071988495,18.75,5.29999999999998));
#26798=CARTESIAN_POINT('Ctrl Pts',(2.31111593326468E-28,18.9473684210527,
5.3));
#26799=CARTESIAN_POINT('Ctrl Pts',(-1.42013071988495,19.1447368421053,5.29999999999999));
#26800=CARTESIAN_POINT('Ctrl Pts',(-2.65,19.3421052631579,4.58993464005751));
#26801=CARTESIAN_POINT('Ctrl Pts',(-3.87986928011504,19.5394736842105,3.87986928011504));
#26802=CARTESIAN_POINT('Ctrl Pts',(-4.58993464005751,19.7368421052632,2.65));
#26803=CARTESIAN_POINT('Ctrl Pts',(-5.29999999999999,19.9342105263158,1.42013071988495));
#26804=CARTESIAN_POINT('Ctrl Pts',(-5.29999999999999,20.1315789473684,3.24531401774221E-16));
#26805=CARTESIAN_POINT('Ctrl Pts',(-5.29999999999999,20.328947368421,-1.42013071988495));
#26806=CARTESIAN_POINT('Ctrl Pts',(-4.58993464005751,20.5263157894737,-2.64999999999999));
#26807=CARTESIAN_POINT('Ctrl Pts',(-3.87986928011504,20.7236842105263,-3.87986928011504));
#26808=CARTESIAN_POINT('Ctrl Pts',(-2.65,20.921052631579,-4.58993464005751));
#26809=CARTESIAN_POINT('Ctrl Pts',(-1.42013071988495,21.1184210526315,-5.29999999999999));
#26810=CARTESIAN_POINT('Ctrl Pts',(-6.49062803547894E-16,21.3157894736842,
-5.29999999999999));
#26811=CARTESIAN_POINT('Ctrl Pts',(1.42013071988495,21.5131578947368,-5.29999999999999));
#26812=CARTESIAN_POINT('Ctrl Pts',(2.64999999999999,21.7105263157895,-4.58993464005751));
#26813=CARTESIAN_POINT('Ctrl Pts',(3.87986928011504,21.9078947368421,-3.87986928011505));
#26814=CARTESIAN_POINT('Ctrl Pts',(4.58993464005751,22.1052631578947,-2.65));
#26815=CARTESIAN_POINT('Ctrl Pts',(5.29999999999999,22.3026315789474,-1.42013071988495));
#26816=CARTESIAN_POINT('Ctrl Pts',(5.29999999999999,22.5,-9.73594205320888E-16));
#26817=CARTESIAN_POINT('Ctrl Pts',(5.29999999999999,22.6973684210527,1.42013071988495));
#26818=CARTESIAN_POINT('Ctrl Pts',(4.58993464005752,22.8947368421052,2.64999999999999));
#26819=CARTESIAN_POINT('Ctrl Pts',(3.87986928011505,23.0921052631579,3.87986928011504));
#26820=CARTESIAN_POINT('Ctrl Pts',(2.65,23.2894736842105,4.58993464005751));
#26821=CARTESIAN_POINT('Ctrl Pts',(1.42013071988495,23.4868421052631,5.29999999999999));
#26822=CARTESIAN_POINT('Ctrl Pts',(2.95822839457879E-28,23.6842105263158,
5.3));
#26823=CARTESIAN_POINT('Ctrl Pts',(-1.42013071988495,23.8815789473684,5.29999999999998));
#26824=CARTESIAN_POINT('Ctrl Pts',(-2.65,24.0789473684211,4.58993464005751));
#26825=CARTESIAN_POINT('Ctrl Pts',(-3.87986928011504,24.2763157894737,3.87986928011504));
#26826=CARTESIAN_POINT('Ctrl Pts',(-4.58993464005751,24.4736842105263,2.65));
#26827=CARTESIAN_POINT('Ctrl Pts',(-5.29999999999999,24.671052631579,1.42013071988495));
#26828=CARTESIAN_POINT('Ctrl Pts',(-5.29999999999999,24.8684210526316,3.24531401774024E-16));
#26829=CARTESIAN_POINT('Ctrl Pts',(-5.29999999999999,25.0657894736842,-1.42013071988495));
#26830=CARTESIAN_POINT('Ctrl Pts',(-4.58993464005751,25.2631578947368,-2.64999999999999));
#26831=CARTESIAN_POINT('Ctrl Pts',(-3.87986928011504,25.4605263157895,-3.87986928011504));
#26832=CARTESIAN_POINT('Ctrl Pts',(-2.65,25.6578947368421,-4.58993464005751));
#26833=CARTESIAN_POINT('Ctrl Pts',(-1.42013071988495,25.8552631578947,-5.29999999999999));
#26834=CARTESIAN_POINT('Ctrl Pts',(-6.49062803547834E-16,26.0526315789473,
-5.29999999999999));
#26835=CARTESIAN_POINT('Ctrl Pts',(1.42013071988495,26.25,-5.29999999999999));
#26836=CARTESIAN_POINT('Ctrl Pts',(2.64999999999999,26.4473684210526,-4.58993464005752));
#26837=CARTESIAN_POINT('Ctrl Pts',(3.87986928011504,26.6447368421052,-3.87986928011505));
#26838=CARTESIAN_POINT('Ctrl Pts',(4.58993464005751,26.8421052631579,-2.65));
#26839=CARTESIAN_POINT('Ctrl Pts',(5.29999999999999,27.0394736842105,-1.42013071988495));
#26840=CARTESIAN_POINT('Ctrl Pts',(5.29999999999999,27.2368421052632,-9.73594205320888E-16));
#26841=CARTESIAN_POINT('Ctrl Pts',(5.29999999999999,27.4342105263158,1.42013071988495));
#26842=CARTESIAN_POINT('Ctrl Pts',(4.58993464005752,27.6315789473685,2.64999999999999));
#26843=CARTESIAN_POINT('Ctrl Pts',(3.87986928011505,27.8289473684211,3.87986928011504));
#26844=CARTESIAN_POINT('Ctrl Pts',(2.65,28.0263157894737,4.58993464005751));
#26845=CARTESIAN_POINT('Ctrl Pts',(1.42013071988495,28.2236842105264,5.29999999999998));
#26846=CARTESIAN_POINT('Ctrl Pts',(3.42045158123173E-28,28.421052631579,
5.3));
#26847=CARTESIAN_POINT('Ctrl Pts',(-1.42013071988495,28.6184210526316,5.29999999999999));
#26848=CARTESIAN_POINT('Ctrl Pts',(-2.65,28.8157894736842,4.58993464005751));
#26849=CARTESIAN_POINT('Ctrl Pts',(-3.87986928011504,29.0131578947368,3.87986928011504));
#26850=CARTESIAN_POINT('Ctrl Pts',(-4.58993464005751,29.2105263157895,2.65));
#26851=CARTESIAN_POINT('Ctrl Pts',(-5.29999999999999,29.4078947368421,1.42013071988495));
#26852=CARTESIAN_POINT('Ctrl Pts',(-5.29999999999999,29.6052631578947,3.24531401774024E-16));
#26853=CARTESIAN_POINT('Ctrl Pts',(-5.29999999999999,29.8026315789473,-1.42013071988495));
#26854=CARTESIAN_POINT('Ctrl Pts',(-4.58993464005751,30.,-2.64999999999999));
#26855=CARTESIAN_POINT('Ctrl Pts',(-3.87986928011504,30.1973684210526,-3.87986928011504));
#26856=CARTESIAN_POINT('Ctrl Pts',(-2.65,30.3947368421053,-4.58993464005751));
#26857=CARTESIAN_POINT('Ctrl Pts',(-1.42013071988495,30.5921052631579,-5.29999999999999));
#26858=CARTESIAN_POINT('Ctrl Pts',(-6.49062803547783E-16,30.7894736842105,
-5.29999999999999));
#26859=CARTESIAN_POINT('Ctrl Pts',(1.42013071988495,30.9868421052631,-5.29999999999999));
#26860=CARTESIAN_POINT('Ctrl Pts',(2.64999999999999,31.1842105263158,-4.58993464005752));
#26861=CARTESIAN_POINT('Ctrl Pts',(3.87986928011504,31.3815789473684,-3.87986928011505));
#26862=CARTESIAN_POINT('Ctrl Pts',(4.58993464005751,31.578947368421,-2.65));
#26863=CARTESIAN_POINT('Ctrl Pts',(5.29999999999999,31.7763157894737,-1.42013071988495));
#26864=CARTESIAN_POINT('Ctrl Pts',(5.29999999999999,31.9736842105263,-9.73594205321085E-16));
#26865=CARTESIAN_POINT('Ctrl Pts',(5.29999999999999,32.1710526315789,1.42013071988495));
#26866=CARTESIAN_POINT('Ctrl Pts',(4.58993464005752,32.3684210526316,2.64999999999999));
#26867=CARTESIAN_POINT('Ctrl Pts',(3.87986928011505,32.5657894736842,3.87986928011504));
#26868=CARTESIAN_POINT('Ctrl Pts',(2.65,32.7631578947368,4.58993464005751));
#26869=CARTESIAN_POINT('Ctrl Pts',(1.42013071988495,32.9605263157895,5.29999999999999));
#26870=CARTESIAN_POINT('Ctrl Pts',(3.88267476788467E-28,33.1578947368421,
5.3));
#26871=CARTESIAN_POINT('Ctrl Pts',(-1.42013071988495,33.3552631578948,5.29999999999998));
#26872=CARTESIAN_POINT('Ctrl Pts',(-2.65,33.5526315789474,4.58993464005751));
#26873=CARTESIAN_POINT('Ctrl Pts',(-3.87986928011504,33.75,3.87986928011505));
#26874=CARTESIAN_POINT('Ctrl Pts',(-4.58993464005751,33.9473684210526,2.65));
#26875=CARTESIAN_POINT('Ctrl Pts',(-5.29999999999999,34.1447368421052,1.42013071988495));
#26876=CARTESIAN_POINT('Ctrl Pts',(-5.29999999999999,34.3421052631579,3.24531401774024E-16));
#26877=CARTESIAN_POINT('Ctrl Pts',(-5.29999999999999,34.5394736842105,-1.42013071988495));
#26878=CARTESIAN_POINT('Ctrl Pts',(-4.58993464005751,34.7368421052631,-2.65));
#26879=CARTESIAN_POINT('Ctrl Pts',(-3.87986928011504,34.9342105263158,-3.87986928011504));
#26880=CARTESIAN_POINT('Ctrl Pts',(-2.65,35.1315789473684,-4.58993464005751));
#26881=CARTESIAN_POINT('Ctrl Pts',(-1.42013071988495,35.328947368421,-5.29999999999999));
#26882=CARTESIAN_POINT('Ctrl Pts',(-6.49062803547736E-16,35.5263157894737,
-5.29999999999999));
#26883=CARTESIAN_POINT('Ctrl Pts',(1.42013071988495,35.7236842105263,-5.29999999999999));
#26884=CARTESIAN_POINT('Ctrl Pts',(2.64999999999999,35.9210526315789,-4.58993464005752));
#26885=CARTESIAN_POINT('Ctrl Pts',(3.87986928011504,36.1184210526315,-3.87986928011505));
#26886=CARTESIAN_POINT('Ctrl Pts',(4.58993464005751,36.3157894736842,-2.65));
#26887=CARTESIAN_POINT('Ctrl Pts',(5.29999999999999,36.5131578947368,-1.42013071988495));
#26888=CARTESIAN_POINT('Ctrl Pts',(5.29999999999999,36.7105263157895,-9.73594205322072E-16));
#26889=CARTESIAN_POINT('Ctrl Pts',(5.29999999999999,36.9078947368421,1.42013071988495));
#26890=CARTESIAN_POINT('Ctrl Pts',(4.58993464005752,37.1052631578948,2.64999999999999));
#26891=CARTESIAN_POINT('Ctrl Pts',(3.87986928011505,37.3026315789473,3.87986928011504));
#26892=CARTESIAN_POINT('Ctrl Pts',(2.65,37.5,4.58993464005751));
#26893=CARTESIAN_POINT('Ctrl Pts',(1.42013071988495,37.6973684210526,5.29999999999998));
#26894=CARTESIAN_POINT('Ctrl Pts',(4.42193515231309E-28,37.8947368421053,
5.29999999999999));
#26895=CARTESIAN_POINT('Ctrl Pts',(-1.42013071988495,38.0921052631579,5.29999999999999));
#26896=CARTESIAN_POINT('Ctrl Pts',(-2.65,38.2894736842105,4.58993464005752));
#26897=CARTESIAN_POINT('Ctrl Pts',(-3.87986928011504,38.4868421052632,3.87986928011504));
#26898=CARTESIAN_POINT('Ctrl Pts',(-4.58993464005751,38.6842105263158,2.65));
#26899=CARTESIAN_POINT('Ctrl Pts',(-5.29999999999999,38.8815789473684,1.42013071988495));
#26900=CARTESIAN_POINT('Ctrl Pts',(-5.29999999999999,39.078947368421,3.24531401774024E-16));
#26901=CARTESIAN_POINT('Ctrl Pts',(-5.29999999999999,39.2763157894737,-1.42013071988495));
#26902=CARTESIAN_POINT('Ctrl Pts',(-4.58993464005751,39.4736842105263,-2.64999999999999));
#26903=CARTESIAN_POINT('Ctrl Pts',(-3.87986928011504,39.6710526315789,-3.87986928011504));
#26904=CARTESIAN_POINT('Ctrl Pts',(-2.65,39.8684210526316,-4.58993464005751));
#26905=CARTESIAN_POINT('Ctrl Pts',(-1.42013071988495,40.0657894736842,-5.29999999999999));
#26906=CARTESIAN_POINT('Ctrl Pts',(-6.49062803547683E-16,40.2631578947368,
-5.29999999999999));
#26907=CARTESIAN_POINT('Ctrl Pts',(1.42013071988495,40.4605263157895,-5.29999999999999));
#26908=CARTESIAN_POINT('Ctrl Pts',(2.64999999999999,40.6578947368421,-4.58993464005752));
#26909=CARTESIAN_POINT('Ctrl Pts',(3.87986928011504,40.8552631578947,-3.87986928011505));
#26910=CARTESIAN_POINT('Ctrl Pts',(4.58993464005751,41.0526315789473,-2.65));
#26911=CARTESIAN_POINT('Ctrl Pts',(5.29999999999999,41.25,-1.42013071988495));
#26912=CARTESIAN_POINT('Ctrl Pts',(5.29999999999999,41.4473684210526,-9.73594205322072E-16));
#26913=CARTESIAN_POINT('Ctrl Pts',(5.29999999999999,41.6447368421053,1.42013071988495));
#26914=CARTESIAN_POINT('Ctrl Pts',(4.58993464005752,41.8421052631579,2.64999999999999));
#26915=CARTESIAN_POINT('Ctrl Pts',(3.87986928011505,42.0394736842106,3.87986928011504));
#26916=CARTESIAN_POINT('Ctrl Pts',(2.65,42.2368421052632,4.58993464005751));
#26917=CARTESIAN_POINT('Ctrl Pts',(1.42013071988495,42.4342105263158,5.29999999999999));
#26918=CARTESIAN_POINT('Ctrl Pts',(4.99201041585172E-28,42.6315789473684,
5.29999999999999));
#26919=CARTESIAN_POINT('Ctrl Pts',(-1.42013071988495,42.8289473684211,5.29999999999998));
#26920=CARTESIAN_POINT('Ctrl Pts',(-2.65,43.0263157894737,4.58993464005752));
#26921=CARTESIAN_POINT('Ctrl Pts',(-3.87986928011504,43.2236842105263,3.87986928011504));
#26922=CARTESIAN_POINT('Ctrl Pts',(-4.58993464005751,43.421052631579,2.65));
#26923=CARTESIAN_POINT('Ctrl Pts',(-5.29999999999999,43.6184210526316,1.42013071988495));
#26924=CARTESIAN_POINT('Ctrl Pts',(-5.29999999999999,43.8157894736842,3.24531401774024E-16));
#26925=CARTESIAN_POINT('Ctrl Pts',(-5.29999999999999,44.0131578947368,-1.42013071988495));
#26926=CARTESIAN_POINT('Ctrl Pts',(-4.58993464005751,44.2105263157895,-2.64999999999999));
#26927=CARTESIAN_POINT('Ctrl Pts',(-3.87986928011504,44.4078947368421,-3.87986928011504));
#26928=CARTESIAN_POINT('Ctrl Pts',(-2.65,44.6052631578947,-4.58993464005751));
#26929=CARTESIAN_POINT('Ctrl Pts',(-1.42013071988495,44.8026315789473,-5.29999999999999));
#26930=CARTESIAN_POINT('Ctrl Pts',(-6.49062803547635E-16,45.,-5.29999999999999));
#26931=CARTESIAN_POINT('Ctrl Pts',(1.42013071988495,45.1973684210526,-5.29999999999999));
#26932=CARTESIAN_POINT('Ctrl Pts',(2.64999999999999,45.3947368421053,-4.58993464005752));
#26933=CARTESIAN_POINT('Ctrl Pts',(3.87986928011504,45.5921052631579,-3.87986928011505));
#26934=CARTESIAN_POINT('Ctrl Pts',(4.58993464005751,45.7894736842105,-2.65));
#26935=CARTESIAN_POINT('Ctrl Pts',(5.29999999999999,45.9868421052631,-1.42013071988495));
#26936=CARTESIAN_POINT('Ctrl Pts',(5.29999999999999,46.1842105263158,-9.73594205321085E-16));
#26937=CARTESIAN_POINT('Ctrl Pts',(5.29999999999999,46.3815789473684,1.42013071988495));
#26938=CARTESIAN_POINT('Ctrl Pts',(4.58993464005752,46.5789473684211,2.64999999999999));
#26939=CARTESIAN_POINT('Ctrl Pts',(3.87986928011505,46.7763157894737,3.87986928011504));
#26940=CARTESIAN_POINT('Ctrl Pts',(2.65,46.9736842105263,4.58993464005752));
#26941=CARTESIAN_POINT('Ctrl Pts',(1.42013071988495,47.1710526315789,5.29999999999999));
#26942=CARTESIAN_POINT('Ctrl Pts',(5.54667823983524E-28,47.3684210526316,
5.29999999999999));
#26943=CARTESIAN_POINT('Ctrl Pts',(-1.42013071988495,47.5657894736842,5.29999999999998));
#26944=CARTESIAN_POINT('Ctrl Pts',(-2.65,47.7631578947368,4.58993464005752));
#26945=CARTESIAN_POINT('Ctrl Pts',(-3.87986928011504,47.9605263157895,3.87986928011504));
#26946=CARTESIAN_POINT('Ctrl Pts',(-4.58993464005751,48.1578947368421,2.65));
#26947=CARTESIAN_POINT('Ctrl Pts',(-5.29999999999999,48.3552631578947,1.42013071988495));
#26948=CARTESIAN_POINT('Ctrl Pts',(-5.29999999999999,48.5526315789474,3.24531401773827E-16));
#26949=CARTESIAN_POINT('Ctrl Pts',(-5.29999999999999,48.75,-1.42013071988495));
#26950=CARTESIAN_POINT('Ctrl Pts',(-4.58993464005751,48.9473684210526,-2.64999999999999));
#26951=CARTESIAN_POINT('Ctrl Pts',(-3.87986928011504,49.1447368421053,-3.87986928011504));
#26952=CARTESIAN_POINT('Ctrl Pts',(-2.65,49.3421052631579,-4.58993464005751));
#26953=CARTESIAN_POINT('Ctrl Pts',(-1.42013071988495,49.5394736842105,-5.29999999999999));
#26954=CARTESIAN_POINT('Ctrl Pts',(-6.49062803547579E-16,49.7368421052631,
-5.29999999999999));
#26955=CARTESIAN_POINT('Ctrl Pts',(1.42013071988495,49.9342105263158,-5.29999999999999));
#26956=CARTESIAN_POINT('Ctrl Pts',(2.64999999999999,50.1315789473684,-4.58993464005752));
#26957=CARTESIAN_POINT('Ctrl Pts',(3.87986928011504,50.328947368421,-3.87986928011505));
#26958=CARTESIAN_POINT('Ctrl Pts',(4.58993464005751,50.5263157894737,-2.65));
#26959=CARTESIAN_POINT('Ctrl Pts',(5.29999999999999,50.7236842105263,-1.42013071988495));
#26960=CARTESIAN_POINT('Ctrl Pts',(5.29999999999999,50.9210526315789,-9.73594205321085E-16));
#26961=CARTESIAN_POINT('Ctrl Pts',(5.29999999999999,51.1184210526316,1.42013071988495));
#26962=CARTESIAN_POINT('Ctrl Pts',(4.58993464005752,51.3157894736842,2.64999999999999));
#26963=CARTESIAN_POINT('Ctrl Pts',(3.87986928011505,51.5131578947368,3.87986928011504));
#26964=CARTESIAN_POINT('Ctrl Pts',(2.65,51.7105263157895,4.58993464005752));
#26965=CARTESIAN_POINT('Ctrl Pts',(1.42013071988495,51.9078947368421,5.29999999999998));
#26966=CARTESIAN_POINT('Ctrl Pts',(6.00890142648818E-28,52.1052631578948,
5.29999999999999));
#26967=CARTESIAN_POINT('Ctrl Pts',(-1.42013071988495,52.3026315789474,5.29999999999999));
#26968=CARTESIAN_POINT('Ctrl Pts',(-2.65,52.5,4.58993464005752));
#26969=CARTESIAN_POINT('Ctrl Pts',(-3.87986928011504,52.6973684210526,3.87986928011504));
#26970=CARTESIAN_POINT('Ctrl Pts',(-4.58993464005751,52.8947368421053,2.65));
#26971=CARTESIAN_POINT('Ctrl Pts',(-5.29999999999999,53.0921052631579,1.42013071988495));
#26972=CARTESIAN_POINT('Ctrl Pts',(-5.29999999999999,53.2894736842105,3.245314017757E-16));
#26973=CARTESIAN_POINT('Ctrl Pts',(-5.29999999999999,53.4868421052631,-1.42013071988495));
#26974=CARTESIAN_POINT('Ctrl Pts',(-4.58993464005751,53.6842105263158,-2.64999999999999));
#26975=CARTESIAN_POINT('Ctrl Pts',(-3.87986928011504,53.8815789473684,-3.87986928011504));
#26976=CARTESIAN_POINT('Ctrl Pts',(-2.65,54.0789473684211,-4.58993464005751));
#26977=CARTESIAN_POINT('Ctrl Pts',(-1.42013071988495,54.2763157894737,-5.29999999999999));
#26978=CARTESIAN_POINT('Ctrl Pts',(-6.4906280354753E-16,54.4736842105263,
-5.29999999999999));
#26979=CARTESIAN_POINT('Ctrl Pts',(1.42013071988495,54.6710526315789,-5.29999999999999));
#26980=CARTESIAN_POINT('Ctrl Pts',(2.64999999999999,54.8684210526316,-4.58993464005752));
#26981=CARTESIAN_POINT('Ctrl Pts',(3.87986928011504,55.0657894736842,-3.87986928011505));
#26982=CARTESIAN_POINT('Ctrl Pts',(4.58993464005751,55.2631578947368,-2.65));
#26983=CARTESIAN_POINT('Ctrl Pts',(5.29999999999999,55.4605263157895,-1.42013071988495));
#26984=CARTESIAN_POINT('Ctrl Pts',(5.29999999999999,55.6578947368421,-9.73594205321578E-16));
#26985=CARTESIAN_POINT('Ctrl Pts',(5.29999999999999,55.8552631578947,1.42013071988495));
#26986=CARTESIAN_POINT('Ctrl Pts',(4.58993464005752,56.0526315789474,2.64999999999999));
#26987=CARTESIAN_POINT('Ctrl Pts',(3.87986928011505,56.25,3.87986928011504));
#26988=CARTESIAN_POINT('Ctrl Pts',(2.65,56.4473684210526,4.58993464005752));
#26989=CARTESIAN_POINT('Ctrl Pts',(1.42013071988495,56.6447368421052,5.29999999999999));
#26990=CARTESIAN_POINT('Ctrl Pts',(6.5635692504717E-28,56.8421052631579,
5.29999999999999));
#26991=CARTESIAN_POINT('Ctrl Pts',(-1.42013071988495,57.0394736842105,5.29999999999998));
#26992=CARTESIAN_POINT('Ctrl Pts',(-2.65,57.2368421052632,4.58993464005752));
#26993=CARTESIAN_POINT('Ctrl Pts',(-3.87986928011504,57.4342105263158,3.87986928011504));
#26994=CARTESIAN_POINT('Ctrl Pts',(-4.58993464005751,57.6315789473684,2.65));
#26995=CARTESIAN_POINT('Ctrl Pts',(-5.29999999999999,57.8289473684211,1.42013071988495));
#26996=CARTESIAN_POINT('Ctrl Pts',(-5.29999999999999,58.0263157894737,3.24531401775207E-16));
#26997=CARTESIAN_POINT('Ctrl Pts',(-5.29999999999999,58.2236842105263,-1.42013071988495));
#26998=CARTESIAN_POINT('Ctrl Pts',(-4.58993464005751,58.4210526315789,-2.64999999999999));
#26999=CARTESIAN_POINT('Ctrl Pts',(-3.87986928011504,58.6184210526315,-3.87986928011504));
#27000=CARTESIAN_POINT('Ctrl Pts',(-2.65,58.8157894736842,-4.58993464005751));
#27001=CARTESIAN_POINT('Ctrl Pts',(-1.42013071988495,59.0131578947368,-5.29999999999999));
#27002=CARTESIAN_POINT('Ctrl Pts',(-6.49062803547473E-16,59.2105263157894,
-5.29999999999999));
#27003=CARTESIAN_POINT('Ctrl Pts',(1.42013071988495,59.4078947368421,-5.29999999999999));
#27004=CARTESIAN_POINT('Ctrl Pts',(2.64999999999999,59.6052631578947,-4.58993464005752));
#27005=CARTESIAN_POINT('Ctrl Pts',(3.87986928011504,59.8026315789473,-3.87986928011505));
#27006=CARTESIAN_POINT('Ctrl Pts',(4.58993464005751,60.,-2.65));
#27007=CARTESIAN_POINT('Ctrl Pts',(5.29999999999999,60.1973684210526,-1.42013071988495));
#27008=CARTESIAN_POINT('Ctrl Pts',(5.29999999999999,60.3947368421052,-9.73594205321184E-16));
#27009=CARTESIAN_POINT('Ctrl Pts',(5.29999999999999,60.5921052631579,1.42013071988495));
#27010=CARTESIAN_POINT('Ctrl Pts',(4.58993464005752,60.7894736842105,2.64999999999999));
#27011=CARTESIAN_POINT('Ctrl Pts',(3.87986928011505,60.9868421052632,3.87986928011504));
#27012=CARTESIAN_POINT('Ctrl Pts',(2.65,61.1842105263158,4.58993464005752));
#27013=CARTESIAN_POINT('Ctrl Pts',(1.42013071988495,61.3815789473684,5.29999999999998));
#27014=CARTESIAN_POINT('Ctrl Pts',(7.02579243712464E-28,61.5789473684211,
5.29999999999999));
#27015=CARTESIAN_POINT('Ctrl Pts',(-1.42013071988495,61.7763157894737,5.29999999999999));
#27016=CARTESIAN_POINT('Ctrl Pts',(-2.65,61.9736842105264,4.58993464005752));
#27017=CARTESIAN_POINT('Ctrl Pts',(-3.87986928011504,62.171052631579,3.87986928011505));
#27018=CARTESIAN_POINT('Ctrl Pts',(-4.58993464005751,62.3684210526316,2.65));
#27019=CARTESIAN_POINT('Ctrl Pts',(-5.29999999999999,62.5657894736842,1.42013071988495));
#27020=CARTESIAN_POINT('Ctrl Pts',(-5.29999999999999,62.7631578947368,3.24531401775109E-16));
#27021=CARTESIAN_POINT('Ctrl Pts',(-5.29999999999999,62.9605263157895,-1.42013071988495));
#27022=CARTESIAN_POINT('Ctrl Pts',(-4.58993464005751,63.1578947368421,-2.64999999999999));
#27023=CARTESIAN_POINT('Ctrl Pts',(-3.87986928011504,63.3552631578947,-3.87986928011504));
#27024=CARTESIAN_POINT('Ctrl Pts',(-2.65,63.5526315789474,-4.58993464005751));
#27025=CARTESIAN_POINT('Ctrl Pts',(-1.42013071988495,63.75,-5.29999999999999));
#27026=CARTESIAN_POINT('Ctrl Pts',(-6.49062803547422E-16,63.9473684210526,
-5.29999999999999));
#27027=CARTESIAN_POINT('Ctrl Pts',(1.42013071988495,64.1447368421053,-5.29999999999999));
#27028=CARTESIAN_POINT('Ctrl Pts',(2.64999999999999,64.3421052631579,-4.58993464005752));
#27029=CARTESIAN_POINT('Ctrl Pts',(3.87986928011504,64.5394736842105,-3.87986928011505));
#27030=CARTESIAN_POINT('Ctrl Pts',(4.58993464005751,64.7368421052632,-2.65));
#27031=CARTESIAN_POINT('Ctrl Pts',(5.29999999999999,64.9342105263157,-1.42013071988495));
#27032=CARTESIAN_POINT('Ctrl Pts',(5.29999999999999,65.1315789473684,-9.73594205320987E-16));
#27033=CARTESIAN_POINT('Ctrl Pts',(5.29999999999999,65.328947368421,1.42013071988495));
#27034=CARTESIAN_POINT('Ctrl Pts',(4.58993464005752,65.5263157894737,2.64999999999999));
#27035=CARTESIAN_POINT('Ctrl Pts',(3.87986928011505,65.7236842105264,3.87986928011504));
#27036=CARTESIAN_POINT('Ctrl Pts',(2.65,65.9210526315789,4.58993464005752));
#27037=CARTESIAN_POINT('Ctrl Pts',(1.42013071988495,66.1184210526315,5.29999999999999));
#27038=CARTESIAN_POINT('Ctrl Pts',(7.48801562377757E-28,66.3157894736842,
5.29999999999999));
#27039=CARTESIAN_POINT('Ctrl Pts',(-1.42013071988495,66.5131578947368,5.29999999999998));
#27040=CARTESIAN_POINT('Ctrl Pts',(-2.65,66.7105263157894,4.58993464005752));
#27041=CARTESIAN_POINT('Ctrl Pts',(-3.87986928011504,66.9078947368421,3.87986928011504));
#27042=CARTESIAN_POINT('Ctrl Pts',(-4.58993464005751,67.1052631578947,2.65));
#27043=CARTESIAN_POINT('Ctrl Pts',(-5.29999999999999,67.3026315789474,1.42013071988495));
#27044=CARTESIAN_POINT('Ctrl Pts',(-5.29999999999999,67.5,3.24531401774714E-16));
#27045=CARTESIAN_POINT('Ctrl Pts',(-5.29999999999999,67.6973684210526,-1.42013071988495));
#27046=CARTESIAN_POINT('Ctrl Pts',(-4.58993464005751,67.8947368421052,-2.64999999999999));
#27047=CARTESIAN_POINT('Ctrl Pts',(-3.87986928011504,68.0921052631578,-3.87986928011504));
#27048=CARTESIAN_POINT('Ctrl Pts',(-2.65,68.2894736842105,-4.58993464005751));
#27049=CARTESIAN_POINT('Ctrl Pts',(-1.42013071988495,68.4868421052632,-5.29999999999999));
#27050=CARTESIAN_POINT('Ctrl Pts',(-6.49062803547376E-16,68.6842105263158,
-5.29999999999999));
#27051=CARTESIAN_POINT('Ctrl Pts',(1.42013071988495,68.8815789473684,-5.29999999999999));
#27052=CARTESIAN_POINT('Ctrl Pts',(2.64999999999999,69.078947368421,-4.58993464005752));
#27053=CARTESIAN_POINT('Ctrl Pts',(3.87986928011504,69.2763157894736,-3.87986928011505));
#27054=CARTESIAN_POINT('Ctrl Pts',(4.58993464005751,69.4736842105263,-2.65));
#27055=CARTESIAN_POINT('Ctrl Pts',(5.29999999999999,69.6710526315789,-1.42013071988495));
#27056=CARTESIAN_POINT('Ctrl Pts',(5.29999999999999,69.8684210526316,-9.73594205320888E-16));
#27057=CARTESIAN_POINT('Ctrl Pts',(5.29999999999999,70.0657894736842,1.42013071988495));
#27058=CARTESIAN_POINT('Ctrl Pts',(4.58993464005752,70.2631578947369,2.64999999999999));
#27059=CARTESIAN_POINT('Ctrl Pts',(3.87986928011505,70.4605263157895,3.87986928011504));
#27060=CARTESIAN_POINT('Ctrl Pts',(2.65,70.6578947368421,4.58993464005752));
#27061=CARTESIAN_POINT('Ctrl Pts',(1.42013071988495,70.8552631578947,5.29999999999998));
#27062=CARTESIAN_POINT('Ctrl Pts',(7.96564624998561E-28,71.0526315789473,
5.29999999999999));
#27063=CARTESIAN_POINT('Ctrl Pts',(-1.42013071988495,71.2499999999999,5.29999999999999));
#27064=CARTESIAN_POINT('Ctrl Pts',(-2.65,71.4473684210526,4.58993464005751));
#27065=CARTESIAN_POINT('Ctrl Pts',(-3.87986928011504,71.6447368421053,3.87986928011504));
#27066=CARTESIAN_POINT('Ctrl Pts',(-4.58993464005751,71.8421052631579,2.65));
#27067=CARTESIAN_POINT('Ctrl Pts',(-5.29999999999999,72.0394736842105,1.42013071988495));
#27068=CARTESIAN_POINT('Ctrl Pts',(-5.29999999999999,72.2368421052632,3.24531401775306E-16));
#27069=CARTESIAN_POINT('Ctrl Pts',(-5.29999999999999,72.4342105263157,-1.42013071988495));
#27070=CARTESIAN_POINT('Ctrl Pts',(-4.58993464005751,72.6315789473684,-2.64999999999999));
#27071=CARTESIAN_POINT('Ctrl Pts',(-3.87986928011504,72.828947368421,-3.87986928011504));
#27072=CARTESIAN_POINT('Ctrl Pts',(-2.65,73.0263157894737,-4.58993464005751));
#27073=CARTESIAN_POINT('Ctrl Pts',(-1.42013071988495,73.2236842105263,-5.29999999999999));
#27074=CARTESIAN_POINT('Ctrl Pts',(-6.4906280354732E-16,73.421052631579,
-5.29999999999999));
#27075=CARTESIAN_POINT('Ctrl Pts',(1.42013071988495,73.6184210526315,-5.29999999999999));
#27076=CARTESIAN_POINT('Ctrl Pts',(2.64999999999999,73.8157894736842,-4.58993464005751));
#27077=CARTESIAN_POINT('Ctrl Pts',(3.87986928011504,74.0131578947368,-3.87986928011505));
#27078=CARTESIAN_POINT('Ctrl Pts',(4.58993464005751,74.2105263157895,-2.65));
#27079=CARTESIAN_POINT('Ctrl Pts',(5.29999999999999,74.4078947368421,-1.42013071988495));
#27080=CARTESIAN_POINT('Ctrl Pts',(5.29999999999999,74.6052631578947,-9.73594205321085E-16));
#27081=CARTESIAN_POINT('Ctrl Pts',(5.29999999999999,74.8026315789473,1.42013071988495));
#27082=CARTESIAN_POINT('Ctrl Pts',(4.58993464005752,75.,2.64999999999999));
#27083=CARTESIAN_POINT('Ctrl Pts',(3.87986928011505,75.1973684210526,3.87986928011504));
#27084=CARTESIAN_POINT('Ctrl Pts',(2.65,75.3947368421052,4.58993464005751));
#27085=CARTESIAN_POINT('Ctrl Pts',(1.42013071988495,75.5921052631578,5.29999999999998));
#27086=CARTESIAN_POINT('Ctrl Pts',(8.68979590907521E-28,75.7894736842105,
5.29999999999999));
#27087=CARTESIAN_POINT('Ctrl Pts',(-1.42013071988495,75.9868421052631,5.29999999999999));
#27088=CARTESIAN_POINT('Ctrl Pts',(-2.65,76.1842105263158,4.58993464005751));
#27089=CARTESIAN_POINT('Ctrl Pts',(-3.87986928011504,76.3815789473684,3.87986928011504));
#27090=CARTESIAN_POINT('Ctrl Pts',(-4.58993464005751,76.5789473684211,2.65));
#27091=CARTESIAN_POINT('Ctrl Pts',(-5.29999999999999,76.7763157894737,1.42013071988495));
#27092=CARTESIAN_POINT('Ctrl Pts',(-5.29999999999999,76.9736842105263,3.24531401774615E-16));
#27093=CARTESIAN_POINT('Ctrl Pts',(-5.29999999999999,77.1710526315789,-1.42013071988495));
#27094=CARTESIAN_POINT('Ctrl Pts',(-4.58993464005751,77.3684210526315,-2.64999999999999));
#27095=CARTESIAN_POINT('Ctrl Pts',(-3.87986928011504,77.5657894736842,-3.87986928011504));
#27096=CARTESIAN_POINT('Ctrl Pts',(-2.65,77.7631578947368,-4.58993464005751));
#27097=CARTESIAN_POINT('Ctrl Pts',(-1.42013071988495,77.9605263157895,-5.29999999999999));
#27098=CARTESIAN_POINT('Ctrl Pts',(-6.49062803547265E-16,78.1578947368421,
-5.29999999999999));
#27099=CARTESIAN_POINT('Ctrl Pts',(1.42013071988495,78.3552631578948,-5.29999999999999));
#27100=CARTESIAN_POINT('Ctrl Pts',(2.64999999999999,78.5526315789474,-4.58993464005751));
#27101=CARTESIAN_POINT('Ctrl Pts',(3.87986928011504,78.7499999999999,-3.87986928011505));
#27102=CARTESIAN_POINT('Ctrl Pts',(4.58993464005751,78.9473684210526,-2.65));
#27103=CARTESIAN_POINT('Ctrl Pts',(5.29999999999999,79.1447368421052,-1.42013071988495));
#27104=CARTESIAN_POINT('Ctrl Pts',(5.29999999999999,79.3421052631579,-9.73594205320987E-16));
#27105=CARTESIAN_POINT('Ctrl Pts',(5.29999999999999,79.5394736842105,1.42013071988495));
#27106=CARTESIAN_POINT('Ctrl Pts',(4.58993464005752,79.7368421052632,2.64999999999999));
#27107=CARTESIAN_POINT('Ctrl Pts',(3.87986928011505,79.9342105263158,3.87986928011504));
#27108=CARTESIAN_POINT('Ctrl Pts',(2.65,80.1315789473684,4.58993464005751));
#27109=CARTESIAN_POINT('Ctrl Pts',(1.42013071988495,80.328947368421,5.29999999999999));
#27110=CARTESIAN_POINT('Ctrl Pts',(9.15201909572814E-28,80.5263157894736,
5.3));
#27111=CARTESIAN_POINT('Ctrl Pts',(-1.42013071988495,80.7236842105263,5.29999999999998));
#27112=CARTESIAN_POINT('Ctrl Pts',(-2.65,80.9210526315789,4.58993464005751));
#27113=CARTESIAN_POINT('Ctrl Pts',(-3.87986928011504,81.1184210526315,3.87986928011504));
#27114=CARTESIAN_POINT('Ctrl Pts',(-4.58993464005751,81.3157894736842,2.64999999999999));
#27115=CARTESIAN_POINT('Ctrl Pts',(-5.29999999999999,81.5131578947368,1.42013071988495));
#27116=CARTESIAN_POINT('Ctrl Pts',(-5.29999999999999,81.7105263157895,3.24531401775207E-16));
#27117=CARTESIAN_POINT('Ctrl Pts',(-5.29999999999999,81.9078947368421,-1.42013071988495));
#27118=CARTESIAN_POINT('Ctrl Pts',(-4.58993464005751,82.1052631578947,-2.64999999999999));
#27119=CARTESIAN_POINT('Ctrl Pts',(-3.87986928011504,82.3026315789473,-3.87986928011504));
#27120=CARTESIAN_POINT('Ctrl Pts',(-2.65,82.5,-4.58993464005751));
#27121=CARTESIAN_POINT('Ctrl Pts',(-1.42013071988495,82.6973684210527,-5.29999999999999));
#27122=CARTESIAN_POINT('Ctrl Pts',(-6.49062803547219E-16,82.8947368421053,
-5.29999999999999));
#27123=CARTESIAN_POINT('Ctrl Pts',(1.42013071988495,83.0921052631579,-5.29999999999999));
#27124=CARTESIAN_POINT('Ctrl Pts',(2.64999999999999,83.2894736842105,-4.58993464005751));
#27125=CARTESIAN_POINT('Ctrl Pts',(3.87986928011504,83.4868421052631,-3.87986928011505));
#27126=CARTESIAN_POINT('Ctrl Pts',(4.58993464005751,83.6842105263158,-2.65));
#27127=CARTESIAN_POINT('Ctrl Pts',(5.29999999999999,83.8815789473684,-1.42013071988495));
#27128=CARTESIAN_POINT('Ctrl Pts',(5.29999999999999,84.078947368421,-9.73594205321184E-16));
#27129=CARTESIAN_POINT('Ctrl Pts',(5.29999999999999,84.2763157894736,1.42013071988495));
#27130=CARTESIAN_POINT('Ctrl Pts',(4.58993464005752,84.4736842105263,2.64999999999999));
#27131=CARTESIAN_POINT('Ctrl Pts',(3.87986928011505,84.6710526315789,3.87986928011504));
#27132=CARTESIAN_POINT('Ctrl Pts',(2.65,84.8684210526316,4.58993464005751));
#27133=CARTESIAN_POINT('Ctrl Pts',(1.42013071988495,85.0657894736842,5.29999999999998));
#27134=CARTESIAN_POINT('Ctrl Pts',(9.61424228238108E-28,85.2631578947368,
5.3));
#27135=CARTESIAN_POINT('Ctrl Pts',(-1.42013071988495,85.4605263157894,5.29999999999999));
#27136=CARTESIAN_POINT('Ctrl Pts',(-2.65,85.6578947368421,4.58993464005751));
#27137=CARTESIAN_POINT('Ctrl Pts',(-3.87986928011504,85.8552631578947,3.87986928011504));
#27138=CARTESIAN_POINT('Ctrl Pts',(-4.58993464005751,86.0526315789474,2.65));
#27139=CARTESIAN_POINT('Ctrl Pts',(-5.29999999999999,86.25,1.42013071988495));
#27140=CARTESIAN_POINT('Ctrl Pts',(-5.29999999999999,86.4473684210526,3.24531401775207E-16));
#27141=CARTESIAN_POINT('Ctrl Pts',(-5.29999999999999,86.6447368421052,-1.42013071988495));
#27142=CARTESIAN_POINT('Ctrl Pts',(-4.58993464005751,86.8421052631579,-2.64999999999999));
#27143=CARTESIAN_POINT('Ctrl Pts',(-3.87986928011504,87.0394736842105,-3.87986928011504));
#27144=CARTESIAN_POINT('Ctrl Pts',(-2.65,87.2368421052631,-4.58993464005751));
#27145=CARTESIAN_POINT('Ctrl Pts',(-1.42013071988495,87.4342105263158,-5.29999999999999));
#27146=CARTESIAN_POINT('Ctrl Pts',(-6.49062803547173E-16,87.6315789473684,
-5.29999999999999));
#27147=CARTESIAN_POINT('Ctrl Pts',(1.42013071988495,87.828947368421,-5.29999999999999));
#27148=CARTESIAN_POINT('Ctrl Pts',(2.64999999999999,88.0263157894737,-4.58993464005751));
#27149=CARTESIAN_POINT('Ctrl Pts',(3.87986928011504,88.2236842105263,-3.87986928011505));
#27150=CARTESIAN_POINT('Ctrl Pts',(4.58993464005751,88.4210526315789,-2.65));
#27151=CARTESIAN_POINT('Ctrl Pts',(5.29999999999999,88.6184210526316,-1.42013071988495));
#27152=CARTESIAN_POINT('Ctrl Pts',(5.29999999999999,88.8157894736842,-9.73594205321085E-16));
#27153=CARTESIAN_POINT('Ctrl Pts',(5.29999999999999,89.0131578947368,1.42013071988495));
#27154=CARTESIAN_POINT('Ctrl Pts',(4.58993464005752,89.2105263157895,2.64999999999999));
#27155=CARTESIAN_POINT('Ctrl Pts',(3.87986928011505,89.4078947368421,3.87986928011504));
#27156=CARTESIAN_POINT('Ctrl Pts',(2.65,89.6052631578947,4.58993464005751));
#27157=CARTESIAN_POINT('Ctrl Pts',(1.42013071988495,89.8026315789473,5.29999999999999));
#27158=CARTESIAN_POINT('Ctrl Pts',(1.01689101063646E-27,89.9999999999999,
5.3));
#27159=CARTESIAN_POINT('Ctrl Pts',(2.77333911991762E-29,0.,5.29999999999999));
#27160=CARTESIAN_POINT('Ctrl Pts',(-1.42013071988495,0.197368421052638,
5.29999999999998));
#27161=CARTESIAN_POINT('Ctrl Pts',(-2.65,0.394736842105281,4.58993464005751));
#27162=CARTESIAN_POINT('Ctrl Pts',(-3.87986928011504,0.592105263157915,
3.87986928011505));
#27163=CARTESIAN_POINT('Ctrl Pts',(-4.58993464005751,0.789473684210562,
2.65));
#27164=CARTESIAN_POINT('Ctrl Pts',(-5.29999999999999,0.986842105263191,
1.42013071988495));
#27165=CARTESIAN_POINT('Ctrl Pts',(-5.29999999999999,1.18421052631579,3.24531401774024E-16));
#27166=CARTESIAN_POINT('Ctrl Pts',(-5.29999999999999,1.38157894736841,-1.42013071988495));
#27167=CARTESIAN_POINT('Ctrl Pts',(-4.58993464005751,1.57894736842107,-2.64999999999999));
#27168=CARTESIAN_POINT('Ctrl Pts',(-3.87986928011504,1.77631578947369,-3.87986928011504));
#27169=CARTESIAN_POINT('Ctrl Pts',(-2.65,1.97368421052629,-4.58993464005751));
#27170=CARTESIAN_POINT('Ctrl Pts',(-1.42013071988495,2.17105263157891,-5.29999999999999));
#27171=CARTESIAN_POINT('Ctrl Pts',(-6.49062803548097E-16,2.36842105263158,
-5.29999999999999));
#27172=CARTESIAN_POINT('Ctrl Pts',(1.42013071988495,2.56578947368418,-5.29999999999999));
#27173=CARTESIAN_POINT('Ctrl Pts',(2.64999999999999,2.7631578947368,-4.58993464005751));
#27174=CARTESIAN_POINT('Ctrl Pts',(3.87986928011504,2.96052631578946,-3.87986928011505));
#27175=CARTESIAN_POINT('Ctrl Pts',(4.58993464005751,3.15789473684208,-2.65));
#27176=CARTESIAN_POINT('Ctrl Pts',(5.29999999999999,3.35526315789473,-1.42013071988495));
#27177=CARTESIAN_POINT('Ctrl Pts',(5.29999999999999,3.55263157894736,-9.73594205321085E-16));
#27178=CARTESIAN_POINT('Ctrl Pts',(5.29999999999999,3.75000000000001,1.42013071988494));
#27179=CARTESIAN_POINT('Ctrl Pts',(4.58993464005752,3.94736842105264,2.64999999999999));
#27180=CARTESIAN_POINT('Ctrl Pts',(3.87986928011505,4.14473684210529,3.87986928011504));
#27181=CARTESIAN_POINT('Ctrl Pts',(2.65,4.34210526315792,4.58993464005751));
#27182=CARTESIAN_POINT('Ctrl Pts',(1.42013071988495,4.53947368421056,5.29999999999998));
#27183=CARTESIAN_POINT('Ctrl Pts',(8.32001735975286E-29,4.73684210526315,
5.29999999999999));
#27184=CARTESIAN_POINT('Ctrl Pts',(-1.42013071988495,4.93421052631578,5.29999999999999));
#27185=CARTESIAN_POINT('Ctrl Pts',(-2.65,5.13157894736843,4.58993464005751));
#27186=CARTESIAN_POINT('Ctrl Pts',(-3.87986928011504,5.32894736842106,3.87986928011505));
#27187=CARTESIAN_POINT('Ctrl Pts',(-4.58993464005751,5.52631578947371,2.65));
#27188=CARTESIAN_POINT('Ctrl Pts',(-5.29999999999999,5.72368421052634,1.42013071988495));
#27189=CARTESIAN_POINT('Ctrl Pts',(-5.29999999999999,5.92105263157894,3.24531401774024E-16));
#27190=CARTESIAN_POINT('Ctrl Pts',(-5.29999999999999,6.11842105263156,-1.42013071988495));
#27191=CARTESIAN_POINT('Ctrl Pts',(-4.58993464005751,6.31578947368422,-2.64999999999999));
#27192=CARTESIAN_POINT('Ctrl Pts',(-3.87986928011504,6.51315789473683,-3.87986928011504));
#27193=CARTESIAN_POINT('Ctrl Pts',(-2.65,6.71052631578944,-4.58993464005751));
#27194=CARTESIAN_POINT('Ctrl Pts',(-1.42013071988495,6.90789473684211,-5.29999999999999));
#27195=CARTESIAN_POINT('Ctrl Pts',(-6.49062803548043E-16,7.10526315789473,
-5.29999999999999));
#27196=CARTESIAN_POINT('Ctrl Pts',(1.42013071988495,7.30263157894733,-5.29999999999999));
#27197=CARTESIAN_POINT('Ctrl Pts',(2.64999999999999,7.50000000000001,-4.58993464005751));
#27198=CARTESIAN_POINT('Ctrl Pts',(3.87986928011504,7.69736842105261,-3.87986928011505));
#27199=CARTESIAN_POINT('Ctrl Pts',(4.58993464005751,7.89473684210523,-2.65));
#27200=CARTESIAN_POINT('Ctrl Pts',(5.29999999999999,8.09210526315788,-1.42013071988495));
#27201=CARTESIAN_POINT('Ctrl Pts',(5.29999999999999,8.28947368421051,-9.73594205321085E-16));
#27202=CARTESIAN_POINT('Ctrl Pts',(5.29999999999999,8.48684210526316,1.42013071988495));
#27203=CARTESIAN_POINT('Ctrl Pts',(4.58993464005752,8.68421052631579,2.64999999999999));
#27204=CARTESIAN_POINT('Ctrl Pts',(3.87986928011505,8.88157894736843,3.87986928011504));
#27205=CARTESIAN_POINT('Ctrl Pts',(2.65,9.07894736842108,4.58993464005751));
#27206=CARTESIAN_POINT('Ctrl Pts',(1.42013071988495,9.27631578947371,5.29999999999999));
#27207=CARTESIAN_POINT('Ctrl Pts',(1.35585468084861E-28,9.47368421052636,
5.3));
#27208=CARTESIAN_POINT('Ctrl Pts',(-1.42013071988495,9.67105263157899,5.29999999999998));
#27209=CARTESIAN_POINT('Ctrl Pts',(-2.65,9.86842105263158,4.58993464005751));
#27210=CARTESIAN_POINT('Ctrl Pts',(-3.87986928011504,10.0657894736842,3.87986928011504));
#27211=CARTESIAN_POINT('Ctrl Pts',(-4.58993464005751,10.2631578947369,2.65));
#27212=CARTESIAN_POINT('Ctrl Pts',(-5.29999999999999,10.4605263157895,1.42013071988495));
#27213=CARTESIAN_POINT('Ctrl Pts',(-5.29999999999999,10.6578947368421,3.24531401772841E-16));
#27214=CARTESIAN_POINT('Ctrl Pts',(-5.29999999999999,10.8552631578948,-1.42013071988495));
#27215=CARTESIAN_POINT('Ctrl Pts',(-4.58993464005751,11.0526315789474,-2.64999999999999));
#27216=CARTESIAN_POINT('Ctrl Pts',(-3.87986928011504,11.25,-3.87986928011504));
#27217=CARTESIAN_POINT('Ctrl Pts',(-2.65,11.4473684210526,-4.58993464005751));
#27218=CARTESIAN_POINT('Ctrl Pts',(-1.42013071988495,11.6447368421052,-5.29999999999999));
#27219=CARTESIAN_POINT('Ctrl Pts',(-6.49062803547995E-16,11.8421052631579,
-5.29999999999999));
#27220=CARTESIAN_POINT('Ctrl Pts',(1.42013071988495,12.0394736842105,-5.29999999999999));
#27221=CARTESIAN_POINT('Ctrl Pts',(2.64999999999999,12.2368421052632,-4.58993464005751));
#27222=CARTESIAN_POINT('Ctrl Pts',(3.87986928011504,12.4342105263158,-3.87986928011505));
#27223=CARTESIAN_POINT('Ctrl Pts',(4.58993464005751,12.6315789473684,-2.65));
#27224=CARTESIAN_POINT('Ctrl Pts',(5.29999999999999,12.828947368421,-1.42013071988495));
#27225=CARTESIAN_POINT('Ctrl Pts',(5.29999999999999,13.0263157894737,-9.73594205322072E-16));
#27226=CARTESIAN_POINT('Ctrl Pts',(5.29999999999999,13.2236842105263,1.42013071988495));
#27227=CARTESIAN_POINT('Ctrl Pts',(4.58993464005752,13.4210526315789,2.64999999999999));
#27228=CARTESIAN_POINT('Ctrl Pts',(3.87986928011505,13.6184210526316,3.87986928011504));
#27229=CARTESIAN_POINT('Ctrl Pts',(2.65,13.8157894736842,4.58993464005751));
#27230=CARTESIAN_POINT('Ctrl Pts',(1.42013071988495,14.0131578947369,5.29999999999998));
#27231=CARTESIAN_POINT('Ctrl Pts',(1.84889274661175E-28,14.2105263157895,
5.3));
#27232=CARTESIAN_POINT('Ctrl Pts',(-1.42013071988495,14.4078947368421,5.29999999999999));
#27233=CARTESIAN_POINT('Ctrl Pts',(-2.65,14.6052631578947,4.58993464005751));
#27234=CARTESIAN_POINT('Ctrl Pts',(-3.87986928011504,14.8026315789474,3.87986928011504));
#27235=CARTESIAN_POINT('Ctrl Pts',(-4.58993464005751,15.,2.65));
#27236=CARTESIAN_POINT('Ctrl Pts',(-5.29999999999999,15.1973684210526,1.42013071988495));
#27237=CARTESIAN_POINT('Ctrl Pts',(-5.29999999999999,15.3947368421052,3.24531401774024E-16));
#27238=CARTESIAN_POINT('Ctrl Pts',(-5.29999999999999,15.5921052631579,-1.42013071988495));
#27239=CARTESIAN_POINT('Ctrl Pts',(-4.58993464005751,15.7894736842105,-2.64999999999999));
#27240=CARTESIAN_POINT('Ctrl Pts',(-3.87986928011504,15.9868421052631,-3.87986928011504));
#27241=CARTESIAN_POINT('Ctrl Pts',(-2.65,16.1842105263157,-4.58993464005751));
#27242=CARTESIAN_POINT('Ctrl Pts',(-1.42013071988495,16.3815789473684,-5.29999999999999));
#27243=CARTESIAN_POINT('Ctrl Pts',(-6.49062803547949E-16,16.578947368421,
-5.29999999999999));
#27244=CARTESIAN_POINT('Ctrl Pts',(1.42013071988495,16.7763157894737,-5.29999999999999));
#27245=CARTESIAN_POINT('Ctrl Pts',(2.64999999999999,16.9736842105263,-4.58993464005751));
#27246=CARTESIAN_POINT('Ctrl Pts',(3.87986928011504,17.171052631579,-3.87986928011505));
#27247=CARTESIAN_POINT('Ctrl Pts',(4.58993464005751,17.3684210526316,-2.65));
#27248=CARTESIAN_POINT('Ctrl Pts',(5.29999999999999,17.5657894736842,-1.42013071988495));
#27249=CARTESIAN_POINT('Ctrl Pts',(5.29999999999999,17.7631578947368,-9.73594205322269E-16));
#27250=CARTESIAN_POINT('Ctrl Pts',(5.29999999999999,17.9605263157895,1.42013071988494));
#27251=CARTESIAN_POINT('Ctrl Pts',(4.58993464005752,18.1578947368421,2.64999999999999));
#27252=CARTESIAN_POINT('Ctrl Pts',(3.87986928011505,18.3552631578947,3.87986928011504));
#27253=CARTESIAN_POINT('Ctrl Pts',(2.65,18.5526315789474,4.58993464005751));
#27254=CARTESIAN_POINT('Ctrl Pts',(1.42013071988495,18.75,5.29999999999998));
#27255=CARTESIAN_POINT('Ctrl Pts',(2.31111593326468E-28,18.9473684210527,
5.3));
#27256=CARTESIAN_POINT('Ctrl Pts',(-1.42013071988495,19.1447368421053,5.29999999999999));
#27257=CARTESIAN_POINT('Ctrl Pts',(-2.65,19.3421052631579,4.58993464005751));
#27258=CARTESIAN_POINT('Ctrl Pts',(-3.87986928011504,19.5394736842105,3.87986928011504));
#27259=CARTESIAN_POINT('Ctrl Pts',(-4.58993464005751,19.7368421052632,2.65));
#27260=CARTESIAN_POINT('Ctrl Pts',(-5.29999999999999,19.9342105263158,1.42013071988495));
#27261=CARTESIAN_POINT('Ctrl Pts',(-5.29999999999999,20.1315789473684,3.24531401774221E-16));
#27262=CARTESIAN_POINT('Ctrl Pts',(-5.29999999999999,20.328947368421,-1.42013071988495));
#27263=CARTESIAN_POINT('Ctrl Pts',(-4.58993464005751,20.5263157894737,-2.64999999999999));
#27264=CARTESIAN_POINT('Ctrl Pts',(-3.87986928011504,20.7236842105263,-3.87986928011504));
#27265=CARTESIAN_POINT('Ctrl Pts',(-2.65,20.921052631579,-4.58993464005751));
#27266=CARTESIAN_POINT('Ctrl Pts',(-1.42013071988495,21.1184210526315,-5.29999999999999));
#27267=CARTESIAN_POINT('Ctrl Pts',(-6.49062803547894E-16,21.3157894736842,
-5.29999999999999));
#27268=CARTESIAN_POINT('Ctrl Pts',(1.42013071988495,21.5131578947368,-5.29999999999999));
#27269=CARTESIAN_POINT('Ctrl Pts',(2.64999999999999,21.7105263157895,-4.58993464005751));
#27270=CARTESIAN_POINT('Ctrl Pts',(3.87986928011504,21.9078947368421,-3.87986928011505));
#27271=CARTESIAN_POINT('Ctrl Pts',(4.58993464005751,22.1052631578947,-2.65));
#27272=CARTESIAN_POINT('Ctrl Pts',(5.29999999999999,22.3026315789474,-1.42013071988495));
#27273=CARTESIAN_POINT('Ctrl Pts',(5.29999999999999,22.5,-9.73594205320888E-16));
#27274=CARTESIAN_POINT('Ctrl Pts',(5.29999999999999,22.6973684210527,1.42013071988495));
#27275=CARTESIAN_POINT('Ctrl Pts',(4.58993464005752,22.8947368421052,2.64999999999999));
#27276=CARTESIAN_POINT('Ctrl Pts',(3.87986928011505,23.0921052631579,3.87986928011504));
#27277=CARTESIAN_POINT('Ctrl Pts',(2.65,23.2894736842105,4.58993464005751));
#27278=CARTESIAN_POINT('Ctrl Pts',(1.42013071988495,23.4868421052631,5.29999999999999));
#27279=CARTESIAN_POINT('Ctrl Pts',(2.95822839457879E-28,23.6842105263158,
5.3));
#27280=CARTESIAN_POINT('Ctrl Pts',(-1.42013071988495,23.8815789473684,5.29999999999998));
#27281=CARTESIAN_POINT('Ctrl Pts',(-2.65,24.0789473684211,4.58993464005751));
#27282=CARTESIAN_POINT('Ctrl Pts',(-3.87986928011504,24.2763157894737,3.87986928011504));
#27283=CARTESIAN_POINT('Ctrl Pts',(-4.58993464005751,24.4736842105263,2.65));
#27284=CARTESIAN_POINT('Ctrl Pts',(-5.29999999999999,24.671052631579,1.42013071988495));
#27285=CARTESIAN_POINT('Ctrl Pts',(-5.29999999999999,24.8684210526316,3.24531401774024E-16));
#27286=CARTESIAN_POINT('Ctrl Pts',(-5.29999999999999,25.0657894736842,-1.42013071988495));
#27287=CARTESIAN_POINT('Ctrl Pts',(-4.58993464005751,25.2631578947368,-2.64999999999999));
#27288=CARTESIAN_POINT('Ctrl Pts',(-3.87986928011504,25.4605263157895,-3.87986928011504));
#27289=CARTESIAN_POINT('Ctrl Pts',(-2.65,25.6578947368421,-4.58993464005751));
#27290=CARTESIAN_POINT('Ctrl Pts',(-1.42013071988495,25.8552631578947,-5.29999999999999));
#27291=CARTESIAN_POINT('Ctrl Pts',(-6.49062803547834E-16,26.0526315789473,
-5.29999999999999));
#27292=CARTESIAN_POINT('Ctrl Pts',(1.42013071988495,26.25,-5.29999999999999));
#27293=CARTESIAN_POINT('Ctrl Pts',(2.64999999999999,26.4473684210526,-4.58993464005752));
#27294=CARTESIAN_POINT('Ctrl Pts',(3.87986928011504,26.6447368421052,-3.87986928011505));
#27295=CARTESIAN_POINT('Ctrl Pts',(4.58993464005751,26.8421052631579,-2.65));
#27296=CARTESIAN_POINT('Ctrl Pts',(5.29999999999999,27.0394736842105,-1.42013071988495));
#27297=CARTESIAN_POINT('Ctrl Pts',(5.29999999999999,27.2368421052632,-9.73594205320888E-16));
#27298=CARTESIAN_POINT('Ctrl Pts',(5.29999999999999,27.4342105263158,1.42013071988495));
#27299=CARTESIAN_POINT('Ctrl Pts',(4.58993464005752,27.6315789473685,2.64999999999999));
#27300=CARTESIAN_POINT('Ctrl Pts',(3.87986928011505,27.8289473684211,3.87986928011504));
#27301=CARTESIAN_POINT('Ctrl Pts',(2.65,28.0263157894737,4.58993464005751));
#27302=CARTESIAN_POINT('Ctrl Pts',(1.42013071988495,28.2236842105264,5.29999999999998));
#27303=CARTESIAN_POINT('Ctrl Pts',(3.42045158123173E-28,28.421052631579,
5.3));
#27304=CARTESIAN_POINT('Ctrl Pts',(-1.42013071988495,28.6184210526316,5.29999999999999));
#27305=CARTESIAN_POINT('Ctrl Pts',(-2.65,28.8157894736842,4.58993464005751));
#27306=CARTESIAN_POINT('Ctrl Pts',(-3.87986928011504,29.0131578947368,3.87986928011504));
#27307=CARTESIAN_POINT('Ctrl Pts',(-4.58993464005751,29.2105263157895,2.65));
#27308=CARTESIAN_POINT('Ctrl Pts',(-5.29999999999999,29.4078947368421,1.42013071988495));
#27309=CARTESIAN_POINT('Ctrl Pts',(-5.29999999999999,29.6052631578947,3.24531401774024E-16));
#27310=CARTESIAN_POINT('Ctrl Pts',(-5.29999999999999,29.8026315789473,-1.42013071988495));
#27311=CARTESIAN_POINT('Ctrl Pts',(-4.58993464005751,30.,-2.64999999999999));
#27312=CARTESIAN_POINT('Ctrl Pts',(-3.87986928011504,30.1973684210526,-3.87986928011504));
#27313=CARTESIAN_POINT('Ctrl Pts',(-2.65,30.3947368421053,-4.58993464005751));
#27314=CARTESIAN_POINT('Ctrl Pts',(-1.42013071988495,30.5921052631579,-5.29999999999999));
#27315=CARTESIAN_POINT('Ctrl Pts',(-6.49062803547783E-16,30.7894736842105,
-5.29999999999999));
#27316=CARTESIAN_POINT('Ctrl Pts',(1.42013071988495,30.9868421052631,-5.29999999999999));
#27317=CARTESIAN_POINT('Ctrl Pts',(2.64999999999999,31.1842105263158,-4.58993464005752));
#27318=CARTESIAN_POINT('Ctrl Pts',(3.87986928011504,31.3815789473684,-3.87986928011505));
#27319=CARTESIAN_POINT('Ctrl Pts',(4.58993464005751,31.578947368421,-2.65));
#27320=CARTESIAN_POINT('Ctrl Pts',(5.29999999999999,31.7763157894737,-1.42013071988495));
#27321=CARTESIAN_POINT('Ctrl Pts',(5.29999999999999,31.9736842105263,-9.73594205321085E-16));
#27322=CARTESIAN_POINT('Ctrl Pts',(5.29999999999999,32.1710526315789,1.42013071988495));
#27323=CARTESIAN_POINT('Ctrl Pts',(4.58993464005752,32.3684210526316,2.64999999999999));
#27324=CARTESIAN_POINT('Ctrl Pts',(3.87986928011505,32.5657894736842,3.87986928011504));
#27325=CARTESIAN_POINT('Ctrl Pts',(2.65,32.7631578947368,4.58993464005751));
#27326=CARTESIAN_POINT('Ctrl Pts',(1.42013071988495,32.9605263157895,5.29999999999999));
#27327=CARTESIAN_POINT('Ctrl Pts',(3.88267476788467E-28,33.1578947368421,
5.3));
#27328=CARTESIAN_POINT('Ctrl Pts',(-1.42013071988495,33.3552631578948,5.29999999999998));
#27329=CARTESIAN_POINT('Ctrl Pts',(-2.65,33.5526315789474,4.58993464005751));
#27330=CARTESIAN_POINT('Ctrl Pts',(-3.87986928011504,33.75,3.87986928011505));
#27331=CARTESIAN_POINT('Ctrl Pts',(-4.58993464005751,33.9473684210526,2.65));
#27332=CARTESIAN_POINT('Ctrl Pts',(-5.29999999999999,34.1447368421052,1.42013071988495));
#27333=CARTESIAN_POINT('Ctrl Pts',(-5.29999999999999,34.3421052631579,3.24531401774024E-16));
#27334=CARTESIAN_POINT('Ctrl Pts',(-5.29999999999999,34.5394736842105,-1.42013071988495));
#27335=CARTESIAN_POINT('Ctrl Pts',(-4.58993464005751,34.7368421052631,-2.65));
#27336=CARTESIAN_POINT('Ctrl Pts',(-3.87986928011504,34.9342105263158,-3.87986928011504));
#27337=CARTESIAN_POINT('Ctrl Pts',(-2.65,35.1315789473684,-4.58993464005751));
#27338=CARTESIAN_POINT('Ctrl Pts',(-1.42013071988495,35.328947368421,-5.29999999999999));
#27339=CARTESIAN_POINT('Ctrl Pts',(-6.49062803547736E-16,35.5263157894737,
-5.29999999999999));
#27340=CARTESIAN_POINT('Ctrl Pts',(1.42013071988495,35.7236842105263,-5.29999999999999));
#27341=CARTESIAN_POINT('Ctrl Pts',(2.64999999999999,35.9210526315789,-4.58993464005752));
#27342=CARTESIAN_POINT('Ctrl Pts',(3.87986928011504,36.1184210526315,-3.87986928011505));
#27343=CARTESIAN_POINT('Ctrl Pts',(4.58993464005751,36.3157894736842,-2.65));
#27344=CARTESIAN_POINT('Ctrl Pts',(5.29999999999999,36.5131578947368,-1.42013071988495));
#27345=CARTESIAN_POINT('Ctrl Pts',(5.29999999999999,36.7105263157895,-9.73594205322072E-16));
#27346=CARTESIAN_POINT('Ctrl Pts',(5.29999999999999,36.9078947368421,1.42013071988495));
#27347=CARTESIAN_POINT('Ctrl Pts',(4.58993464005752,37.1052631578948,2.64999999999999));
#27348=CARTESIAN_POINT('Ctrl Pts',(3.87986928011505,37.3026315789473,3.87986928011504));
#27349=CARTESIAN_POINT('Ctrl Pts',(2.65,37.5,4.58993464005751));
#27350=CARTESIAN_POINT('Ctrl Pts',(1.42013071988495,37.6973684210526,5.29999999999998));
#27351=CARTESIAN_POINT('Ctrl Pts',(4.42193515231309E-28,37.8947368421053,
5.29999999999999));
#27352=CARTESIAN_POINT('Ctrl Pts',(-1.42013071988495,38.0921052631579,5.29999999999999));
#27353=CARTESIAN_POINT('Ctrl Pts',(-2.65,38.2894736842105,4.58993464005752));
#27354=CARTESIAN_POINT('Ctrl Pts',(-3.87986928011504,38.4868421052632,3.87986928011504));
#27355=CARTESIAN_POINT('Ctrl Pts',(-4.58993464005751,38.6842105263158,2.65));
#27356=CARTESIAN_POINT('Ctrl Pts',(-5.29999999999999,38.8815789473684,1.42013071988495));
#27357=CARTESIAN_POINT('Ctrl Pts',(-5.29999999999999,39.078947368421,3.24531401774024E-16));
#27358=CARTESIAN_POINT('Ctrl Pts',(-5.29999999999999,39.2763157894737,-1.42013071988495));
#27359=CARTESIAN_POINT('Ctrl Pts',(-4.58993464005751,39.4736842105263,-2.64999999999999));
#27360=CARTESIAN_POINT('Ctrl Pts',(-3.87986928011504,39.6710526315789,-3.87986928011504));
#27361=CARTESIAN_POINT('Ctrl Pts',(-2.65,39.8684210526316,-4.58993464005751));
#27362=CARTESIAN_POINT('Ctrl Pts',(-1.42013071988495,40.0657894736842,-5.29999999999999));
#27363=CARTESIAN_POINT('Ctrl Pts',(-6.49062803547683E-16,40.2631578947368,
-5.29999999999999));
#27364=CARTESIAN_POINT('Ctrl Pts',(1.42013071988495,40.4605263157895,-5.29999999999999));
#27365=CARTESIAN_POINT('Ctrl Pts',(2.64999999999999,40.6578947368421,-4.58993464005752));
#27366=CARTESIAN_POINT('Ctrl Pts',(3.87986928011504,40.8552631578947,-3.87986928011505));
#27367=CARTESIAN_POINT('Ctrl Pts',(4.58993464005751,41.0526315789473,-2.65));
#27368=CARTESIAN_POINT('Ctrl Pts',(5.29999999999999,41.25,-1.42013071988495));
#27369=CARTESIAN_POINT('Ctrl Pts',(5.29999999999999,41.4473684210526,-9.73594205322072E-16));
#27370=CARTESIAN_POINT('Ctrl Pts',(5.29999999999999,41.6447368421053,1.42013071988495));
#27371=CARTESIAN_POINT('Ctrl Pts',(4.58993464005752,41.8421052631579,2.64999999999999));
#27372=CARTESIAN_POINT('Ctrl Pts',(3.87986928011505,42.0394736842106,3.87986928011504));
#27373=CARTESIAN_POINT('Ctrl Pts',(2.65,42.2368421052632,4.58993464005751));
#27374=CARTESIAN_POINT('Ctrl Pts',(1.42013071988495,42.4342105263158,5.29999999999999));
#27375=CARTESIAN_POINT('Ctrl Pts',(4.99201041585172E-28,42.6315789473684,
5.29999999999999));
#27376=CARTESIAN_POINT('Ctrl Pts',(-1.42013071988495,42.8289473684211,5.29999999999998));
#27377=CARTESIAN_POINT('Ctrl Pts',(-2.65,43.0263157894737,4.58993464005752));
#27378=CARTESIAN_POINT('Ctrl Pts',(-3.87986928011504,43.2236842105263,3.87986928011504));
#27379=CARTESIAN_POINT('Ctrl Pts',(-4.58993464005751,43.421052631579,2.65));
#27380=CARTESIAN_POINT('Ctrl Pts',(-5.29999999999999,43.6184210526316,1.42013071988495));
#27381=CARTESIAN_POINT('Ctrl Pts',(-5.29999999999999,43.8157894736842,3.24531401774024E-16));
#27382=CARTESIAN_POINT('Ctrl Pts',(-5.29999999999999,44.0131578947368,-1.42013071988495));
#27383=CARTESIAN_POINT('Ctrl Pts',(-4.58993464005751,44.2105263157895,-2.64999999999999));
#27384=CARTESIAN_POINT('Ctrl Pts',(-3.87986928011504,44.4078947368421,-3.87986928011504));
#27385=CARTESIAN_POINT('Ctrl Pts',(-2.65,44.6052631578947,-4.58993464005751));
#27386=CARTESIAN_POINT('Ctrl Pts',(-1.42013071988495,44.8026315789473,-5.29999999999999));
#27387=CARTESIAN_POINT('Ctrl Pts',(-6.49062803547635E-16,45.,-5.29999999999999));
#27388=CARTESIAN_POINT('Ctrl Pts',(1.42013071988495,45.1973684210526,-5.29999999999999));
#27389=CARTESIAN_POINT('Ctrl Pts',(2.64999999999999,45.3947368421053,-4.58993464005752));
#27390=CARTESIAN_POINT('Ctrl Pts',(3.87986928011504,45.5921052631579,-3.87986928011505));
#27391=CARTESIAN_POINT('Ctrl Pts',(4.58993464005751,45.7894736842105,-2.65));
#27392=CARTESIAN_POINT('Ctrl Pts',(5.29999999999999,45.9868421052631,-1.42013071988495));
#27393=CARTESIAN_POINT('Ctrl Pts',(5.29999999999999,46.1842105263158,-9.73594205321085E-16));
#27394=CARTESIAN_POINT('Ctrl Pts',(5.29999999999999,46.3815789473684,1.42013071988495));
#27395=CARTESIAN_POINT('Ctrl Pts',(4.58993464005752,46.5789473684211,2.64999999999999));
#27396=CARTESIAN_POINT('Ctrl Pts',(3.87986928011505,46.7763157894737,3.87986928011504));
#27397=CARTESIAN_POINT('Ctrl Pts',(2.65,46.9736842105263,4.58993464005752));
#27398=CARTESIAN_POINT('Ctrl Pts',(1.42013071988495,47.1710526315789,5.29999999999999));
#27399=CARTESIAN_POINT('Ctrl Pts',(5.54667823983524E-28,47.3684210526316,
5.29999999999999));
#27400=CARTESIAN_POINT('Ctrl Pts',(-1.42013071988495,47.5657894736842,5.29999999999998));
#27401=CARTESIAN_POINT('Ctrl Pts',(-2.65,47.7631578947368,4.58993464005752));
#27402=CARTESIAN_POINT('Ctrl Pts',(-3.87986928011504,47.9605263157895,3.87986928011504));
#27403=CARTESIAN_POINT('Ctrl Pts',(-4.58993464005751,48.1578947368421,2.65));
#27404=CARTESIAN_POINT('Ctrl Pts',(-5.29999999999999,48.3552631578947,1.42013071988495));
#27405=CARTESIAN_POINT('Ctrl Pts',(-5.29999999999999,48.5526315789474,3.24531401773827E-16));
#27406=CARTESIAN_POINT('Ctrl Pts',(-5.29999999999999,48.75,-1.42013071988495));
#27407=CARTESIAN_POINT('Ctrl Pts',(-4.58993464005751,48.9473684210526,-2.64999999999999));
#27408=CARTESIAN_POINT('Ctrl Pts',(-3.87986928011504,49.1447368421053,-3.87986928011504));
#27409=CARTESIAN_POINT('Ctrl Pts',(-2.65,49.3421052631579,-4.58993464005751));
#27410=CARTESIAN_POINT('Ctrl Pts',(-1.42013071988495,49.5394736842105,-5.29999999999999));
#27411=CARTESIAN_POINT('Ctrl Pts',(-6.49062803547579E-16,49.7368421052631,
-5.29999999999999));
#27412=CARTESIAN_POINT('Ctrl Pts',(1.42013071988495,49.9342105263158,-5.29999999999999));
#27413=CARTESIAN_POINT('Ctrl Pts',(2.64999999999999,50.1315789473684,-4.58993464005752));
#27414=CARTESIAN_POINT('Ctrl Pts',(3.87986928011504,50.328947368421,-3.87986928011505));
#27415=CARTESIAN_POINT('Ctrl Pts',(4.58993464005751,50.5263157894737,-2.65));
#27416=CARTESIAN_POINT('Ctrl Pts',(5.29999999999999,50.7236842105263,-1.42013071988495));
#27417=CARTESIAN_POINT('Ctrl Pts',(5.29999999999999,50.9210526315789,-9.73594205321085E-16));
#27418=CARTESIAN_POINT('Ctrl Pts',(5.29999999999999,51.1184210526316,1.42013071988495));
#27419=CARTESIAN_POINT('Ctrl Pts',(4.58993464005752,51.3157894736842,2.64999999999999));
#27420=CARTESIAN_POINT('Ctrl Pts',(3.87986928011505,51.5131578947368,3.87986928011504));
#27421=CARTESIAN_POINT('Ctrl Pts',(2.65,51.7105263157895,4.58993464005752));
#27422=CARTESIAN_POINT('Ctrl Pts',(1.42013071988495,51.9078947368421,5.29999999999998));
#27423=CARTESIAN_POINT('Ctrl Pts',(6.00890142648818E-28,52.1052631578948,
5.29999999999999));
#27424=CARTESIAN_POINT('Ctrl Pts',(-1.42013071988495,52.3026315789474,5.29999999999999));
#27425=CARTESIAN_POINT('Ctrl Pts',(-2.65,52.5,4.58993464005752));
#27426=CARTESIAN_POINT('Ctrl Pts',(-3.87986928011504,52.6973684210526,3.87986928011504));
#27427=CARTESIAN_POINT('Ctrl Pts',(-4.58993464005751,52.8947368421053,2.65));
#27428=CARTESIAN_POINT('Ctrl Pts',(-5.29999999999999,53.0921052631579,1.42013071988495));
#27429=CARTESIAN_POINT('Ctrl Pts',(-5.29999999999999,53.2894736842105,3.245314017757E-16));
#27430=CARTESIAN_POINT('Ctrl Pts',(-5.29999999999999,53.4868421052631,-1.42013071988495));
#27431=CARTESIAN_POINT('Ctrl Pts',(-4.58993464005751,53.6842105263158,-2.64999999999999));
#27432=CARTESIAN_POINT('Ctrl Pts',(-3.87986928011504,53.8815789473684,-3.87986928011504));
#27433=CARTESIAN_POINT('Ctrl Pts',(-2.65,54.0789473684211,-4.58993464005751));
#27434=CARTESIAN_POINT('Ctrl Pts',(-1.42013071988495,54.2763157894737,-5.29999999999999));
#27435=CARTESIAN_POINT('Ctrl Pts',(-6.4906280354753E-16,54.4736842105263,
-5.29999999999999));
#27436=CARTESIAN_POINT('Ctrl Pts',(1.42013071988495,54.6710526315789,-5.29999999999999));
#27437=CARTESIAN_POINT('Ctrl Pts',(2.64999999999999,54.8684210526316,-4.58993464005752));
#27438=CARTESIAN_POINT('Ctrl Pts',(3.87986928011504,55.0657894736842,-3.87986928011505));
#27439=CARTESIAN_POINT('Ctrl Pts',(4.58993464005751,55.2631578947368,-2.65));
#27440=CARTESIAN_POINT('Ctrl Pts',(5.29999999999999,55.4605263157895,-1.42013071988495));
#27441=CARTESIAN_POINT('Ctrl Pts',(5.29999999999999,55.6578947368421,-9.73594205321578E-16));
#27442=CARTESIAN_POINT('Ctrl Pts',(5.29999999999999,55.8552631578947,1.42013071988495));
#27443=CARTESIAN_POINT('Ctrl Pts',(4.58993464005752,56.0526315789474,2.64999999999999));
#27444=CARTESIAN_POINT('Ctrl Pts',(3.87986928011505,56.25,3.87986928011504));
#27445=CARTESIAN_POINT('Ctrl Pts',(2.65,56.4473684210526,4.58993464005752));
#27446=CARTESIAN_POINT('Ctrl Pts',(1.42013071988495,56.6447368421052,5.29999999999999));
#27447=CARTESIAN_POINT('Ctrl Pts',(6.5635692504717E-28,56.8421052631579,
5.29999999999999));
#27448=CARTESIAN_POINT('Ctrl Pts',(-1.42013071988495,57.0394736842105,5.29999999999998));
#27449=CARTESIAN_POINT('Ctrl Pts',(-2.65,57.2368421052632,4.58993464005752));
#27450=CARTESIAN_POINT('Ctrl Pts',(-3.87986928011504,57.4342105263158,3.87986928011504));
#27451=CARTESIAN_POINT('Ctrl Pts',(-4.58993464005751,57.6315789473684,2.65));
#27452=CARTESIAN_POINT('Ctrl Pts',(-5.29999999999999,57.8289473684211,1.42013071988495));
#27453=CARTESIAN_POINT('Ctrl Pts',(-5.29999999999999,58.0263157894737,3.24531401775207E-16));
#27454=CARTESIAN_POINT('Ctrl Pts',(-5.29999999999999,58.2236842105263,-1.42013071988495));
#27455=CARTESIAN_POINT('Ctrl Pts',(-4.58993464005751,58.4210526315789,-2.64999999999999));
#27456=CARTESIAN_POINT('Ctrl Pts',(-3.87986928011504,58.6184210526315,-3.87986928011504));
#27457=CARTESIAN_POINT('Ctrl Pts',(-2.65,58.8157894736842,-4.58993464005751));
#27458=CARTESIAN_POINT('Ctrl Pts',(-1.42013071988495,59.0131578947368,-5.29999999999999));
#27459=CARTESIAN_POINT('Ctrl Pts',(-6.49062803547473E-16,59.2105263157894,
-5.29999999999999));
#27460=CARTESIAN_POINT('Ctrl Pts',(1.42013071988495,59.4078947368421,-5.29999999999999));
#27461=CARTESIAN_POINT('Ctrl Pts',(2.64999999999999,59.6052631578947,-4.58993464005752));
#27462=CARTESIAN_POINT('Ctrl Pts',(3.87986928011504,59.8026315789473,-3.87986928011505));
#27463=CARTESIAN_POINT('Ctrl Pts',(4.58993464005751,60.,-2.65));
#27464=CARTESIAN_POINT('Ctrl Pts',(5.29999999999999,60.1973684210526,-1.42013071988495));
#27465=CARTESIAN_POINT('Ctrl Pts',(5.29999999999999,60.3947368421052,-9.73594205321184E-16));
#27466=CARTESIAN_POINT('Ctrl Pts',(5.29999999999999,60.5921052631579,1.42013071988495));
#27467=CARTESIAN_POINT('Ctrl Pts',(4.58993464005752,60.7894736842105,2.64999999999999));
#27468=CARTESIAN_POINT('Ctrl Pts',(3.87986928011505,60.9868421052632,3.87986928011504));
#27469=CARTESIAN_POINT('Ctrl Pts',(2.65,61.1842105263158,4.58993464005752));
#27470=CARTESIAN_POINT('Ctrl Pts',(1.42013071988495,61.3815789473684,5.29999999999998));
#27471=CARTESIAN_POINT('Ctrl Pts',(7.02579243712464E-28,61.5789473684211,
5.29999999999999));
#27472=CARTESIAN_POINT('Ctrl Pts',(-1.42013071988495,61.7763157894737,5.29999999999999));
#27473=CARTESIAN_POINT('Ctrl Pts',(-2.65,61.9736842105264,4.58993464005752));
#27474=CARTESIAN_POINT('Ctrl Pts',(-3.87986928011504,62.171052631579,3.87986928011505));
#27475=CARTESIAN_POINT('Ctrl Pts',(-4.58993464005751,62.3684210526316,2.65));
#27476=CARTESIAN_POINT('Ctrl Pts',(-5.29999999999999,62.5657894736842,1.42013071988495));
#27477=CARTESIAN_POINT('Ctrl Pts',(-5.29999999999999,62.7631578947368,3.24531401775109E-16));
#27478=CARTESIAN_POINT('Ctrl Pts',(-5.29999999999999,62.9605263157895,-1.42013071988495));
#27479=CARTESIAN_POINT('Ctrl Pts',(-4.58993464005751,63.1578947368421,-2.64999999999999));
#27480=CARTESIAN_POINT('Ctrl Pts',(-3.87986928011504,63.3552631578947,-3.87986928011504));
#27481=CARTESIAN_POINT('Ctrl Pts',(-2.65,63.5526315789474,-4.58993464005751));
#27482=CARTESIAN_POINT('Ctrl Pts',(-1.42013071988495,63.75,-5.29999999999999));
#27483=CARTESIAN_POINT('Ctrl Pts',(-6.49062803547422E-16,63.9473684210526,
-5.29999999999999));
#27484=CARTESIAN_POINT('Ctrl Pts',(1.42013071988495,64.1447368421053,-5.29999999999999));
#27485=CARTESIAN_POINT('Ctrl Pts',(2.64999999999999,64.3421052631579,-4.58993464005752));
#27486=CARTESIAN_POINT('Ctrl Pts',(3.87986928011504,64.5394736842105,-3.87986928011505));
#27487=CARTESIAN_POINT('Ctrl Pts',(4.58993464005751,64.7368421052632,-2.65));
#27488=CARTESIAN_POINT('Ctrl Pts',(5.29999999999999,64.9342105263157,-1.42013071988495));
#27489=CARTESIAN_POINT('Ctrl Pts',(5.29999999999999,65.1315789473684,-9.73594205320987E-16));
#27490=CARTESIAN_POINT('Ctrl Pts',(5.29999999999999,65.328947368421,1.42013071988495));
#27491=CARTESIAN_POINT('Ctrl Pts',(4.58993464005752,65.5263157894737,2.64999999999999));
#27492=CARTESIAN_POINT('Ctrl Pts',(3.87986928011505,65.7236842105264,3.87986928011504));
#27493=CARTESIAN_POINT('Ctrl Pts',(2.65,65.9210526315789,4.58993464005752));
#27494=CARTESIAN_POINT('Ctrl Pts',(1.42013071988495,66.1184210526315,5.29999999999999));
#27495=CARTESIAN_POINT('Ctrl Pts',(7.48801562377757E-28,66.3157894736842,
5.29999999999999));
#27496=CARTESIAN_POINT('Ctrl Pts',(-1.42013071988495,66.5131578947368,5.29999999999998));
#27497=CARTESIAN_POINT('Ctrl Pts',(-2.65,66.7105263157894,4.58993464005752));
#27498=CARTESIAN_POINT('Ctrl Pts',(-3.87986928011504,66.9078947368421,3.87986928011504));
#27499=CARTESIAN_POINT('Ctrl Pts',(-4.58993464005751,67.1052631578947,2.65));
#27500=CARTESIAN_POINT('Ctrl Pts',(-5.29999999999999,67.3026315789474,1.42013071988495));
#27501=CARTESIAN_POINT('Ctrl Pts',(-5.29999999999999,67.5,3.24531401774714E-16));
#27502=CARTESIAN_POINT('Ctrl Pts',(-5.29999999999999,67.6973684210526,-1.42013071988495));
#27503=CARTESIAN_POINT('Ctrl Pts',(-4.58993464005751,67.8947368421052,-2.64999999999999));
#27504=CARTESIAN_POINT('Ctrl Pts',(-3.87986928011504,68.0921052631578,-3.87986928011504));
#27505=CARTESIAN_POINT('Ctrl Pts',(-2.65,68.2894736842105,-4.58993464005751));
#27506=CARTESIAN_POINT('Ctrl Pts',(-1.42013071988495,68.4868421052632,-5.29999999999999));
#27507=CARTESIAN_POINT('Ctrl Pts',(-6.49062803547376E-16,68.6842105263158,
-5.29999999999999));
#27508=CARTESIAN_POINT('Ctrl Pts',(1.42013071988495,68.8815789473684,-5.29999999999999));
#27509=CARTESIAN_POINT('Ctrl Pts',(2.64999999999999,69.078947368421,-4.58993464005752));
#27510=CARTESIAN_POINT('Ctrl Pts',(3.87986928011504,69.2763157894736,-3.87986928011505));
#27511=CARTESIAN_POINT('Ctrl Pts',(4.58993464005751,69.4736842105263,-2.65));
#27512=CARTESIAN_POINT('Ctrl Pts',(5.29999999999999,69.6710526315789,-1.42013071988495));
#27513=CARTESIAN_POINT('Ctrl Pts',(5.29999999999999,69.8684210526316,-9.73594205320888E-16));
#27514=CARTESIAN_POINT('Ctrl Pts',(5.29999999999999,70.0657894736842,1.42013071988495));
#27515=CARTESIAN_POINT('Ctrl Pts',(4.58993464005752,70.2631578947369,2.64999999999999));
#27516=CARTESIAN_POINT('Ctrl Pts',(3.87986928011505,70.4605263157895,3.87986928011504));
#27517=CARTESIAN_POINT('Ctrl Pts',(2.65,70.6578947368421,4.58993464005752));
#27518=CARTESIAN_POINT('Ctrl Pts',(1.42013071988495,70.8552631578947,5.29999999999998));
#27519=CARTESIAN_POINT('Ctrl Pts',(7.96564624998561E-28,71.0526315789473,
5.29999999999999));
#27520=CARTESIAN_POINT('Ctrl Pts',(-1.42013071988495,71.2499999999999,5.29999999999999));
#27521=CARTESIAN_POINT('Ctrl Pts',(-2.65,71.4473684210526,4.58993464005751));
#27522=CARTESIAN_POINT('Ctrl Pts',(-3.87986928011504,71.6447368421053,3.87986928011504));
#27523=CARTESIAN_POINT('Ctrl Pts',(-4.58993464005751,71.8421052631579,2.65));
#27524=CARTESIAN_POINT('Ctrl Pts',(-5.29999999999999,72.0394736842105,1.42013071988495));
#27525=CARTESIAN_POINT('Ctrl Pts',(-5.29999999999999,72.2368421052632,3.24531401775306E-16));
#27526=CARTESIAN_POINT('Ctrl Pts',(-5.29999999999999,72.4342105263157,-1.42013071988495));
#27527=CARTESIAN_POINT('Ctrl Pts',(-4.58993464005751,72.6315789473684,-2.64999999999999));
#27528=CARTESIAN_POINT('Ctrl Pts',(-3.87986928011504,72.828947368421,-3.87986928011504));
#27529=CARTESIAN_POINT('Ctrl Pts',(-2.65,73.0263157894737,-4.58993464005751));
#27530=CARTESIAN_POINT('Ctrl Pts',(-1.42013071988495,73.2236842105263,-5.29999999999999));
#27531=CARTESIAN_POINT('Ctrl Pts',(-6.4906280354732E-16,73.421052631579,
-5.29999999999999));
#27532=CARTESIAN_POINT('Ctrl Pts',(1.42013071988495,73.6184210526315,-5.29999999999999));
#27533=CARTESIAN_POINT('Ctrl Pts',(2.64999999999999,73.8157894736842,-4.58993464005751));
#27534=CARTESIAN_POINT('Ctrl Pts',(3.87986928011504,74.0131578947368,-3.87986928011505));
#27535=CARTESIAN_POINT('Ctrl Pts',(4.58993464005751,74.2105263157895,-2.65));
#27536=CARTESIAN_POINT('Ctrl Pts',(5.29999999999999,74.4078947368421,-1.42013071988495));
#27537=CARTESIAN_POINT('Ctrl Pts',(5.29999999999999,74.6052631578947,-9.73594205321085E-16));
#27538=CARTESIAN_POINT('Ctrl Pts',(5.29999999999999,74.8026315789473,1.42013071988495));
#27539=CARTESIAN_POINT('Ctrl Pts',(4.58993464005752,75.,2.64999999999999));
#27540=CARTESIAN_POINT('Ctrl Pts',(3.87986928011505,75.1973684210526,3.87986928011504));
#27541=CARTESIAN_POINT('Ctrl Pts',(2.65,75.3947368421052,4.58993464005751));
#27542=CARTESIAN_POINT('Ctrl Pts',(1.42013071988495,75.5921052631578,5.29999999999998));
#27543=CARTESIAN_POINT('Ctrl Pts',(8.68979590907521E-28,75.7894736842105,
5.29999999999999));
#27544=CARTESIAN_POINT('Ctrl Pts',(-1.42013071988495,75.9868421052631,5.29999999999999));
#27545=CARTESIAN_POINT('Ctrl Pts',(-2.65,76.1842105263158,4.58993464005751));
#27546=CARTESIAN_POINT('Ctrl Pts',(-3.87986928011504,76.3815789473684,3.87986928011504));
#27547=CARTESIAN_POINT('Ctrl Pts',(-4.58993464005751,76.5789473684211,2.65));
#27548=CARTESIAN_POINT('Ctrl Pts',(-5.29999999999999,76.7763157894737,1.42013071988495));
#27549=CARTESIAN_POINT('Ctrl Pts',(-5.29999999999999,76.9736842105263,3.24531401774615E-16));
#27550=CARTESIAN_POINT('Ctrl Pts',(-5.29999999999999,77.1710526315789,-1.42013071988495));
#27551=CARTESIAN_POINT('Ctrl Pts',(-4.58993464005751,77.3684210526315,-2.64999999999999));
#27552=CARTESIAN_POINT('Ctrl Pts',(-3.87986928011504,77.5657894736842,-3.87986928011504));
#27553=CARTESIAN_POINT('Ctrl Pts',(-2.65,77.7631578947368,-4.58993464005751));
#27554=CARTESIAN_POINT('Ctrl Pts',(-1.42013071988495,77.9605263157895,-5.29999999999999));
#27555=CARTESIAN_POINT('Ctrl Pts',(-6.49062803547265E-16,78.1578947368421,
-5.29999999999999));
#27556=CARTESIAN_POINT('Ctrl Pts',(1.42013071988495,78.3552631578948,-5.29999999999999));
#27557=CARTESIAN_POINT('Ctrl Pts',(2.64999999999999,78.5526315789474,-4.58993464005751));
#27558=CARTESIAN_POINT('Ctrl Pts',(3.87986928011504,78.7499999999999,-3.87986928011505));
#27559=CARTESIAN_POINT('Ctrl Pts',(4.58993464005751,78.9473684210526,-2.65));
#27560=CARTESIAN_POINT('Ctrl Pts',(5.29999999999999,79.1447368421052,-1.42013071988495));
#27561=CARTESIAN_POINT('Ctrl Pts',(5.29999999999999,79.3421052631579,-9.73594205320987E-16));
#27562=CARTESIAN_POINT('Ctrl Pts',(5.29999999999999,79.5394736842105,1.42013071988495));
#27563=CARTESIAN_POINT('Ctrl Pts',(4.58993464005752,79.7368421052632,2.64999999999999));
#27564=CARTESIAN_POINT('Ctrl Pts',(3.87986928011505,79.9342105263158,3.87986928011504));
#27565=CARTESIAN_POINT('Ctrl Pts',(2.65,80.1315789473684,4.58993464005751));
#27566=CARTESIAN_POINT('Ctrl Pts',(1.42013071988495,80.328947368421,5.29999999999999));
#27567=CARTESIAN_POINT('Ctrl Pts',(9.15201909572814E-28,80.5263157894736,
5.3));
#27568=CARTESIAN_POINT('Ctrl Pts',(-1.42013071988495,80.7236842105263,5.29999999999998));
#27569=CARTESIAN_POINT('Ctrl Pts',(-2.65,80.9210526315789,4.58993464005751));
#27570=CARTESIAN_POINT('Ctrl Pts',(-3.87986928011504,81.1184210526315,3.87986928011504));
#27571=CARTESIAN_POINT('Ctrl Pts',(-4.58993464005751,81.3157894736842,2.64999999999999));
#27572=CARTESIAN_POINT('Ctrl Pts',(-5.29999999999999,81.5131578947368,1.42013071988495));
#27573=CARTESIAN_POINT('Ctrl Pts',(-5.29999999999999,81.7105263157895,3.24531401775207E-16));
#27574=CARTESIAN_POINT('Ctrl Pts',(-5.29999999999999,81.9078947368421,-1.42013071988495));
#27575=CARTESIAN_POINT('Ctrl Pts',(-4.58993464005751,82.1052631578947,-2.64999999999999));
#27576=CARTESIAN_POINT('Ctrl Pts',(-3.87986928011504,82.3026315789473,-3.87986928011504));
#27577=CARTESIAN_POINT('Ctrl Pts',(-2.65,82.5,-4.58993464005751));
#27578=CARTESIAN_POINT('Ctrl Pts',(-1.42013071988495,82.6973684210527,-5.29999999999999));
#27579=CARTESIAN_POINT('Ctrl Pts',(-6.49062803547219E-16,82.8947368421053,
-5.29999999999999));
#27580=CARTESIAN_POINT('Ctrl Pts',(1.42013071988495,83.0921052631579,-5.29999999999999));
#27581=CARTESIAN_POINT('Ctrl Pts',(2.64999999999999,83.2894736842105,-4.58993464005751));
#27582=CARTESIAN_POINT('Ctrl Pts',(3.87986928011504,83.4868421052631,-3.87986928011505));
#27583=CARTESIAN_POINT('Ctrl Pts',(4.58993464005751,83.6842105263158,-2.65));
#27584=CARTESIAN_POINT('Ctrl Pts',(5.29999999999999,83.8815789473684,-1.42013071988495));
#27585=CARTESIAN_POINT('Ctrl Pts',(5.29999999999999,84.078947368421,-9.73594205321184E-16));
#27586=CARTESIAN_POINT('Ctrl Pts',(5.29999999999999,84.2763157894736,1.42013071988495));
#27587=CARTESIAN_POINT('Ctrl Pts',(4.58993464005752,84.4736842105263,2.64999999999999));
#27588=CARTESIAN_POINT('Ctrl Pts',(3.87986928011505,84.6710526315789,3.87986928011504));
#27589=CARTESIAN_POINT('Ctrl Pts',(2.65,84.8684210526316,4.58993464005751));
#27590=CARTESIAN_POINT('Ctrl Pts',(1.42013071988495,85.0657894736842,5.29999999999998));
#27591=CARTESIAN_POINT('Ctrl Pts',(9.61424228238108E-28,85.2631578947368,
5.3));
#27592=CARTESIAN_POINT('Ctrl Pts',(-1.42013071988495,85.4605263157894,5.29999999999999));
#27593=CARTESIAN_POINT('Ctrl Pts',(-2.65,85.6578947368421,4.58993464005751));
#27594=CARTESIAN_POINT('Ctrl Pts',(-3.87986928011504,85.8552631578947,3.87986928011504));
#27595=CARTESIAN_POINT('Ctrl Pts',(-4.58993464005751,86.0526315789474,2.65));
#27596=CARTESIAN_POINT('Ctrl Pts',(-5.29999999999999,86.25,1.42013071988495));
#27597=CARTESIAN_POINT('Ctrl Pts',(-5.29999999999999,86.4473684210526,3.24531401775207E-16));
#27598=CARTESIAN_POINT('Ctrl Pts',(-5.29999999999999,86.6447368421052,-1.42013071988495));
#27599=CARTESIAN_POINT('Ctrl Pts',(-4.58993464005751,86.8421052631579,-2.64999999999999));
#27600=CARTESIAN_POINT('Ctrl Pts',(-3.87986928011504,87.0394736842105,-3.87986928011504));
#27601=CARTESIAN_POINT('Ctrl Pts',(-2.65,87.2368421052631,-4.58993464005751));
#27602=CARTESIAN_POINT('Ctrl Pts',(-1.42013071988495,87.4342105263158,-5.29999999999999));
#27603=CARTESIAN_POINT('Ctrl Pts',(-6.49062803547173E-16,87.6315789473684,
-5.29999999999999));
#27604=CARTESIAN_POINT('Ctrl Pts',(1.42013071988495,87.828947368421,-5.29999999999999));
#27605=CARTESIAN_POINT('Ctrl Pts',(2.64999999999999,88.0263157894737,-4.58993464005751));
#27606=CARTESIAN_POINT('Ctrl Pts',(3.87986928011504,88.2236842105263,-3.87986928011505));
#27607=CARTESIAN_POINT('Ctrl Pts',(4.58993464005751,88.4210526315789,-2.65));
#27608=CARTESIAN_POINT('Ctrl Pts',(5.29999999999999,88.6184210526316,-1.42013071988495));
#27609=CARTESIAN_POINT('Ctrl Pts',(5.29999999999999,88.8157894736842,-9.73594205321085E-16));
#27610=CARTESIAN_POINT('Ctrl Pts',(5.29999999999999,89.0131578947368,1.42013071988495));
#27611=CARTESIAN_POINT('Ctrl Pts',(4.58993464005752,89.2105263157895,2.64999999999999));
#27612=CARTESIAN_POINT('Ctrl Pts',(3.87986928011505,89.4078947368421,3.87986928011504));
#27613=CARTESIAN_POINT('Ctrl Pts',(2.65,89.6052631578947,4.58993464005751));
#27614=CARTESIAN_POINT('Ctrl Pts',(1.42013071988495,89.8026315789473,5.29999999999999));
#27615=CARTESIAN_POINT('Ctrl Pts',(1.01689101063646E-27,89.9999999999999,
5.3));
#27616=CARTESIAN_POINT('Ctrl Pts',(-1.11022302462516E-15,90.,5.3));
#27617=CARTESIAN_POINT('Ctrl Pts',(0.705100735517942,90.,5.29999999999999));
#27618=CARTESIAN_POINT('Ctrl Pts',(1.4049232938638,90.,5.16650652249293));
#27619=CARTESIAN_POINT('Ctrl Pts',(2.30127966598412,90.,4.81265289415681));
#27620=CARTESIAN_POINT('Ctrl Pts',(2.53381374000113,90.,4.70178046144737));
#27621=CARTESIAN_POINT('Ctrl Pts',(3.38128440167258,90.,4.22331897236908));
#27622=CARTESIAN_POINT('Ctrl Pts',(3.93207008557601,90.,3.75829552364623));
#27623=CARTESIAN_POINT('Ctrl Pts',(4.62745111738881,90.,2.90535644419948));
#27624=CARTESIAN_POINT('Ctrl Pts',(4.84005013405767,90.,2.58173505428712));
#27625=CARTESIAN_POINT('Ctrl Pts',(5.20015385755245,90.,1.9003141675501));
#27626=CARTESIAN_POINT('Ctrl Pts',(5.3477175335123,90.,1.53988706209255));
#27627=CARTESIAN_POINT('Ctrl Pts',(5.73877457275006,90.,0.239224399660193));
#27628=CARTESIAN_POINT('Ctrl Pts',(5.75207974392297,90.,-0.612754734201201));
#27629=CARTESIAN_POINT('Ctrl Pts',(5.58692017936483,90.,-2.20371577024327));
#27630=CARTESIAN_POINT('Ctrl Pts',(5.30528429685785,90.,-3.05722906998427));
#27631=CARTESIAN_POINT('Ctrl Pts',(4.41388010965142,90.,-4.76270163974273));
#27632=CARTESIAN_POINT('Ctrl Pts',(3.88988452656918,90.0000000000059,-5.3939572843751));
#27633=CARTESIAN_POINT('Ctrl Pts',(3.51744452299761,90.0000000000059,-5.97932511428333));
#27634=CARTESIAN_POINT('Ctrl Pts',(3.46100601870892,90.,-6.08614105674003));
#27635=CARTESIAN_POINT('Ctrl Pts',(3.41267186745819,90.,-6.22249169412421));
#27636=CARTESIAN_POINT('Ctrl Pts',(3.39968442225245,90.,-6.27278714382266));
#27637=CARTESIAN_POINT('Ctrl Pts',(3.39615776458109,90.,-6.35191890437968));
#27638=CARTESIAN_POINT('Ctrl Pts',(3.3988649016033,90.,-6.38210532885075));
#27639=CARTESIAN_POINT('Ctrl Pts',(3.41578433719734,90.,-6.43733794772286));
#27640=CARTESIAN_POINT('Ctrl Pts',(3.4285533280344,90.0000000000201,-6.4611916715849));
#27641=CARTESIAN_POINT('Ctrl Pts',(3.4673290106001,90.0000000000201,-6.50808285636127));
#27642=CARTESIAN_POINT('Ctrl Pts',(3.49403994958472,90.0000000000001,-6.52813135760766));
#27643=CARTESIAN_POINT('Ctrl Pts',(3.57279538848092,90.0000000000001,-6.57029447033136));
#27644=CARTESIAN_POINT('Ctrl Pts',(3.63078887712831,90.,-6.58503381585687));
#27645=CARTESIAN_POINT('Ctrl Pts',(3.79711934339588,90.,-6.60906710879125));
#27646=CARTESIAN_POINT('Ctrl Pts',(3.92236333330237,90.,-6.6017658708962));
#27647=CARTESIAN_POINT('Ctrl Pts',(4.35612042347956,90.,-6.54400669481274));
#27648=CARTESIAN_POINT('Ctrl Pts',(4.78534531728318,90.0000000000001,-6.40675881673715));
#27649=CARTESIAN_POINT('Ctrl Pts',(5.85107880669982,90.0000000000001,-5.83387569838342));
#27650=CARTESIAN_POINT('Ctrl Pts',(6.48172283195264,90.,-5.34839112546546));
#27651=CARTESIAN_POINT('Ctrl Pts',(7.64464329931856,90.,-3.9916659757713));
#27652=CARTESIAN_POINT('Ctrl Pts',(8.17812076497661,90.,-3.10007009428681));
#27653=CARTESIAN_POINT('Ctrl Pts',(8.90148181129173,90.,-0.887883537440906));
#27654=CARTESIAN_POINT('Ctrl Pts',(8.98096602140476,89.9999999997875,0.240626946476822));
#27655=CARTESIAN_POINT('Ctrl Pts',(8.80307772603727,89.9999999997875,2.35592379430447));
#27656=CARTESIAN_POINT('Ctrl Pts',(8.48937235653017,90.,3.44640186127508));
#27657=CARTESIAN_POINT('Ctrl Pts',(7.84903191346606,90.,4.69681107334978));
#27658=CARTESIAN_POINT('Ctrl Pts',(7.70886753716707,90.,4.94099545221441));
#27659=CARTESIAN_POINT('Ctrl Pts',(6.95641557015424,90.,6.11888992491444));
#27660=CARTESIAN_POINT('Ctrl Pts',(6.18323092075226,90.,6.93754127757638));
#27661=CARTESIAN_POINT('Ctrl Pts',(4.86855345588626,90.,7.88920095492676));
#27662=CARTESIAN_POINT('Ctrl Pts',(4.43381295061861,90.,8.15052437235101));
#27663=CARTESIAN_POINT('Ctrl Pts',(3.34564146975116,90.,8.68638626613442));
#27664=CARTESIAN_POINT('Ctrl Pts',(2.67551791995553,89.9999999999999,8.92322547450994));
#27665=CARTESIAN_POINT('Ctrl Pts',(1.65577548687742,89.9999999999999,9.15323079586583));
#27666=CARTESIAN_POINT('Ctrl Pts',(1.32324826699197,89.9999999999954,9.20885494539258));
#27667=CARTESIAN_POINT('Ctrl Pts',(0.660151381649946,89.9999999999954,9.28190034665736));
#27668=CARTESIAN_POINT('Ctrl Pts',(0.330207854361134,90.,9.29999999999998));
#27669=CARTESIAN_POINT('Ctrl Pts',(1.17961196366423E-14,90.,9.29999999999998));
#27670=CARTESIAN_POINT('Ctrl Pts',(-3.46944695195361E-17,-3.22290425329321E-15,
5.29999999999999));
#27671=CARTESIAN_POINT('Ctrl Pts',(-0.169644532845145,-3.22267314244815E-15,
5.29999999999999));
#27672=CARTESIAN_POINT('Ctrl Pts',(-0.339214759582775,1.69602044929706E-12,
5.2922718595307));
#27673=CARTESIAN_POINT('Ctrl Pts',(-0.680184164497541,1.69602044929706E-12,
5.26118280144906));
#27674=CARTESIAN_POINT('Ctrl Pts',(-0.851408033835457,-2.72945075257972E-15,
5.23755326103085));
#27675=CARTESIAN_POINT('Ctrl Pts',(-1.37651569900196,-2.70949669069754E-15,
5.14023686030182));
#27676=CARTESIAN_POINT('Ctrl Pts',(-1.72474458805228,-3.73063229218745E-15,
5.04025101866987));
#27677=CARTESIAN_POINT('Ctrl Pts',(-2.30127966599588,-3.70905464750116E-15,
4.81265289415161));
#27678=CARTESIAN_POINT('Ctrl Pts',(-2.53381374001407,-3.36411559846784E-15,
4.70178046144089));
#27679=CARTESIAN_POINT('Ctrl Pts',(-3.38128440168497,-3.31624161775105E-15,
4.22331897235982));
#27680=CARTESIAN_POINT('Ctrl Pts',(-3.93207008558682,-3.10712189669725E-15,
3.75829552363584));
#27681=CARTESIAN_POINT('Ctrl Pts',(-4.62745111739741,-3.00622202880969E-15,
2.90535644418744));
#27682=CARTESIAN_POINT('Ctrl Pts',(-4.84005013406567,-2.86023292837575E-15,
2.58173505427411));
#27683=CARTESIAN_POINT('Ctrl Pts',(-5.20015385755875,-2.76909805416762E-15,
1.90031416753604));
#27684=CARTESIAN_POINT('Ctrl Pts',(-5.34771753351767,3.39051007573177E-14,
1.53988706207808));
#27685=CARTESIAN_POINT('Ctrl Pts',(-5.73877457275226,3.40242515497888E-14,
0.239224399644201));
#27686=CARTESIAN_POINT('Ctrl Pts',(-5.75207974392291,-3.39098433734155E-15,
-0.612754734217791));
#27687=CARTESIAN_POINT('Ctrl Pts',(-5.58692017936078,-3.20318749950661E-15,
-2.20371577025992));
#27688=CARTESIAN_POINT('Ctrl Pts',(-5.30528429685125,-2.68925673330566E-15,
-3.05722907000087));
#27689=CARTESIAN_POINT('Ctrl Pts',(-4.41388010964463,-2.49467807752504E-15,
-4.76270163975131));
#27690=CARTESIAN_POINT('Ctrl Pts',(-3.88988452656653,-5.92898608183421E-12,
-5.3939572843788));
#27691=CARTESIAN_POINT('Ctrl Pts',(-3.51744452299239,-5.92890982212414E-12,
-5.97932511429165));
#27692=CARTESIAN_POINT('Ctrl Pts',(-3.46100601870684,-2.78405185707395E-15,
-6.08614105674537));
#27693=CARTESIAN_POINT('Ctrl Pts',(-3.41267186745706,-2.76558424548778E-15,
-6.22249169412705));
#27694=CARTESIAN_POINT('Ctrl Pts',(-3.39968442225255,-2.23295764606424E-15,
-6.27278714382351));
#27695=CARTESIAN_POINT('Ctrl Pts',(-3.39615776458133,-2.22289674085925E-15,
-6.35191890437837));
#27696=CARTESIAN_POINT('Ctrl Pts',(-3.39886490160313,-3.34829527742224E-15,
-6.38210532885045));
#27697=CARTESIAN_POINT('Ctrl Pts',(-3.41578433719774,-3.34140661391927E-15,
-6.43733794772428));
#27698=CARTESIAN_POINT('Ctrl Pts',(-3.42855332803508,-2.0063968588949E-11,
-6.46119167158541));
#27699=CARTESIAN_POINT('Ctrl Pts',(-3.46732901060007,-2.00639629001137E-11,
-6.50808285636085));
#27700=CARTESIAN_POINT('Ctrl Pts',(-3.49403994958348,-2.22765705204529E-15,
-6.52813135760707));
#27701=CARTESIAN_POINT('Ctrl Pts',(-3.57279538848081,-2.22376902594429E-15,
-6.5702944703313));
#27702=CARTESIAN_POINT('Ctrl Pts',(-3.63078887712726,-2.21658829378393E-15,
-6.58503381585689));
#27703=CARTESIAN_POINT('Ctrl Pts',(-3.79711934339621,-2.2129999729789E-15,
-6.60906710879137));
#27704=CARTESIAN_POINT('Ctrl Pts',(-3.9223633333031,-1.1011763607202E-15,
-6.60176587089621));
#27705=CARTESIAN_POINT('Ctrl Pts',(-4.35612042348101,-1.1011763607202E-15,
-6.54400669481249));
#27706=CARTESIAN_POINT('Ctrl Pts',(-4.78534531728578,-1.58613680503368E-15,
-6.40675881673634));
#27707=CARTESIAN_POINT('Ctrl Pts',(-5.85107880670852,-1.66733944063455E-15,
-5.83387569837821));
#27708=CARTESIAN_POINT('Ctrl Pts',(-6.48172283196021,-3.9730222950244E-15,
-5.34839112545779));
#27709=CARTESIAN_POINT('Ctrl Pts',(-7.64464329931948,-4.13836029449498E-15,
-3.99166597576912));
#27710=CARTESIAN_POINT('Ctrl Pts',(-8.17812076497821,-3.19046254333735E-15,
-3.10007009428486));
#27711=CARTESIAN_POINT('Ctrl Pts',(-8.90148181129361,-3.46494457383746E-15,
-0.887883537432394));
#27712=CARTESIAN_POINT('Ctrl Pts',(-8.98096602140475,2.12463464266943E-10,
0.240626946485903));
#27713=CARTESIAN_POINT('Ctrl Pts',(-8.8030777260359,2.12463194834947E-10,
2.3559237943109));
#27714=CARTESIAN_POINT('Ctrl Pts',(-8.48937235652788,-2.82135042331067E-15,
3.44640186128145));
#27715=CARTESIAN_POINT('Ctrl Pts',(-7.84903191346284,-2.94513386976895E-15,
4.69681107335558));
#27716=CARTESIAN_POINT('Ctrl Pts',(-7.70886753716375,-3.79933706437609E-15,
4.94099545221998));
#27717=CARTESIAN_POINT('Ctrl Pts',(-6.95641557015005,-3.92492878533535E-15,
6.11888992491946));
#27718=CARTESIAN_POINT('Ctrl Pts',(-6.18323092074754,-3.63640987014422E-15,
6.93754127758076));
#27719=CARTESIAN_POINT('Ctrl Pts',(-4.86855345588147,-3.72862351382448E-15,
7.88920095492979));
#27720=CARTESIAN_POINT('Ctrl Pts',(-4.4338129506142,-3.2452453412235E-15,
8.15052437235346));
#27721=CARTESIAN_POINT('Ctrl Pts',(-3.34564146974786,-3.30469395986477E-15,
8.68638626613567));
#27722=CARTESIAN_POINT('Ctrl Pts',(-2.67551791995298,-3.67618129863226E-15,
8.92322547451067));
#27723=CARTESIAN_POINT('Ctrl Pts',(-1.33313154318946,-3.71996106794212E-15,
9.22600390164642));
#27724=CARTESIAN_POINT('Ctrl Pts',(-0.667662034038393,-3.71105124528613E-15,
9.29999999999998));
#27725=CARTESIAN_POINT('Ctrl Pts',(1.38777878078145E-16,-3.71274633697002E-15,
9.29999999999998));
#27726=CARTESIAN_POINT('Origin',(-9.29999999999998,0.,-21.4633238078319));
#27727=CARTESIAN_POINT('Origin',(-9.29999999999998,90.,-21.4633238078319));
#32968=UNCERTAINTY_MEASURE_WITH_UNIT(LENGTH_MEASURE(0.01),#33017,
'DISTANCE_ACCURACY_VALUE',
'Maximum model space distance between geometric entities at asserted c
onnectivities');
#32984=UNCERTAINTY_MEASURE_WITH_UNIT(LENGTH_MEASURE(0.01),#33017,
'DISTANCE_ACCURACY_VALUE',
'Maximum model space distance between geometric entities at asserted c
onnectivities');
#33000=(
GEOMETRIC_REPRESENTATION_CONTEXT(3)
GLOBAL_UNCERTAINTY_ASSIGNED_CONTEXT((#32968))
GLOBAL_UNIT_ASSIGNED_CONTEXT((#33017,#33019,#33020))
REPRESENTATION_CONTEXT('','3D')
);
#33016=(
GEOMETRIC_REPRESENTATION_CONTEXT(3)
GLOBAL_UNCERTAINTY_ASSIGNED_CONTEXT((#32984))
GLOBAL_UNIT_ASSIGNED_CONTEXT((#33017,#33019,#33020))
REPRESENTATION_CONTEXT('','3D')
);
#33017=(
LENGTH_UNIT()
NAMED_UNIT(*)
SI_UNIT(.MILLI.,.METRE.)
);
#33019=(
NAMED_UNIT(*)
PLANE_ANGLE_UNIT()
SI_UNIT($,.RADIAN.)
);
#33020=(
NAMED_UNIT(*)
SI_UNIT($,.STERADIAN.)
SOLID_ANGLE_UNIT()
);
#33036=SHAPE_DEFINITION_REPRESENTATION(#33075,#33139);
#33075=PRODUCT_DEFINITION_SHAPE('',$,#33171);
#33139=SHAPE_REPRESENTATION('',(#10807),#33000);
#33155=PRODUCT_DEFINITION_CONTEXT('part definition',#33250,'design');
#33171=PRODUCT_DEFINITION(
'BO21-002_Spring_PUR-HW-4060_18.5T_4 mm x 18.6 mm x 100 mm (C)',
'PUR-HW-4060',#33202,#33155);
#33202=PRODUCT_DEFINITION_FORMATION('',$,#33267);
#33250=APPLICATION_CONTEXT(
'Core Data for Automotive Mechanical Design Process');
#33251=PRODUCT_CONTEXT('part definition',#33250,'mechanical');
#33267=PRODUCT(
'BO21-002_Spring_PUR-HW-4060_18.5T_4 mm x 18.6 mm x 100 mm (C)',
'PUR-HW-4060',$,(#33251));
#33285=PRESENTATION_STYLE_ASSIGNMENT((#33292));
#33292=SURFACE_STYLE_USAGE(.BOTH.,#33299);
#33299=SURFACE_SIDE_STYLE('',(#33306));
#33306=SURFACE_STYLE_FILL_AREA(#33313);
#33313=FILL_AREA_STYLE('Opaque(202,209,238)',(#33320));
#33320=FILL_AREA_STYLE_COLOUR('Opaque(202,209,238)',#33327);
#33327=COLOUR_RGB('Opaque(202,209,238)', 0.08235294, 0.09019608, 0.10196078);
ENDSEC;
END-ISO-10303-21;
